ISO-10303-21;
HEADER;
/* Generated by software containing ST-Developer
 * from STEP Tools, Inc. (www.steptools.com) 
 */

FILE_DESCRIPTION(
/* description */ ('Independent direct-acting normally-closed roller-plunger limit-switch
 CAD. Removable cover, insulated terminal supports, captured bus/conta
ct bridge, native Coil return spring, integral lower travel stop, reus
able instanced hardware and free roller. Manual geometric contact open
ing4mm; no snap-action/contact-force, electrical/current/voltage, envi
ronmental seal, safety-switch, wear, load or life certification. Exter
nal wiring and anchors omitted; fits and application engineering requi
red.'),
/* implementation_level */ '2;1');

FILE_NAME(
/* name */ 'Socket head cap screw M3x10.step',
/* time_stamp */ '2026-11-08T07:32:43-08:00',
/* author */ (''),
/* organization */ (''),
/* preprocessor_version */ 'ST-DEVELOPER v20.2',
/* originating_system */ 'Autodesk Translation Framework v15.17.0.0',
/* authorisation */ '');

FILE_SCHEMA (('AUTOMOTIVE_DESIGN { 1 0 10303 214 3 1 1 }'));
ENDSEC;

DATA;
#10=MECHANICAL_DESIGN_GEOMETRIC_PRESENTATION_REPRESENTATION('',(#192),#36482);
#141=CONICAL_SURFACE('',#10640,0.1,0.785398163397448);
#158=SHAPE_REPRESENTATION_RELATIONSHIP('SRR','None',#36571,#175);
#175=ADVANCED_BREP_SHAPE_REPRESENTATION('',(#209),#36481);
#192=STYLED_ITEM('',(#36659),#209);
#209=MANIFOLD_SOLID_BREP('Body1',#9783);
#233=B_SPLINE_SURFACE_WITH_KNOTS('',3,3,((#35222,#35223,#35224,#35225,#35226,
#35227,#35228,#35229,#35230,#35231,#35232,#35233,#35234,#35235,#35236,#35237,
#35238,#35239,#35240,#35241,#35242,#35243,#35244,#35245,#35246,#35247,#35248,
#35249,#35250,#35251,#35252,#35253,#35254,#35255,#35256,#35257,#35258,#35259,
#35260,#35261,#35262,#35263,#35264,#35265,#35266,#35267,#35268,#35269,#35270,
#35271,#35272,#35273,#35274,#35275,#35276,#35277,#35278,#35279,#35280,#35281,
#35282,#35283,#35284,#35285,#35286,#35287,#35288,#35289,#35290,#35291,#35292,
#35293,#35294,#35295,#35296,#35297,#35298,#35299,#35300,#35301,#35302,#35303,
#35304,#35305,#35306,#35307,#35308,#35309,#35310,#35311,#35312,#35313,#35314,
#35315,#35316,#35317,#35318,#35319,#35320,#35321,#35322,#35323,#35324,#35325,
#35326,#35327,#35328,#35329,#35330,#35331,#35332,#35333,#35334,#35335,#35336,
#35337,#35338,#35339,#35340,#35341,#35342),(#35343,#35344,#35345,#35346,
#35347,#35348,#35349,#35350,#35351,#35352,#35353,#35354,#35355,#35356,#35357,
#35358,#35359,#35360,#35361,#35362,#35363,#35364,#35365,#35366,#35367,#35368,
#35369,#35370,#35371,#35372,#35373,#35374,#35375,#35376,#35377,#35378,#35379,
#35380,#35381,#35382,#35383,#35384,#35385,#35386,#35387,#35388,#35389,#35390,
#35391,#35392,#35393,#35394,#35395,#35396,#35397,#35398,#35399,#35400,#35401,
#35402,#35403,#35404,#35405,#35406,#35407,#35408,#35409,#35410,#35411,#35412,
#35413,#35414,#35415,#35416,#35417,#35418,#35419,#35420,#35421,#35422,#35423,
#35424,#35425,#35426,#35427,#35428,#35429,#35430,#35431,#35432,#35433,#35434,
#35435,#35436,#35437,#35438,#35439,#35440,#35441,#35442,#35443,#35444,#35445,
#35446,#35447,#35448,#35449,#35450,#35451,#35452,#35453,#35454,#35455,#35456,
#35457,#35458,#35459,#35460,#35461,#35462,#35463),(#35464,#35465,#35466,
#35467,#35468,#35469,#35470,#35471,#35472,#35473,#35474,#35475,#35476,#35477,
#35478,#35479,#35480,#35481,#35482,#35483,#35484,#35485,#35486,#35487,#35488,
#35489,#35490,#35491,#35492,#35493,#35494,#35495,#35496,#35497,#35498,#35499,
#35500,#35501,#35502,#35503,#35504,#35505,#35506,#35507,#35508,#35509,#35510,
#35511,#35512,#35513,#35514,#35515,#35516,#35517,#35518,#35519,#35520,#35521,
#35522,#35523,#35524,#35525,#35526,#35527,#35528,#35529,#35530,#35531,#35532,
#35533,#35534,#35535,#35536,#35537,#35538,#35539,#35540,#35541,#35542,#35543,
#35544,#35545,#35546,#35547,#35548,#35549,#35550,#35551,#35552,#35553,#35554,
#35555,#35556,#35557,#35558,#35559,#35560,#35561,#35562,#35563,#35564,#35565,
#35566,#35567,#35568,#35569,#35570,#35571,#35572,#35573,#35574,#35575,#35576,
#35577,#35578,#35579,#35580,#35581,#35582,#35583,#35584),(#35585,#35586,
#35587,#35588,#35589,#35590,#35591,#35592,#35593,#35594,#35595,#35596,#35597,
#35598,#35599,#35600,#35601,#35602,#35603,#35604,#35605,#35606,#35607,#35608,
#35609,#35610,#35611,#35612,#35613,#35614,#35615,#35616,#35617,#35618,#35619,
#35620,#35621,#35622,#35623,#35624,#35625,#35626,#35627,#35628,#35629,#35630,
#35631,#35632,#35633,#35634,#35635,#35636,#35637,#35638,#35639,#35640,#35641,
#35642,#35643,#35644,#35645,#35646,#35647,#35648,#35649,#35650,#35651,#35652,
#35653,#35654,#35655,#35656,#35657,#35658,#35659,#35660,#35661,#35662,#35663,
#35664,#35665,#35666,#35667,#35668,#35669,#35670,#35671,#35672,#35673,#35674,
#35675,#35676,#35677,#35678,#35679,#35680,#35681,#35682,#35683,#35684,#35685,
#35686,#35687,#35688,#35689,#35690,#35691,#35692,#35693,#35694,#35695,#35696,
#35697,#35698,#35699,#35700,#35701,#35702,#35703,#35704,#35705)),
 .UNSPECIFIED.,.F.,.F.,.F.,(4,4),(4,1,1,1,1,1,1,1,1,1,1,1,1,1,1,1,1,1,1,
1,1,1,1,1,1,1,1,1,1,1,1,1,1,1,1,1,1,1,1,1,1,1,1,1,1,1,1,1,1,1,1,1,1,1,1,
1,1,1,1,1,1,1,1,1,1,1,1,1,1,1,1,1,1,1,1,1,1,1,1,1,1,1,1,1,1,1,1,1,1,1,1,
1,1,1,1,1,1,1,1,1,1,1,1,1,1,1,1,1,1,1,1,1,1,1,1,1,1,1,4),(0.,0.0329955678841871),
(11.6159397475003,12.6087096497013,13.6014795519022,14.5942494541031,15.5870193563041,
16.579789258505,17.5725591607059,18.5653290629068,19.5580989651078,20.5508688673087,
21.5436387695096,22.5364086717106,23.5291785739115,24.5219484761124,25.5147183783134,
26.5074882805143,27.5002581827152,28.4930280849161,29.4857979871171,30.478567889318,
31.4713377915189,32.4641076937199,33.4568775959208,34.4496474981217,35.4424174003227,
36.4351873025236,37.4279572047245,38.4207271069255,39.4134970091264,40.4062669113273,
41.3990368135282,42.3918067157292,43.3845766179301,44.377346520131,45.370116422332,
46.3628863245329,47.3556562267338,48.3484261289348,49.3411960311357,50.3339659333366,
51.3267358355376,52.3195057377385,53.3122756399394,54.3050455421403,55.2978154443413,
56.2905853465422,57.2833552487431,58.2761251509441,59.268895053145,60.2616649553459,
61.2544348575469,62.2472047597478,63.2399746619487,64.2327445641497,65.2255144663506,
66.2182843685515,67.2110542707524,68.2038241729534,69.1965940751543,70.1893639773552,
71.1821338795562,72.1749037817571,73.167673683958,74.160443586159,75.1532134883599,
76.1459833905608,77.1387532927618,78.1315231949627,79.1242930971636,80.1170629993645,
81.1098329015655,82.1026028037664,83.0953727059673,84.0881426081683,85.0809125103692,
86.0736824125701,87.0664523147711,88.059222216972,89.0519921191729,90.0447620213739,
91.0375319235748,92.0303018257757,93.0230717279766,94.0158416301776,95.0086115323785,
96.0013814345794,96.9941513367804,97.9869212389813,98.9796911411822,99.9724610433832,
100.965230945584,101.958000847785,102.950770749986,103.943540652187,104.936310554388,
105.929080456589,106.92185035879,107.914620260991,108.907390163192,109.900160065392,
110.892929967593,111.885699869794,112.878469771995,113.871239674196,114.864009576397,
115.856779478598,116.849549380799,117.842319283,118.835089185201,119.827859087402,
120.820628989603,121.813398891804,122.806168794005,123.798938696205,124.791708598406,
125.784478500607,126.777248402808,127.770018305009,128.76278820721),
 .UNSPECIFIED.);
#234=B_SPLINE_SURFACE_WITH_KNOTS('',3,3,((#35801,#35802,#35803,#35804,#35805,
#35806,#35807,#35808,#35809,#35810,#35811,#35812,#35813,#35814,#35815,#35816,
#35817,#35818,#35819,#35820,#35821,#35822,#35823,#35824,#35825,#35826,#35827,
#35828,#35829,#35830,#35831,#35832,#35833,#35834,#35835,#35836,#35837,#35838,
#35839,#35840,#35841,#35842,#35843,#35844,#35845,#35846,#35847,#35848,#35849,
#35850,#35851,#35852,#35853,#35854,#35855,#35856,#35857,#35858,#35859,#35860,
#35861,#35862,#35863,#35864,#35865,#35866,#35867,#35868,#35869,#35870,#35871,
#35872,#35873,#35874,#35875,#35876,#35877,#35878,#35879,#35880,#35881,#35882,
#35883,#35884,#35885,#35886,#35887,#35888,#35889,#35890,#35891,#35892,#35893,
#35894,#35895,#35896,#35897,#35898,#35899,#35900,#35901,#35902,#35903,#35904,
#35905,#35906,#35907,#35908,#35909,#35910,#35911,#35912,#35913,#35914,#35915,
#35916,#35917,#35918,#35919,#35920,#35921,#35922,#35923),(#35924,#35925,
#35926,#35927,#35928,#35929,#35930,#35931,#35932,#35933,#35934,#35935,#35936,
#35937,#35938,#35939,#35940,#35941,#35942,#35943,#35944,#35945,#35946,#35947,
#35948,#35949,#35950,#35951,#35952,#35953,#35954,#35955,#35956,#35957,#35958,
#35959,#35960,#35961,#35962,#35963,#35964,#35965,#35966,#35967,#35968,#35969,
#35970,#35971,#35972,#35973,#35974,#35975,#35976,#35977,#35978,#35979,#35980,
#35981,#35982,#35983,#35984,#35985,#35986,#35987,#35988,#35989,#35990,#35991,
#35992,#35993,#35994,#35995,#35996,#35997,#35998,#35999,#36000,#36001,#36002,
#36003,#36004,#36005,#36006,#36007,#36008,#36009,#36010,#36011,#36012,#36013,
#36014,#36015,#36016,#36017,#36018,#36019,#36020,#36021,#36022,#36023,#36024,
#36025,#36026,#36027,#36028,#36029,#36030,#36031,#36032,#36033,#36034,#36035,
#36036,#36037,#36038,#36039,#36040,#36041,#36042,#36043,#36044,#36045,#36046),
(#36047,#36048,#36049,#36050,#36051,#36052,#36053,#36054,#36055,#36056,
#36057,#36058,#36059,#36060,#36061,#36062,#36063,#36064,#36065,#36066,#36067,
#36068,#36069,#36070,#36071,#36072,#36073,#36074,#36075,#36076,#36077,#36078,
#36079,#36080,#36081,#36082,#36083,#36084,#36085,#36086,#36087,#36088,#36089,
#36090,#36091,#36092,#36093,#36094,#36095,#36096,#36097,#36098,#36099,#36100,
#36101,#36102,#36103,#36104,#36105,#36106,#36107,#36108,#36109,#36110,#36111,
#36112,#36113,#36114,#36115,#36116,#36117,#36118,#36119,#36120,#36121,#36122,
#36123,#36124,#36125,#36126,#36127,#36128,#36129,#36130,#36131,#36132,#36133,
#36134,#36135,#36136,#36137,#36138,#36139,#36140,#36141,#36142,#36143,#36144,
#36145,#36146,#36147,#36148,#36149,#36150,#36151,#36152,#36153,#36154,#36155,
#36156,#36157,#36158,#36159,#36160,#36161,#36162,#36163,#36164,#36165,#36166,
#36167,#36168,#36169),(#36170,#36171,#36172,#36173,#36174,#36175,#36176,
#36177,#36178,#36179,#36180,#36181,#36182,#36183,#36184,#36185,#36186,#36187,
#36188,#36189,#36190,#36191,#36192,#36193,#36194,#36195,#36196,#36197,#36198,
#36199,#36200,#36201,#36202,#36203,#36204,#36205,#36206,#36207,#36208,#36209,
#36210,#36211,#36212,#36213,#36214,#36215,#36216,#36217,#36218,#36219,#36220,
#36221,#36222,#36223,#36224,#36225,#36226,#36227,#36228,#36229,#36230,#36231,
#36232,#36233,#36234,#36235,#36236,#36237,#36238,#36239,#36240,#36241,#36242,
#36243,#36244,#36245,#36246,#36247,#36248,#36249,#36250,#36251,#36252,#36253,
#36254,#36255,#36256,#36257,#36258,#36259,#36260,#36261,#36262,#36263,#36264,
#36265,#36266,#36267,#36268,#36269,#36270,#36271,#36272,#36273,#36274,#36275,
#36276,#36277,#36278,#36279,#36280,#36281,#36282,#36283,#36284,#36285,#36286,
#36287,#36288,#36289,#36290,#36291,#36292)),.UNSPECIFIED.,.F.,.F.,.F.,(4,
4),(4,1,1,1,1,1,1,1,1,1,1,1,1,1,1,1,1,1,1,1,1,1,1,1,1,1,1,1,1,1,1,1,1,1,
1,1,1,1,1,1,1,1,1,1,1,1,1,1,1,1,1,1,1,1,1,1,1,1,1,1,1,1,1,1,1,1,1,1,1,1,
1,1,1,1,1,1,1,1,1,1,1,1,1,1,1,1,1,1,1,1,1,1,1,1,1,1,1,1,1,1,1,1,1,1,1,1,
1,1,1,1,1,1,1,1,1,1,1,1,1,1,4),(0.,0.0329955678841871),(8.30203615430831,
9.29553633041689,10.2890365065255,11.282536682634,12.2760368587426,13.2695370348512,
14.2630372109598,15.2565373870684,16.2500375631769,17.2435377392855,18.2370379153941,
19.2305380915027,20.2240382676113,21.2175384437198,22.2110386198284,23.204538795937,
24.1980389720456,25.1915391481542,26.1850393242627,27.1785395003713,28.1720396764799,
29.1655398525885,30.1590400286971,31.1525402048056,32.1460403809142,33.1395405570228,
34.1330407331314,35.1265409092399,36.1200410853485,37.1135412614571,38.1070414375657,
39.1005416136743,40.0940417897828,41.0875419658914,42.081042142,43.0745423181086,
44.0680424942172,45.0615426703257,46.0550428464343,47.0485430225429,48.0420431986515,
49.0355433747601,50.0290435508686,51.0225437269772,52.0160439030858,53.0095440791944,
54.003044255303,54.9965444314115,55.9900446075201,56.9835447836287,57.9770449597373,
58.9705451358458,59.9640453119544,60.957545488063,61.9510456641716,62.9445458402802,
63.9380460163887,64.9315461924973,65.9250463686059,66.9185465447145,67.9120467208231,
68.9055468969316,69.8990470730402,70.8925472491488,71.8860474252574,72.879547601366,
73.8730477774745,74.8665479535831,75.8600481296917,76.8535483058003,77.8470484819088,
78.8405486580174,79.834048834126,80.8275490102346,81.8210491863432,82.8145493624517,
83.8080495385603,84.8015497146689,85.7950498907775,86.7885500668861,87.7820502429946,
88.7755504191032,89.7690505952118,90.7625507713204,91.756050947429,92.7495511235375,
93.7430512996461,94.7365514757547,95.7300516518633,96.7235518279718,97.7170520040804,
98.710552180189,99.7040523562976,100.697552532406,101.691052708515,102.684552884623,
103.678053060732,104.67155323684,105.665053412949,106.658553589058,107.652053765166,
108.645553941275,109.639054117383,110.632554293492,111.626054469601,112.619554645709,
113.613054821818,114.606554997926,115.600055174035,116.593555350143,117.587055526252,
118.580555702361,119.574055878469,120.567556054578,121.561056230686,122.554556406795,
123.548056582903,124.541556759012,125.535056935121,126.528557111229,127.522057287338),
 .UNSPECIFIED.);
#300=FACE_BOUND('',#1577,.T.);
#301=FACE_BOUND('',#1580,.T.);
#429=PLANE('',#10646);
#430=PLANE('',#10647);
#431=PLANE('',#10648);
#432=PLANE('',#10649);
#433=PLANE('',#10650);
#434=PLANE('',#10651);
#435=PLANE('',#10652);
#436=PLANE('',#10653);
#437=PLANE('',#10657);
#438=PLANE('',#10658);
#925=FACE_OUTER_BOUND('',#1528,.T.);
#926=FACE_OUTER_BOUND('',#1529,.T.);
#927=FACE_OUTER_BOUND('',#1530,.T.);
#928=FACE_OUTER_BOUND('',#1531,.T.);
#929=FACE_OUTER_BOUND('',#1532,.T.);
#930=FACE_OUTER_BOUND('',#1533,.T.);
#931=FACE_OUTER_BOUND('',#1534,.T.);
#932=FACE_OUTER_BOUND('',#1535,.T.);
#933=FACE_OUTER_BOUND('',#1536,.T.);
#934=FACE_OUTER_BOUND('',#1537,.T.);
#935=FACE_OUTER_BOUND('',#1538,.T.);
#936=FACE_OUTER_BOUND('',#1539,.T.);
#937=FACE_OUTER_BOUND('',#1540,.T.);
#938=FACE_OUTER_BOUND('',#1541,.T.);
#939=FACE_OUTER_BOUND('',#1542,.T.);
#940=FACE_OUTER_BOUND('',#1543,.T.);
#941=FACE_OUTER_BOUND('',#1544,.T.);
#942=FACE_OUTER_BOUND('',#1545,.T.);
#943=FACE_OUTER_BOUND('',#1546,.T.);
#944=FACE_OUTER_BOUND('',#1547,.T.);
#945=FACE_OUTER_BOUND('',#1548,.T.);
#946=FACE_OUTER_BOUND('',#1549,.T.);
#947=FACE_OUTER_BOUND('',#1550,.T.);
#948=FACE_OUTER_BOUND('',#1551,.T.);
#949=FACE_OUTER_BOUND('',#1552,.T.);
#950=FACE_OUTER_BOUND('',#1553,.T.);
#951=FACE_OUTER_BOUND('',#1554,.T.);
#952=FACE_OUTER_BOUND('',#1555,.T.);
#953=FACE_OUTER_BOUND('',#1556,.T.);
#954=FACE_OUTER_BOUND('',#1557,.T.);
#955=FACE_OUTER_BOUND('',#1558,.T.);
#956=FACE_OUTER_BOUND('',#1559,.T.);
#957=FACE_OUTER_BOUND('',#1560,.T.);
#958=FACE_OUTER_BOUND('',#1561,.T.);
#959=FACE_OUTER_BOUND('',#1562,.T.);
#960=FACE_OUTER_BOUND('',#1563,.T.);
#961=FACE_OUTER_BOUND('',#1564,.T.);
#962=FACE_OUTER_BOUND('',#1565,.T.);
#963=FACE_OUTER_BOUND('',#1566,.T.);
#964=FACE_OUTER_BOUND('',#1567,.T.);
#965=FACE_OUTER_BOUND('',#1568,.T.);
#966=FACE_OUTER_BOUND('',#1569,.T.);
#967=FACE_OUTER_BOUND('',#1570,.T.);
#968=FACE_OUTER_BOUND('',#1571,.T.);
#969=FACE_OUTER_BOUND('',#1572,.T.);
#970=FACE_OUTER_BOUND('',#1573,.T.);
#971=FACE_OUTER_BOUND('',#1574,.T.);
#972=FACE_OUTER_BOUND('',#1575,.T.);
#973=FACE_OUTER_BOUND('',#1576,.T.);
#974=FACE_OUTER_BOUND('',#1578,.T.);
#975=FACE_OUTER_BOUND('',#1579,.T.);
#976=FACE_OUTER_BOUND('',#1581,.T.);
#1528=EDGE_LOOP('',(#8572,#8573,#8574,#8575));
#1529=EDGE_LOOP('',(#8576,#8577,#8578,#8579));
#1530=EDGE_LOOP('',(#8580,#8581,#8582,#8583));
#1531=EDGE_LOOP('',(#8584,#8585,#8586,#8587));
#1532=EDGE_LOOP('',(#8588,#8589,#8590,#8591));
#1533=EDGE_LOOP('',(#8592,#8593,#8594,#8595));
#1534=EDGE_LOOP('',(#8596,#8597,#8598,#8599));
#1535=EDGE_LOOP('',(#8600,#8601,#8602,#8603));
#1536=EDGE_LOOP('',(#8604,#8605,#8606,#8607));
#1537=EDGE_LOOP('',(#8608,#8609,#8610,#8611));
#1538=EDGE_LOOP('',(#8612,#8613,#8614,#8615));
#1539=EDGE_LOOP('',(#8616,#8617,#8618,#8619));
#1540=EDGE_LOOP('',(#8620,#8621,#8622,#8623));
#1541=EDGE_LOOP('',(#8624,#8625,#8626,#8627));
#1542=EDGE_LOOP('',(#8628,#8629,#8630,#8631));
#1543=EDGE_LOOP('',(#8632,#8633,#8634,#8635));
#1544=EDGE_LOOP('',(#8636,#8637,#8638,#8639));
#1545=EDGE_LOOP('',(#8640,#8641,#8642,#8643));
#1546=EDGE_LOOP('',(#8644,#8645,#8646,#8647));
#1547=EDGE_LOOP('',(#8648,#8649,#8650,#8651));
#1548=EDGE_LOOP('',(#8652,#8653,#8654,#8655));
#1549=EDGE_LOOP('',(#8656,#8657,#8658,#8659));
#1550=EDGE_LOOP('',(#8660,#8661,#8662,#8663));
#1551=EDGE_LOOP('',(#8664,#8665,#8666,#8667));
#1552=EDGE_LOOP('',(#8668,#8669,#8670,#8671));
#1553=EDGE_LOOP('',(#8672,#8673,#8674,#8675));
#1554=EDGE_LOOP('',(#8676,#8677,#8678,#8679));
#1555=EDGE_LOOP('',(#8680,#8681,#8682,#8683));
#1556=EDGE_LOOP('',(#8684,#8685,#8686,#8687));
#1557=EDGE_LOOP('',(#8688,#8689,#8690,#8691));
#1558=EDGE_LOOP('',(#8692,#8693,#8694,#8695));
#1559=EDGE_LOOP('',(#8696,#8697,#8698,#8699));
#1560=EDGE_LOOP('',(#8700,#8701,#8702,#8703));
#1561=EDGE_LOOP('',(#8704,#8705,#8706,#8707));
#1562=EDGE_LOOP('',(#8708,#8709,#8710,#8711));
#1563=EDGE_LOOP('',(#8712,#8713,#8714,#8715));
#1564=EDGE_LOOP('',(#8716,#8717,#8718,#8719,#8720,#8721,#8722,#8723));
#1565=EDGE_LOOP('',(#8724,#8725,#8726,#8727,#8728,#8729,#8730,#8731,#8732,
#8733,#8734,#8735,#8736,#8737,#8738,#8739,#8740,#8741,#8742,#8743,#8744,
#8745,#8746,#8747,#8748,#8749,#8750,#8751,#8752,#8753,#8754,#8755,#8756,
#8757,#8758,#8759,#8760,#8761,#8762,#8763));
#1566=EDGE_LOOP('',(#8764,#8765,#8766,#8767));
#1567=EDGE_LOOP('',(#8768,#8769,#8770,#8771,#8772,#8773,#8774,#8775,#8776,
#8777,#8778,#8779,#8780,#8781,#8782,#8783,#8784,#8785,#8786,#8787,#8788,
#8789,#8790,#8791,#8792,#8793,#8794,#8795,#8796,#8797,#8798,#8799,#8800,
#8801,#8802,#8803,#8804,#8805,#8806,#8807,#8808));
#1568=EDGE_LOOP('',(#8809,#8810,#8811,#8812));
#1569=EDGE_LOOP('',(#8813,#8814,#8815,#8816));
#1570=EDGE_LOOP('',(#8817,#8818,#8819,#8820));
#1571=EDGE_LOOP('',(#8821,#8822,#8823,#8824));
#1572=EDGE_LOOP('',(#8825,#8826,#8827,#8828));
#1573=EDGE_LOOP('',(#8829,#8830,#8831,#8832));
#1574=EDGE_LOOP('',(#8833,#8834,#8835,#8836));
#1575=EDGE_LOOP('',(#8837,#8838,#8839,#8840,#8841,#8842));
#1576=EDGE_LOOP('',(#8843));
#1577=EDGE_LOOP('',(#8844,#8845,#8846,#8847));
#1578=EDGE_LOOP('',(#8848,#8849,#8850,#8851));
#1579=EDGE_LOOP('',(#8852));
#1580=EDGE_LOOP('',(#8853,#8854,#8855,#8856,#8857,#8858));
#1581=EDGE_LOOP('',(#8859));
#1731=CIRCLE('',#10603,0.14635);
#1732=CIRCLE('',#10622,0.117775);
#1733=CIRCLE('',#10641,0.14635);
#1734=CIRCLE('',#10642,0.05);
#1735=CIRCLE('',#10644,0.117775);
#1736=CIRCLE('',#10654,0.3);
#1737=CIRCLE('',#10656,0.3);
#2364=B_SPLINE_CURVE_WITH_KNOTS('',3,(#33737,#33738,#33739,#33740,#33741,
#33742,#33743,#33744,#33745,#33746),.UNSPECIFIED.,.F.,.F.,(4,3,3,4),(-4.09202352044855,
-3.97107960880372,-2.97830970660279,-2.07317267331974),.UNSPECIFIED.);
#2365=B_SPLINE_CURVE_WITH_KNOTS('',3,(#33749,#33750,#33751,#33752,#33753,
#33754,#33755),.UNSPECIFIED.,.F.,.F.,(4,3,4),(0.,0.993500176108578,1.12274180646087),
 .UNSPECIFIED.);
#2366=B_SPLINE_CURVE_WITH_KNOTS('',3,(#33760,#33761,#33762,#33763,#33764,
#33765,#33766,#33767,#33768,#33769,#33770,#33771,#33772,#33773,#33774,#33775,
#33776,#33777,#33778,#33779,#33780,#33781),.UNSPECIFIED.,.F.,.F.,(4,3,3,
3,3,3,3,4),(-10.3752088276281,-9.92769902200931,-8.93492911980838,-7.94215921760745,
-6.94938931540652,-5.95661941320559,-4.96384951100465,-4.09202352044855),
 .UNSPECIFIED.);
#2367=B_SPLINE_CURVE_WITH_KNOTS('',3,(#33782,#33783,#33784,#33785,#33786,
#33787,#33788,#33789,#33790,#33791,#33792,#33793,#33794,#33795,#33796,#33797,
#33798,#33799,#33800,#33801,#33802,#33803),.UNSPECIFIED.,.F.,.F.,(4,3,3,
3,3,3,3,4),(1.12274180646087,1.98700035221716,2.98050052832574,3.97400070443431,
4.96750088054289,5.96100105665147,6.95450123276005,7.40592711364046),
 .UNSPECIFIED.);
#2368=B_SPLINE_CURVE_WITH_KNOTS('',3,(#33808,#33809,#33810,#33811,#33812,
#33813,#33814,#33815,#33816,#33817,#33818,#33819,#33820,#33821,#33822,#33823,
#33824,#33825,#33826,#33827,#33828,#33829),.UNSPECIFIED.,.F.,.F.,(4,3,3,
3,3,3,3,4),(-16.6583941348077,-15.8843184352149,-14.891548533014,-13.898778630813,
-12.9060087286121,-11.9132388264112,-10.9204689242102,-10.3752088276281),
 .UNSPECIFIED.);
#2369=B_SPLINE_CURVE_WITH_KNOTS('',3,(#33830,#33831,#33832,#33833,#33834,
#33835,#33836,#33837,#33838,#33839,#33840,#33841,#33842,#33843,#33844,#33845,
#33846,#33847,#33848,#33849,#33850,#33851),.UNSPECIFIED.,.F.,.F.,(4,3,3,
3,3,3,3,4),(7.40592711364046,7.94800140886863,8.94150158497721,9.93500176108579,
10.9285019371944,11.922002113303,12.9155022894115,13.68911242082),
 .UNSPECIFIED.);
#2370=B_SPLINE_CURVE_WITH_KNOTS('',3,(#33856,#33857,#33858,#33859,#33860,
#33861,#33862,#33863,#33864,#33865,#33866,#33867,#33868,#33869,#33870,#33871,
#33872,#33873,#33874,#33875,#33876,#33877,#33878,#33879,#33880),
 .UNSPECIFIED.,.F.,.F.,(4,3,3,3,3,3,3,3,4),(-22.9415794419873,-22.8337077506214,
-21.8409378484205,-20.8481679462195,-19.8553980440186,-18.8626281418177,
-17.8698582396168,-16.8770883374158,-16.6583941348077),.UNSPECIFIED.);
#2371=B_SPLINE_CURVE_WITH_KNOTS('',3,(#33881,#33882,#33883,#33884,#33885,
#33886,#33887,#33888,#33889,#33890,#33891,#33892,#33893,#33894,#33895,#33896,
#33897,#33898,#33899,#33900,#33901,#33902,#33903,#33904,#33905),
 .UNSPECIFIED.,.F.,.F.,(4,3,3,3,3,3,3,3,4),(13.68911242082,13.9090024655201,
14.9025026416287,15.8960028177373,16.8895029938458,17.8830031699544,18.876503346063,
19.8700035221716,19.9722977279996),.UNSPECIFIED.);
#2372=B_SPLINE_CURVE_WITH_KNOTS('',3,(#33910,#33911,#33912,#33913,#33914,
#33915,#33916,#33917,#33918,#33919,#33920,#33921,#33922,#33923,#33924,#33925,
#33926,#33927,#33928,#33929,#33930,#33931),.UNSPECIFIED.,.F.,.F.,(4,3,3,
3,3,3,3,4),(-29.2247647491669,-28.790327163827,-27.7975572616261,-26.8047873594251,
-25.8120174572242,-24.8192475550233,-23.8264776528223,-22.9415794419873),
 .UNSPECIFIED.);
#2373=B_SPLINE_CURVE_WITH_KNOTS('',3,(#33932,#33933,#33934,#33935,#33936,
#33937,#33938,#33939,#33940,#33941,#33942,#33943,#33944,#33945,#33946,#33947,
#33948,#33949,#33950,#33951,#33952,#33953),.UNSPECIFIED.,.F.,.F.,(4,3,3,
3,3,3,3,4),(19.9722977279996,20.8635036982802,21.8570038743887,22.8505040504973,
23.8440042266059,24.8375044027145,25.8310045788231,26.2554830351792),
 .UNSPECIFIED.);
#2374=B_SPLINE_CURVE_WITH_KNOTS('',3,(#33958,#33959,#33960,#33961,#33962,
#33963,#33964,#33965,#33966,#33967,#33968,#33969,#33970,#33971,#33972,#33973,
#33974,#33975,#33976,#33977,#33978,#33979),.UNSPECIFIED.,.F.,.F.,(4,3,3,
3,3,3,3,4),(-35.5079500563465,-34.7469465770326,-33.7541766748316,-32.7614067726307,
-31.7686368704298,-30.7758669682288,-29.7830970660279,-29.2247647491669),
 .UNSPECIFIED.);
#2375=B_SPLINE_CURVE_WITH_KNOTS('',3,(#33980,#33981,#33982,#33983,#33984,
#33985,#33986,#33987,#33988,#33989,#33990,#33991,#33992,#33993,#33994,#33995,
#33996,#33997,#33998,#33999,#34000,#34001),.UNSPECIFIED.,.F.,.F.,(4,3,3,
3,3,3,3,4),(26.2554830351792,26.8245047549316,27.8180049310402,28.8115051071488,
29.8050052832574,30.798505459366,31.7920056354745,32.5386683423588),
 .UNSPECIFIED.);
#2376=B_SPLINE_CURVE_WITH_KNOTS('',3,(#34006,#34007,#34008,#34009,#34010,
#34011,#34012,#34013,#34014,#34015,#34016,#34017,#34018,#34019,#34020,#34021,
#34022,#34023,#34024,#34025,#34026,#34027,#34028,#34029,#34030),
 .UNSPECIFIED.,.F.,.F.,(4,3,3,3,3,3,3,3,4),(-41.7911353635261,-41.6963358924391,
-40.7035659902382,-39.7107960880372,-38.7180261858363,-37.7252562836354,
-36.7324863814344,-35.7397164792335,-35.5079500563465),.UNSPECIFIED.);
#2377=B_SPLINE_CURVE_WITH_KNOTS('',3,(#34031,#34032,#34033,#34034,#34035,
#34036,#34037,#34038,#34039,#34040,#34041,#34042,#34043,#34044,#34045,#34046,
#34047,#34048,#34049,#34050,#34051,#34052,#34053,#34054,#34055),
 .UNSPECIFIED.,.F.,.F.,(4,3,3,3,3,3,3,3,4),(32.5386683423588,32.7855058115831,
33.7790059876917,34.7725061638003,35.7660063399088,36.7595065160174,37.753006692126,
38.7465068682346,38.8218536495384),.UNSPECIFIED.);
#2378=B_SPLINE_CURVE_WITH_KNOTS('',3,(#34060,#34061,#34062,#34063,#34064,
#34065,#34066,#34067,#34068,#34069,#34070,#34071,#34072,#34073,#34074,#34075,
#34076,#34077,#34078,#34079,#34080,#34081),.UNSPECIFIED.,.F.,.F.,(4,3,3,
3,3,3,3,4),(-48.0743206707057,-47.6529553056447,-46.6601854034437,-45.6674155012428,
-44.6746455990419,-43.6818756968409,-42.68910579464,-41.7911353635261),
 .UNSPECIFIED.);
#2379=B_SPLINE_CURVE_WITH_KNOTS('',3,(#34082,#34083,#34084,#34085,#34086,
#34087,#34088,#34089,#34090,#34091,#34092,#34093,#34094,#34095,#34096,#34097,
#34098,#34099,#34100,#34101,#34102,#34103),.UNSPECIFIED.,.F.,.F.,(4,3,3,
3,3,3,3,4),(38.8218536495384,39.7400070443432,40.7335072204517,41.7270073965603,
42.7205075726689,43.7140077487775,44.7075079248861,45.105038956718),
 .UNSPECIFIED.);
#2380=B_SPLINE_CURVE_WITH_KNOTS('',3,(#34108,#34109,#34110,#34111,#34112,
#34113,#34114,#34115,#34116,#34117,#34118,#34119,#34120,#34121,#34122,#34123,
#34124,#34125,#34126,#34127,#34128,#34129),.UNSPECIFIED.,.F.,.F.,(4,3,3,
3,3,3,3,4),(-54.3575059778853,-53.6095747188503,-52.6168048166493,-51.6240349144484,
-50.6312650122475,-49.6384951100465,-48.6457252078456,-48.0743206707057),
 .UNSPECIFIED.);
#2381=B_SPLINE_CURVE_WITH_KNOTS('',3,(#34130,#34131,#34132,#34133,#34134,
#34135,#34136,#34137,#34138,#34139,#34140,#34141,#34142,#34143,#34144,#34145,
#34146,#34147,#34148,#34149,#34150,#34151),.UNSPECIFIED.,.F.,.F.,(4,3,3,
3,3,3,3,4),(45.105038956718,45.7010081009946,46.6945082771032,47.6880084532118,
48.6815086293204,49.675008805429,50.6685089815375,51.3882242638976),
 .UNSPECIFIED.);
#2382=B_SPLINE_CURVE_WITH_KNOTS('',3,(#34156,#34157,#34158,#34159,#34160,
#34161,#34162,#34163,#34164,#34165,#34166,#34167,#34168,#34169,#34170,#34171,
#34172,#34173,#34174,#34175,#34176,#34177,#34178,#34179,#34180),
 .UNSPECIFIED.,.F.,.F.,(4,3,3,3,3,3,3,3,4),(-60.6406912850649,-60.5589640342568,
-59.5661941320559,-58.5734242298549,-57.580654327654,-56.5878844254531,
-55.5951145232521,-54.6023446210512,-54.3575059778853),.UNSPECIFIED.);
#2383=B_SPLINE_CURVE_WITH_KNOTS('',3,(#34181,#34182,#34183,#34184,#34185,
#34186,#34187,#34188,#34189,#34190,#34191,#34192,#34193,#34194,#34195,#34196,
#34197,#34198,#34199,#34200,#34201,#34202,#34203,#34204,#34205),
 .UNSPECIFIED.,.F.,.F.,(4,3,3,3,3,3,3,3,4),(51.3882242638976,51.6620091576461,
52.6555093337547,53.6490095098633,54.6425096859719,55.6360098620804,56.629510038189,
57.6230102142976,57.6714095710772),.UNSPECIFIED.);
#2384=B_SPLINE_CURVE_WITH_KNOTS('',3,(#34210,#34211,#34212,#34213,#34214,
#34215,#34216,#34217,#34218,#34219,#34220,#34221,#34222,#34223,#34224,#34225,
#34226,#34227,#34228,#34229,#34230,#34231),.UNSPECIFIED.,.F.,.F.,(4,3,3,
3,3,3,3,4),(-66.9238765922445,-66.5155834474624,-65.5228135452614,-64.5300436430605,
-63.5372737408596,-62.5445038386586,-61.5517339364577,-60.6406912850649),
 .UNSPECIFIED.);
#2385=B_SPLINE_CURVE_WITH_KNOTS('',3,(#34232,#34233,#34234,#34235,#34236,
#34237,#34238,#34239,#34240,#34241,#34242,#34243,#34244,#34245,#34246,#34247,
#34248,#34249,#34250,#34251,#34252,#34253),.UNSPECIFIED.,.F.,.F.,(4,3,3,
3,3,3,3,4),(57.6714095710772,58.6165103904062,59.6100105665148,60.6035107426233,
61.5970109187319,62.5905110948405,63.5840112709491,63.9545948782568),
 .UNSPECIFIED.);
#2386=B_SPLINE_CURVE_WITH_KNOTS('',3,(#34258,#34259,#34260,#34261,#34262,
#34263,#34264,#34265,#34266,#34267,#34268,#34269,#34270,#34271,#34272,#34273,
#34274,#34275,#34276,#34277,#34278,#34279),.UNSPECIFIED.,.F.,.F.,(4,3,3,
3,3,3,3,4),(-73.207061899424,-72.4722028606679,-71.479432958467,-70.4866630562661,
-69.4938931540652,-68.5011232518642,-67.5083533496633,-66.9238765922445),
 .UNSPECIFIED.);
#2387=B_SPLINE_CURVE_WITH_KNOTS('',3,(#34280,#34281,#34282,#34283,#34284,
#34285,#34286,#34287,#34288,#34289,#34290,#34291,#34292,#34293,#34294,#34295,
#34296,#34297,#34298,#34299,#34300,#34301),.UNSPECIFIED.,.F.,.F.,(4,3,3,
3,3,3,3,4),(63.9545948782568,64.5775114470576,65.5710116231662,66.5645117992748,
67.5580119753834,68.551512151492,69.5450123276005,70.2377801854364),
 .UNSPECIFIED.);
#2388=B_SPLINE_CURVE_WITH_KNOTS('',3,(#34306,#34307,#34308,#34309,#34310,
#34311,#34312,#34313,#34314,#34315,#34316,#34317,#34318,#34319,#34320,#34321,
#34322,#34323,#34324,#34325,#34326,#34327,#34328,#34329,#34330),
 .UNSPECIFIED.,.F.,.F.,(4,3,3,3,3,3,3,3,4),(-79.4902472066036,-79.4215921760745,
-78.4288222738735,-77.4360523716726,-76.4432824694717,-75.4505125672707,
-74.4577426650698,-73.4649727628689,-73.207061899424),.UNSPECIFIED.);
#2389=B_SPLINE_CURVE_WITH_KNOTS('',3,(#34331,#34332,#34333,#34334,#34335,
#34336,#34337,#34338,#34339,#34340,#34341,#34342,#34343,#34344,#34345,#34346,
#34347,#34348,#34349,#34350,#34351,#34352,#34353,#34354,#34355),
 .UNSPECIFIED.,.F.,.F.,(4,3,3,3,3,3,3,3,4),(70.2377801854364,70.5385125037091,
71.5320126798177,72.5255128559263,73.5190130320348,74.5125132081434,75.506013384252,
76.4995135603606,76.520965492616),.UNSPECIFIED.);
#2390=B_SPLINE_CURVE_WITH_KNOTS('',3,(#34360,#34361,#34362,#34363,#34364,
#34365,#34366,#34367,#34368,#34369,#34370,#34371,#34372,#34373,#34374,#34375,
#34376,#34377,#34378,#34379,#34380,#34381),.UNSPECIFIED.,.F.,.F.,(4,3,3,
3,3,3,3,4),(-85.7734325137832,-85.3782115892801,-84.3854416870791,-83.3926717848782,
-82.3999018826773,-81.4071319804763,-80.4143620782754,-79.4902472066036),
 .UNSPECIFIED.);
#2391=B_SPLINE_CURVE_WITH_KNOTS('',3,(#34382,#34383,#34384,#34385,#34386,
#34387,#34388,#34389,#34390,#34391,#34392,#34393,#34394,#34395,#34396,#34397,
#34398,#34399,#34400,#34401,#34402,#34403),.UNSPECIFIED.,.F.,.F.,(4,3,3,
3,3,3,3,4),(76.520965492616,77.4930137364692,78.4865139125777,79.4800140886863,
80.4735142647949,81.4670144409035,82.4605146170121,82.8041507997956),
 .UNSPECIFIED.);
#2392=B_SPLINE_CURVE_WITH_KNOTS('',3,(#34408,#34409,#34410,#34411,#34412,
#34413,#34414,#34415,#34416,#34417,#34418,#34419,#34420,#34421,#34422,#34423,
#34424,#34425,#34426,#34427,#34428,#34429),.UNSPECIFIED.,.F.,.F.,(4,3,3,
3,3,3,3,4),(-92.0566178209628,-91.3348310024856,-90.3420611002847,-89.3492911980838,
-88.3565212958828,-87.3637513936819,-86.370981491481,-85.7734325137832),
 .UNSPECIFIED.);
#2393=B_SPLINE_CURVE_WITH_KNOTS('',3,(#34430,#34431,#34432,#34433,#34434,
#34435,#34436,#34437,#34438,#34439,#34440,#34441,#34442,#34443,#34444,#34445,
#34446,#34447,#34448,#34449,#34450,#34451),.UNSPECIFIED.,.F.,.F.,(4,3,3,
3,3,3,3,4),(82.8041507997956,83.4540147931206,84.4475149692292,85.4410151453378,
86.4345153214464,87.428015497555,88.4215156736635,89.0873361069751),
 .UNSPECIFIED.);
#2394=B_SPLINE_CURVE_WITH_KNOTS('',3,(#34456,#34457,#34458,#34459,#34460,
#34461,#34462,#34463,#34464,#34465,#34466,#34467,#34468,#34469,#34470,#34471,
#34472,#34473,#34474,#34475,#34476,#34477,#34478,#34479,#34480),
 .UNSPECIFIED.,.F.,.F.,(4,3,3,3,3,3,3,3,4),(-98.3398031281424,-98.2842203178921,
-97.2914504156912,-96.2986805134903,-95.3059106112893,-94.3131407090884,
-93.3203708068875,-92.3276009046866,-92.0566178209628),.UNSPECIFIED.);
#2395=B_SPLINE_CURVE_WITH_KNOTS('',3,(#34481,#34482,#34483,#34484,#34485,
#34486,#34487,#34488,#34489,#34490,#34491,#34492,#34493,#34494,#34495,#34496,
#34497,#34498,#34499,#34500,#34501,#34502),.UNSPECIFIED.,.F.,.F.,(4,3,3,
3,3,3,3,4),(89.0873361069751,89.4150158497721,90.4085160258807,91.4020162019893,
92.3955163780979,93.3890165542064,94.382516730315,95.3705214141547),
 .UNSPECIFIED.);
#2396=B_SPLINE_CURVE_WITH_KNOTS('',3,(#34507,#34508,#34509,#34510,#34511,
#34512,#34513,#34514,#34515,#34516,#34517,#34518,#34519,#34520,#34521,#34522,
#34523,#34524,#34525,#34526,#34527,#34528),.UNSPECIFIED.,.F.,.F.,(4,3,3,
3,3,3,3,4),(-104.622988435322,-104.240839731098,-103.248069828897,-102.255299926696,
-101.262530024495,-100.269760122294,-99.2769902200931,-98.3398031281424),
 .UNSPECIFIED.);
#2397=B_SPLINE_CURVE_WITH_KNOTS('',3,(#34529,#34530,#34531,#34532,#34533,
#34534,#34535,#34536,#34537,#34538,#34539,#34540,#34541,#34542,#34543,#34544,
#34545,#34546,#34547,#34548,#34549,#34550),.UNSPECIFIED.,.F.,.F.,(4,3,3,
3,3,3,3,4),(95.3705214141547,96.3695170825322,97.3630172586407,98.3565174347493,
99.3500176108579,100.343517786966,101.337017963075,101.653706721334),
 .UNSPECIFIED.);
#2398=B_SPLINE_CURVE_WITH_KNOTS('',3,(#34555,#34556,#34557,#34558,#34559,
#34560,#34561,#34562,#34563,#34564,#34565,#34566,#34567,#34568,#34569,#34570,
#34571,#34572,#34573,#34574,#34575,#34576),.UNSPECIFIED.,.F.,.F.,(4,3,3,
3,3,3,3,4),(-110.906173742502,-110.197459144303,-109.204689242102,-108.211919339901,
-107.219149437701,-106.2263795355,-105.233609633299,-104.622988435322),
 .UNSPECIFIED.);
#2399=B_SPLINE_CURVE_WITH_KNOTS('',3,(#34577,#34578,#34579,#34580,#34581,
#34582,#34583,#34584,#34585,#34586,#34587,#34588,#34589,#34590,#34591,#34592,
#34593,#34594,#34595,#34596,#34597,#34598),.UNSPECIFIED.,.F.,.F.,(4,3,3,
3,3,3,3,4),(101.653706721334,102.330518139184,103.324018315292,104.317518491401,
105.311018667509,106.304518843618,107.298019019727,107.936892028514),
 .UNSPECIFIED.);
#2400=B_SPLINE_CURVE_WITH_KNOTS('',3,(#34604,#34605,#34606,#34607,#34608,
#34609,#34610,#34611,#34612,#34613),.UNSPECIFIED.,.F.,.F.,(4,1,1,1,1,1,
1,4),(122.522113490002,122.806168794005,123.798938696205,124.791708598406,
125.784478500607,126.777248402808,127.770018305009,128.76278820721),
 .UNSPECIFIED.);
#2401=B_SPLINE_CURVE_WITH_KNOTS('',3,(#34616,#34617,#34618,#34619,#34620,
#34621,#34622,#34623,#34624),.UNSPECIFIED.,.F.,.F.,(4,1,1,1,1,1,4),(122.522113490002,
122.554556406795,123.548056582903,124.541556759012,125.535056935121,126.528557111229,
127.522057287338),.UNSPECIFIED.);
#2402=B_SPLINE_CURVE_WITH_KNOTS('',3,(#34629,#34630,#34631,#34632,#34633,
#34634,#34635,#34636,#34637,#34638),.UNSPECIFIED.,.F.,.F.,(4,1,1,1,1,1,
1,4),(116.238928182822,116.849549380799,117.842319283,118.835089185201,
119.827859087402,120.820628989603,121.813398891804,122.522113490002),
 .UNSPECIFIED.);
#2403=B_SPLINE_CURVE_WITH_KNOTS('',3,(#34639,#34640,#34641,#34642,#34643,
#34644,#34645,#34646,#34647,#34648),.UNSPECIFIED.,.F.,.F.,(4,1,1,1,1,1,
1,4),(116.238928182822,116.593555350143,117.587055526252,118.580555702361,
119.574055878469,120.567556054578,121.561056230686,122.522113490002),
 .UNSPECIFIED.);
#2404=B_SPLINE_CURVE_WITH_KNOTS('',3,(#34653,#34654,#34655,#34656,#34657,
#34658,#34659,#34660,#34661,#34662),.UNSPECIFIED.,.F.,.F.,(4,1,1,1,1,1,
1,4),(109.955742875643,110.892929967593,111.885699869794,112.878469771995,
113.871239674196,114.864009576397,115.856779478598,116.238928182822),
 .UNSPECIFIED.);
#2405=B_SPLINE_CURVE_WITH_KNOTS('',3,(#34663,#34664,#34665,#34666,#34667,
#34668,#34669,#34670,#34671,#34672),.UNSPECIFIED.,.F.,.F.,(4,1,1,1,1,1,
1,4),(109.955742875643,110.632554293492,111.626054469601,112.619554645709,
113.613054821818,114.606554997926,115.600055174035,116.238928182822),
 .UNSPECIFIED.);
#2406=B_SPLINE_CURVE_WITH_KNOTS('',3,(#34677,#34678,#34679,#34680,#34681,
#34682,#34683,#34684,#34685,#34686,#34687),.UNSPECIFIED.,.F.,.F.,(4,1,1,
1,1,1,1,1,4),(103.672557568463,103.943540652187,104.936310554388,105.929080456589,
106.92185035879,107.914620260991,108.907390163192,109.900160065392,109.955742875643),
 .UNSPECIFIED.);
#2407=B_SPLINE_CURVE_WITH_KNOTS('',3,(#34688,#34689,#34690,#34691,#34692,
#34693,#34694,#34695,#34696,#34697,#34698),.UNSPECIFIED.,.F.,.F.,(4,1,1,
1,1,1,1,1,4),(103.672557568463,103.678053060732,104.67155323684,105.665053412949,
106.658553589058,107.652053765166,108.645553941275,109.639054117383,109.955742875643),
 .UNSPECIFIED.);
#2408=B_SPLINE_CURVE_WITH_KNOTS('',3,(#34703,#34704,#34705,#34706,#34707,
#34708,#34709,#34710,#34711,#34712),.UNSPECIFIED.,.F.,.F.,(4,1,1,1,1,1,
1,4),(97.3893722612836,97.9869212389813,98.9796911411822,99.9724610433832,
100.965230945584,101.958000847785,102.950770749986,103.672557568463),
 .UNSPECIFIED.);
#2409=B_SPLINE_CURVE_WITH_KNOTS('',3,(#34713,#34714,#34715,#34716,#34717,
#34718,#34719,#34720,#34721,#34722),.UNSPECIFIED.,.F.,.F.,(4,1,1,1,1,1,
1,4),(97.3893722612835,97.7170520040804,98.710552180189,99.7040523562976,
100.697552532406,101.691052708515,102.684552884623,103.672557568463),
 .UNSPECIFIED.);
#2410=B_SPLINE_CURVE_WITH_KNOTS('',3,(#34727,#34728,#34729,#34730,#34731,
#34732,#34733,#34734,#34735,#34736),.UNSPECIFIED.,.F.,.F.,(4,1,1,1,1,1,
1,4),(91.106186954104,92.0303018257757,93.0230717279766,94.0158416301776,
95.0086115323785,96.0013814345794,96.9941513367804,97.3893722612836),
 .UNSPECIFIED.);
#2411=B_SPLINE_CURVE_WITH_KNOTS('',3,(#34737,#34738,#34739,#34740,#34741,
#34742,#34743,#34744,#34745,#34746),.UNSPECIFIED.,.F.,.F.,(4,1,1,1,1,1,
1,4),(91.106186954104,91.756050947429,92.7495511235375,93.7430512996461,
94.7365514757547,95.7300516518633,96.7235518279718,97.3893722612835),
 .UNSPECIFIED.);
#2412=B_SPLINE_CURVE_WITH_KNOTS('',3,(#34751,#34752,#34753,#34754,#34755,
#34756,#34757,#34758,#34759,#34760,#34761),.UNSPECIFIED.,.F.,.F.,(4,1,1,
1,1,1,1,1,4),(84.8230016469244,85.0809125103692,86.0736824125701,87.0664523147711,
88.059222216972,89.0519921191729,90.0447620213739,91.0375319235748,91.106186954104),
 .UNSPECIFIED.);
#2413=B_SPLINE_CURVE_WITH_KNOTS('',3,(#34762,#34763,#34764,#34765,#34766,
#34767,#34768,#34769,#34770,#34771),.UNSPECIFIED.,.F.,.F.,(4,1,1,1,1,1,
1,4),(84.8230016469244,85.7950498907775,86.7885500668861,87.7820502429946,
88.7755504191032,89.7690505952118,90.7625507713204,91.106186954104),
 .UNSPECIFIED.);
#2414=B_SPLINE_CURVE_WITH_KNOTS('',3,(#34776,#34777,#34778,#34779,#34780,
#34781,#34782,#34783,#34784,#34785),.UNSPECIFIED.,.F.,.F.,(4,1,1,1,1,1,
1,4),(78.5398163397448,79.1242930971636,80.1170629993645,81.1098329015655,
82.1026028037664,83.0953727059673,84.0881426081683,84.8230016469244),
 .UNSPECIFIED.);
#2415=B_SPLINE_CURVE_WITH_KNOTS('',3,(#34786,#34787,#34788,#34789,#34790,
#34791,#34792,#34793,#34794,#34795,#34796),.UNSPECIFIED.,.F.,.F.,(4,1,1,
1,1,1,1,1,4),(78.5398163397448,78.8405486580174,79.834048834126,80.8275490102346,
81.8210491863432,82.8145493624517,83.8080495385603,84.8015497146689,84.8230016469244),
 .UNSPECIFIED.);
#2416=B_SPLINE_CURVE_WITH_KNOTS('',3,(#34801,#34802,#34803,#34804,#34805,
#34806,#34807,#34808,#34809,#34810),.UNSPECIFIED.,.F.,.F.,(4,1,1,1,1,1,
1,4),(72.2566310325652,73.167673683958,74.160443586159,75.1532134883599,
76.1459833905608,77.1387532927618,78.1315231949627,78.5398163397448),
 .UNSPECIFIED.);
#2417=B_SPLINE_CURVE_WITH_KNOTS('',3,(#34811,#34812,#34813,#34814,#34815,
#34816,#34817,#34818,#34819,#34820),.UNSPECIFIED.,.F.,.F.,(4,1,1,1,1,1,
1,4),(72.2566310325652,72.879547601366,73.8730477774745,74.8665479535831,
75.8600481296917,76.8535483058003,77.8470484819088,78.5398163397448),
 .UNSPECIFIED.);
#2418=B_SPLINE_CURVE_WITH_KNOTS('',3,(#34825,#34826,#34827,#34828,#34829,
#34830,#34831,#34832,#34833,#34834,#34835),.UNSPECIFIED.,.F.,.F.,(4,1,1,
1,1,1,1,1,4),(65.9734457253856,66.2182843685515,67.2110542707524,68.2038241729534,
69.1965940751543,70.1893639773552,71.1821338795562,72.1749037817571,72.2566310325652),
 .UNSPECIFIED.);
#2419=B_SPLINE_CURVE_WITH_KNOTS('',3,(#34836,#34837,#34838,#34839,#34840,
#34841,#34842,#34843,#34844,#34845),.UNSPECIFIED.,.F.,.F.,(4,1,1,1,1,1,
1,4),(65.9734457253856,66.9185465447145,67.9120467208231,68.9055468969316,
69.8990470730402,70.8925472491488,71.8860474252574,72.2566310325652),
 .UNSPECIFIED.);
#2420=B_SPLINE_CURVE_WITH_KNOTS('',3,(#34850,#34851,#34852,#34853,#34854,
#34855,#34856,#34857,#34858,#34859),.UNSPECIFIED.,.F.,.F.,(4,1,1,1,1,1,
1,4),(59.690260418206,60.2616649553459,61.2544348575469,62.2472047597478,
63.2399746619487,64.2327445641497,65.2255144663506,65.9734457253856),
 .UNSPECIFIED.);
#2421=B_SPLINE_CURVE_WITH_KNOTS('',3,(#34860,#34861,#34862,#34863,#34864,
#34865,#34866,#34867,#34868,#34869,#34870),.UNSPECIFIED.,.F.,.F.,(4,1,1,
1,1,1,1,1,4),(59.690260418206,59.9640453119544,60.957545488063,61.9510456641716,
62.9445458402802,63.9380460163887,64.9315461924973,65.9250463686059,65.9734457253856),
 .UNSPECIFIED.);
#2422=B_SPLINE_CURVE_WITH_KNOTS('',3,(#34875,#34876,#34877,#34878,#34879,
#34880,#34881,#34882,#34883,#34884),.UNSPECIFIED.,.F.,.F.,(4,1,1,1,1,1,
1,4),(53.4070751110264,54.3050455421403,55.2978154443413,56.2905853465422,
57.2833552487431,58.2761251509441,59.268895053145,59.690260418206),
 .UNSPECIFIED.);
#2423=B_SPLINE_CURVE_WITH_KNOTS('',3,(#34885,#34886,#34887,#34888,#34889,
#34890,#34891,#34892,#34893,#34894),.UNSPECIFIED.,.F.,.F.,(4,1,1,1,1,1,
1,4),(53.4070751110264,54.003044255303,54.9965444314115,55.9900446075201,
56.9835447836287,57.9770449597373,58.9705451358458,59.690260418206),
 .UNSPECIFIED.);
#2424=B_SPLINE_CURVE_WITH_KNOTS('',3,(#34899,#34900,#34901,#34902,#34903,
#34904,#34905,#34906,#34907,#34908,#34909),.UNSPECIFIED.,.F.,.F.,(4,1,1,
1,1,1,1,1,4),(47.1238898038468,47.3556562267338,48.3484261289348,49.3411960311357,
50.3339659333366,51.3267358355376,52.3195057377385,53.3122756399394,53.4070751110264),
 .UNSPECIFIED.);
#2425=B_SPLINE_CURVE_WITH_KNOTS('',3,(#34910,#34911,#34912,#34913,#34914,
#34915,#34916,#34917,#34918,#34919),.UNSPECIFIED.,.F.,.F.,(4,1,1,1,1,1,
1,4),(47.1238898038468,48.0420431986515,49.0355433747601,50.0290435508686,
51.0225437269772,52.0160439030858,53.0095440791944,53.4070751110264),
 .UNSPECIFIED.);
#2426=B_SPLINE_CURVE_WITH_KNOTS('',3,(#34924,#34925,#34926,#34927,#34928,
#34929,#34930,#34931,#34932,#34933),.UNSPECIFIED.,.F.,.F.,(4,1,1,1,1,1,
1,4),(40.8407044966672,41.3990368135282,42.3918067157292,43.3845766179301,
44.377346520131,45.370116422332,46.3628863245329,47.1238898038468),
 .UNSPECIFIED.);
#2427=B_SPLINE_CURVE_WITH_KNOTS('',3,(#34934,#34935,#34936,#34937,#34938,
#34939,#34940,#34941,#34942,#34943,#34944),.UNSPECIFIED.,.F.,.F.,(4,1,1,
1,1,1,1,1,4),(40.8407044966672,41.0875419658914,42.081042142,43.0745423181086,
44.0680424942172,45.0615426703257,46.0550428464343,47.0485430225429,47.1238898038468),
 .UNSPECIFIED.);
#2428=B_SPLINE_CURVE_WITH_KNOTS('',3,(#34949,#34950,#34951,#34952,#34953,
#34954,#34955,#34956,#34957,#34958),.UNSPECIFIED.,.F.,.F.,(4,1,1,1,1,1,
1,4),(34.5575191894876,35.4424174003227,36.4351873025236,37.4279572047245,
38.4207271069255,39.4134970091264,40.4062669113273,40.8407044966672),
 .UNSPECIFIED.);
#2429=B_SPLINE_CURVE_WITH_KNOTS('',3,(#34959,#34960,#34961,#34962,#34963,
#34964,#34965,#34966,#34967,#34968),.UNSPECIFIED.,.F.,.F.,(4,1,1,1,1,1,
1,4),(34.5575191894876,35.1265409092399,36.1200410853485,37.1135412614571,
38.1070414375657,39.1005416136743,40.0940417897828,40.8407044966672),
 .UNSPECIFIED.);
#2430=B_SPLINE_CURVE_WITH_KNOTS('',3,(#34973,#34974,#34975,#34976,#34977,
#34978,#34979,#34980,#34981,#34982,#34983),.UNSPECIFIED.,.F.,.F.,(4,1,1,
1,1,1,1,1,4),(28.2743338823081,28.4930280849161,29.4857979871171,30.478567889318,
31.4713377915189,32.4641076937199,33.4568775959208,34.4496474981217,34.5575191894876),
 .UNSPECIFIED.);
#2431=B_SPLINE_CURVE_WITH_KNOTS('',3,(#34984,#34985,#34986,#34987,#34988,
#34989,#34990,#34991,#34992,#34993),.UNSPECIFIED.,.F.,.F.,(4,1,1,1,1,1,
1,4),(28.274333882308,29.1655398525885,30.1590400286971,31.1525402048056,
32.1460403809142,33.1395405570228,34.1330407331314,34.5575191894876),
 .UNSPECIFIED.);
#2432=B_SPLINE_CURVE_WITH_KNOTS('',3,(#34998,#34999,#35000,#35001,#35002,
#35003,#35004,#35005,#35006,#35007),.UNSPECIFIED.,.F.,.F.,(4,1,1,1,1,1,
1,4),(21.9911485751285,22.5364086717106,23.5291785739115,24.5219484761124,
25.5147183783134,26.5074882805143,27.5002581827152,28.2743338823081),
 .UNSPECIFIED.);
#2433=B_SPLINE_CURVE_WITH_KNOTS('',3,(#35008,#35009,#35010,#35011,#35012,
#35013,#35014,#35015,#35016,#35017,#35018),.UNSPECIFIED.,.F.,.F.,(4,1,1,
1,1,1,1,1,4),(21.9911485751284,22.2110386198284,23.204538795937,24.1980389720456,
25.1915391481542,26.1850393242627,27.1785395003713,28.1720396764799,28.274333882308),
 .UNSPECIFIED.);
#2434=B_SPLINE_CURVE_WITH_KNOTS('',3,(#35023,#35024,#35025,#35026,#35027,
#35028,#35029,#35030,#35031,#35032),.UNSPECIFIED.,.F.,.F.,(4,1,1,1,1,1,
1,4),(15.7079632679489,16.579789258505,17.5725591607059,18.5653290629068,
19.5580989651078,20.5508688673087,21.5436387695096,21.9911485751285),
 .UNSPECIFIED.);
#2435=B_SPLINE_CURVE_WITH_KNOTS('',3,(#35033,#35034,#35035,#35036,#35037,
#35038,#35039,#35040,#35041,#35042),.UNSPECIFIED.,.F.,.F.,(4,1,1,1,1,1,
1,4),(15.7079632679489,16.2500375631769,17.2435377392855,18.2370379153941,
19.2305380915027,20.2240382676113,21.2175384437198,21.9911485751284),
 .UNSPECIFIED.);
#2436=B_SPLINE_CURVE_WITH_KNOTS('',3,(#35045,#35046,#35047,#35048,#35049,
#35050,#35051,#35052,#35053,#35054,#35055,#35056,#35057,#35058,#35059,#35060,
#35061,#35062,#35063,#35064,#35065,#35066,#35067,#35068,#35069,#35070,#35071,
#35072,#35073,#35074,#35075,#35076,#35077,#35078,#35079,#35080,#35081,#35082,
#35083,#35084,#35085,#35086,#35087,#35088,#35089,#35090,#35091,#35092,#35093,
#35094,#35095,#35096,#35097,#35098,#35099,#35100,#35101,#35102,#35103,#35104,
#35105,#35106,#35107,#35108,#35109,#35110,#35111,#35112,#35113,#35114,#35115,
#35116,#35117,#35118,#35119,#35120,#35121,#35122,#35123,#35124,#35125,#35126,
#35127,#35128,#35129,#35130,#35131,#35132,#35133,#35134,#35135,#35136,#35137,
#35138,#35139,#35140,#35141,#35142,#35143,#35144,#35145,#35146,#35147,#35148,
#35149,#35150,#35151,#35152,#35153,#35154,#35155,#35156,#35157,#35158,#35159,
#35160,#35161,#35162,#35163,#35164,#35165),.UNSPECIFIED.,.F.,.F.,(4,3,3,
3,3,3,3,3,3,3,3,3,3,3,3,3,3,3,3,3,3,3,3,3,3,3,3,3,3,3,3,3,3,3,3,3,3,3,3,
3,4),(-0.753008129282273,-0.726411087083563,-0.715881786499564,-0.695023186638146,
-0.683336694953651,-0.673827840112005,-0.646303346018245,-0.632512441881234,
-0.6236006747729,-0.596001444533992,-0.585111150938268,-0.576118283133321,
-0.547602758918121,-0.536376015702489,-0.528202226180116,-0.507015336770619,
-0.486225152468931,-0.477897600046977,-0.452583818906367,-0.439178352550759,
-0.427196798483684,-0.40191963698411,-0.385160728199621,-0.376642475484535,
-0.347726720901875,-0.333286923643958,-0.323497787746622,-0.293375916145958,
-0.277554167376485,-0.267492310267894,-0.241337846280271,-0.224844604159538,
-0.216317003933383,-0.18753716728625,-0.170582917097926,-0.162078349438165,
-0.131638003391508,-0.115498895283149,-0.106874758104641,-0.101197657344851,
-0.0965360155478817),.UNSPECIFIED.);
#2437=B_SPLINE_CURVE_WITH_KNOTS('',3,(#35167,#35168,#35169,#35170,#35171,
#35172,#35173,#35174,#35175,#35176,#35177,#35178,#35179,#35180,#35181,#35182,
#35183,#35184,#35185,#35186,#35187,#35188,#35189,#35190,#35191,#35192,#35193,
#35194,#35195,#35196,#35197,#35198,#35199,#35200),.UNSPECIFIED.,.F.,.F.,
(4,3,3,3,3,3,3,3,3,3,3,4),(-0.204609524178367,-0.173916487069214,-0.152160152794692,
-0.142779925772755,-0.129154387771013,-0.104956417030493,-0.0922484622970884,
-0.0691863467228163,-0.0542893062834328,-0.041770965424307,-0.0153008738219011,
0.),.UNSPECIFIED.);
#2438=B_SPLINE_CURVE_WITH_KNOTS('',3,(#35203,#35204,#35205,#35206,#35207,
#35208,#35209,#35210,#35211,#35212,#35213,#35214,#35215,#35216,#35217,#35218),
 .UNSPECIFIED.,.F.,.F.,(4,3,3,3,3,4),(-0.0965360155478817,-0.0724020116609113,
-0.0590192863946756,-0.0503863222172558,-0.0186895043865902,0.),
 .UNSPECIFIED.);
#2439=B_SPLINE_CURVE_WITH_KNOTS('',3,(#35707,#35708,#35709,#35710,#35711,
#35712,#35713,#35714),.UNSPECIFIED.,.F.,.F.,(4,1,1,1,1,4),(11.6159397475003,
12.6087096497013,13.6014795519022,14.5942494541031,15.5870193563041,15.7079632679489),
 .UNSPECIFIED.);
#2440=B_SPLINE_CURVE_WITH_KNOTS('',3,(#35715,#35716,#35717,#35718,#35719,
#35720,#35721,#35722,#35723,#35724,#35725,#35726,#35727,#35728,#35729,#35730,
#35731,#35732,#35733,#35734,#35735,#35736,#35737,#35738,#35739,#35740,#35741,
#35742,#35743,#35744,#35745,#35746,#35747,#35748,#35749,#35750,#35751,#35752,
#35753,#35754,#35755,#35756,#35757,#35758,#35759,#35760,#35761,#35762,#35763,
#35764,#35765,#35766,#35767,#35768,#35769),.UNSPECIFIED.,.F.,.F.,(4,3,3,
3,3,3,3,3,3,3,3,3,3,3,3,3,3,3,4),(-0.275362278356885,-0.262570109468003,
-0.240166040204702,-0.228737803218204,-0.209304350143588,-0.199561001302199,
-0.189130684518224,-0.159734566166372,-0.148075950500899,-0.139790942517999,
-0.124720142759856,-0.107306928893897,-0.096279762610833,-0.086780292972213,
-0.0650852197291597,-0.0467838010330817,-0.0380963509139461,-0.011916188874275,
0.),.UNSPECIFIED.);
#2441=B_SPLINE_CURVE_WITH_KNOTS('',3,(#35770,#35771,#35772,#35773,#35774,
#35775,#35776,#35777,#35778,#35779,#35780,#35781,#35782,#35783,#35784,#35785,
#35786,#35787,#35788),.UNSPECIFIED.,.F.,.F.,(4,3,3,3,3,3,4),(-115.629180729976,
-115.161308655308,-114.168538753107,-113.175768850906,-112.182998948705,
-111.190229046504,-110.906173742502),.UNSPECIFIED.);
#2442=B_SPLINE_CURVE_WITH_KNOTS('',3,(#35791,#35792,#35793,#35794,#35795,
#35796,#35797,#35798,#35799),.UNSPECIFIED.,.F.,.F.,(4,1,1,1,1,1,4),(10.375208827628,
11.282536682634,12.2760368587426,13.2695370348512,14.2630372109598,15.2565373870684,
15.7079632679489),.UNSPECIFIED.);
#2443=B_SPLINE_CURVE_WITH_KNOTS('',3,(#36293,#36294,#36295,#36296,#36297,
#36298,#36299,#36300,#36301,#36302,#36303,#36304,#36305,#36306,#36307,#36308,
#36309,#36310,#36311,#36312,#36313,#36314),.UNSPECIFIED.,.F.,.F.,(4,3,3,
3,3,3,3,4),(107.936892028514,108.291519195835,109.285019371944,110.278519548052,
111.272019724161,112.265519900269,113.259020076378,113.556008056657),
 .UNSPECIFIED.);
#2444=B_SPLINE_CURVE_WITH_KNOTS('',3,(#36315,#36316,#36317,#36318,#36319,
#36320,#36321,#36322,#36323,#36324,#36325,#36326,#36327,#36328,#36329,#36330,
#36331,#36332,#36333,#36334,#36335,#36336,#36337,#36338,#36339,#36340,#36341,
#36342,#36343,#36344,#36345,#36346,#36347,#36348,#36349,#36350,#36351,#36352,
#36353,#36354,#36355,#36356,#36357,#36358,#36359,#36360,#36361,#36362,#36363,
#36364,#36365,#36366),.UNSPECIFIED.,.F.,.F.,(4,3,3,3,3,3,3,3,3,3,3,3,3,
3,3,3,3,4),(-0.276631791712727,-0.266310431017225,-0.251016700765444,-0.236970857216412,
-0.216553357237997,-0.204277578780747,-0.175779167785564,-0.164239042752865,
-0.155154932673123,-0.139868422463251,-0.120223860282124,-0.110723029685393,
-0.100734922391118,-0.0755511917933386,-0.0588149891352748,-0.049317539854096,
-0.0183008691858031,0.),.UNSPECIFIED.);
#2963=LINE('',#33735,#3537);
#2964=LINE('',#33759,#3538);
#2965=LINE('',#33807,#3539);
#2966=LINE('',#33855,#3540);
#2967=LINE('',#33909,#3541);
#2968=LINE('',#33957,#3542);
#2969=LINE('',#34005,#3543);
#2970=LINE('',#34059,#3544);
#2971=LINE('',#34107,#3545);
#2972=LINE('',#34155,#3546);
#2973=LINE('',#34209,#3547);
#2974=LINE('',#34257,#3548);
#2975=LINE('',#34305,#3549);
#2976=LINE('',#34359,#3550);
#2977=LINE('',#34407,#3551);
#2978=LINE('',#34455,#3552);
#2979=LINE('',#34506,#3553);
#2980=LINE('',#34554,#3554);
#2981=LINE('',#34602,#3555);
#2982=LINE('',#34628,#3556);
#2983=LINE('',#34652,#3557);
#2984=LINE('',#34676,#3558);
#2985=LINE('',#34702,#3559);
#2986=LINE('',#34726,#3560);
#2987=LINE('',#34750,#3561);
#2988=LINE('',#34775,#3562);
#2989=LINE('',#34800,#3563);
#2990=LINE('',#34824,#3564);
#2991=LINE('',#34849,#3565);
#2992=LINE('',#34874,#3566);
#2993=LINE('',#34898,#3567);
#2994=LINE('',#34923,#3568);
#2995=LINE('',#34948,#3569);
#2996=LINE('',#34972,#3570);
#2997=LINE('',#34997,#3571);
#2998=LINE('',#35022,#3572);
#2999=LINE('',#35220,#3573);
#3000=LINE('',#36371,#3574);
#3001=LINE('',#36373,#3575);
#3002=LINE('',#36375,#3576);
#3003=LINE('',#36376,#3577);
#3004=LINE('',#36379,#3578);
#3005=LINE('',#36381,#3579);
#3006=LINE('',#36382,#3580);
#3007=LINE('',#36385,#3581);
#3008=LINE('',#36387,#3582);
#3009=LINE('',#36388,#3583);
#3010=LINE('',#36391,#3584);
#3011=LINE('',#36393,#3585);
#3012=LINE('',#36394,#3586);
#3013=LINE('',#36397,#3587);
#3014=LINE('',#36399,#3588);
#3015=LINE('',#36400,#3589);
#3016=LINE('',#36402,#3590);
#3017=LINE('',#36403,#3591);
#3018=LINE('',#36410,#3592);
#3537=VECTOR('',#12470,0.15);
#3538=VECTOR('',#12475,0.15);
#3539=VECTOR('',#12478,0.15);
#3540=VECTOR('',#12481,0.15);
#3541=VECTOR('',#12484,0.15);
#3542=VECTOR('',#12487,0.15);
#3543=VECTOR('',#12490,0.15);
#3544=VECTOR('',#12493,0.15);
#3545=VECTOR('',#12496,0.15);
#3546=VECTOR('',#12499,0.15);
#3547=VECTOR('',#12502,0.15);
#3548=VECTOR('',#12505,0.15);
#3549=VECTOR('',#12508,0.15);
#3550=VECTOR('',#12511,0.15);
#3551=VECTOR('',#12514,0.15);
#3552=VECTOR('',#12517,0.15);
#3553=VECTOR('',#12520,0.15);
#3554=VECTOR('',#12523,0.15);
#3555=VECTOR('',#12526,0.117775);
#3556=VECTOR('',#12531,0.117775);
#3557=VECTOR('',#12534,0.117775);
#3558=VECTOR('',#12537,0.117775);
#3559=VECTOR('',#12540,0.117775);
#3560=VECTOR('',#12543,0.117775);
#3561=VECTOR('',#12546,0.117775);
#3562=VECTOR('',#12549,0.117775);
#3563=VECTOR('',#12552,0.117775);
#3564=VECTOR('',#12555,0.117775);
#3565=VECTOR('',#12558,0.117775);
#3566=VECTOR('',#12561,0.117775);
#3567=VECTOR('',#12564,0.117775);
#3568=VECTOR('',#12567,0.117775);
#3569=VECTOR('',#12570,0.117775);
#3570=VECTOR('',#12573,0.117775);
#3571=VECTOR('',#12576,0.117775);
#3572=VECTOR('',#12579,0.117775);
#3573=VECTOR('',#12584,0.1);
#3574=VECTOR('',#12595,1.);
#3575=VECTOR('',#12596,1.);
#3576=VECTOR('',#12597,1.);
#3577=VECTOR('',#12598,1.);
#3578=VECTOR('',#12601,1.);
#3579=VECTOR('',#12602,1.);
#3580=VECTOR('',#12603,1.);
#3581=VECTOR('',#12606,1.);
#3582=VECTOR('',#12607,1.);
#3583=VECTOR('',#12608,1.);
#3584=VECTOR('',#12611,1.);
#3585=VECTOR('',#12612,1.);
#3586=VECTOR('',#12613,1.);
#3587=VECTOR('',#12616,1.);
#3588=VECTOR('',#12617,1.);
#3589=VECTOR('',#12618,1.);
#3590=VECTOR('',#12621,1.);
#3591=VECTOR('',#12622,1.);
#3592=VECTOR('',#12631,0.3);
#4453=VERTEX_POINT('',#33733);
#4454=VERTEX_POINT('',#33734);
#4455=VERTEX_POINT('',#33736);
#4456=VERTEX_POINT('',#33747);
#4457=VERTEX_POINT('',#33757);
#4458=VERTEX_POINT('',#33758);
#4459=VERTEX_POINT('',#33805);
#4460=VERTEX_POINT('',#33806);
#4461=VERTEX_POINT('',#33853);
#4462=VERTEX_POINT('',#33854);
#4463=VERTEX_POINT('',#33907);
#4464=VERTEX_POINT('',#33908);
#4465=VERTEX_POINT('',#33955);
#4466=VERTEX_POINT('',#33956);
#4467=VERTEX_POINT('',#34003);
#4468=VERTEX_POINT('',#34004);
#4469=VERTEX_POINT('',#34057);
#4470=VERTEX_POINT('',#34058);
#4471=VERTEX_POINT('',#34105);
#4472=VERTEX_POINT('',#34106);
#4473=VERTEX_POINT('',#34153);
#4474=VERTEX_POINT('',#34154);
#4475=VERTEX_POINT('',#34207);
#4476=VERTEX_POINT('',#34208);
#4477=VERTEX_POINT('',#34255);
#4478=VERTEX_POINT('',#34256);
#4479=VERTEX_POINT('',#34303);
#4480=VERTEX_POINT('',#34304);
#4481=VERTEX_POINT('',#34357);
#4482=VERTEX_POINT('',#34358);
#4483=VERTEX_POINT('',#34405);
#4484=VERTEX_POINT('',#34406);
#4485=VERTEX_POINT('',#34453);
#4486=VERTEX_POINT('',#34454);
#4487=VERTEX_POINT('',#34504);
#4488=VERTEX_POINT('',#34505);
#4489=VERTEX_POINT('',#34552);
#4490=VERTEX_POINT('',#34553);
#4491=VERTEX_POINT('',#34600);
#4492=VERTEX_POINT('',#34601);
#4493=VERTEX_POINT('',#34603);
#4494=VERTEX_POINT('',#34614);
#4495=VERTEX_POINT('',#34626);
#4496=VERTEX_POINT('',#34627);
#4497=VERTEX_POINT('',#34650);
#4498=VERTEX_POINT('',#34651);
#4499=VERTEX_POINT('',#34674);
#4500=VERTEX_POINT('',#34675);
#4501=VERTEX_POINT('',#34700);
#4502=VERTEX_POINT('',#34701);
#4503=VERTEX_POINT('',#34724);
#4504=VERTEX_POINT('',#34725);
#4505=VERTEX_POINT('',#34748);
#4506=VERTEX_POINT('',#34749);
#4507=VERTEX_POINT('',#34773);
#4508=VERTEX_POINT('',#34774);
#4509=VERTEX_POINT('',#34798);
#4510=VERTEX_POINT('',#34799);
#4511=VERTEX_POINT('',#34822);
#4512=VERTEX_POINT('',#34823);
#4513=VERTEX_POINT('',#34847);
#4514=VERTEX_POINT('',#34848);
#4515=VERTEX_POINT('',#34872);
#4516=VERTEX_POINT('',#34873);
#4517=VERTEX_POINT('',#34896);
#4518=VERTEX_POINT('',#34897);
#4519=VERTEX_POINT('',#34921);
#4520=VERTEX_POINT('',#34922);
#4521=VERTEX_POINT('',#34946);
#4522=VERTEX_POINT('',#34947);
#4523=VERTEX_POINT('',#34970);
#4524=VERTEX_POINT('',#34971);
#4525=VERTEX_POINT('',#34995);
#4526=VERTEX_POINT('',#34996);
#4527=VERTEX_POINT('',#35020);
#4528=VERTEX_POINT('',#35021);
#4529=VERTEX_POINT('',#35044);
#4530=VERTEX_POINT('',#35166);
#4531=VERTEX_POINT('',#35201);
#4532=VERTEX_POINT('',#35219);
#4533=VERTEX_POINT('',#35706);
#4534=VERTEX_POINT('',#35790);
#4535=VERTEX_POINT('',#36369);
#4536=VERTEX_POINT('',#36370);
#4537=VERTEX_POINT('',#36372);
#4538=VERTEX_POINT('',#36374);
#4539=VERTEX_POINT('',#36378);
#4540=VERTEX_POINT('',#36380);
#4541=VERTEX_POINT('',#36384);
#4542=VERTEX_POINT('',#36386);
#4543=VERTEX_POINT('',#36390);
#4544=VERTEX_POINT('',#36392);
#4545=VERTEX_POINT('',#36396);
#4546=VERTEX_POINT('',#36398);
#4547=VERTEX_POINT('',#36406);
#4548=VERTEX_POINT('',#36409);
#5842=EDGE_CURVE('',#4453,#4454,#2963,.T.);
#5843=EDGE_CURVE('',#4453,#4455,#2364,.T.);
#5844=EDGE_CURVE('',#4455,#4456,#1731,.F.);
#5845=EDGE_CURVE('',#4456,#4454,#2365,.T.);
#5846=EDGE_CURVE('',#4457,#4458,#2964,.T.);
#5847=EDGE_CURVE('',#4457,#4453,#2366,.T.);
#5848=EDGE_CURVE('',#4454,#4458,#2367,.T.);
#5849=EDGE_CURVE('',#4459,#4460,#2965,.T.);
#5850=EDGE_CURVE('',#4459,#4457,#2368,.T.);
#5851=EDGE_CURVE('',#4458,#4460,#2369,.T.);
#5852=EDGE_CURVE('',#4461,#4462,#2966,.T.);
#5853=EDGE_CURVE('',#4461,#4459,#2370,.T.);
#5854=EDGE_CURVE('',#4460,#4462,#2371,.T.);
#5855=EDGE_CURVE('',#4463,#4464,#2967,.T.);
#5856=EDGE_CURVE('',#4463,#4461,#2372,.T.);
#5857=EDGE_CURVE('',#4462,#4464,#2373,.T.);
#5858=EDGE_CURVE('',#4465,#4466,#2968,.T.);
#5859=EDGE_CURVE('',#4465,#4463,#2374,.T.);
#5860=EDGE_CURVE('',#4464,#4466,#2375,.T.);
#5861=EDGE_CURVE('',#4467,#4468,#2969,.T.);
#5862=EDGE_CURVE('',#4467,#4465,#2376,.T.);
#5863=EDGE_CURVE('',#4466,#4468,#2377,.T.);
#5864=EDGE_CURVE('',#4469,#4470,#2970,.T.);
#5865=EDGE_CURVE('',#4469,#4467,#2378,.T.);
#5866=EDGE_CURVE('',#4468,#4470,#2379,.T.);
#5867=EDGE_CURVE('',#4471,#4472,#2971,.T.);
#5868=EDGE_CURVE('',#4471,#4469,#2380,.T.);
#5869=EDGE_CURVE('',#4470,#4472,#2381,.T.);
#5870=EDGE_CURVE('',#4473,#4474,#2972,.T.);
#5871=EDGE_CURVE('',#4473,#4471,#2382,.T.);
#5872=EDGE_CURVE('',#4472,#4474,#2383,.T.);
#5873=EDGE_CURVE('',#4475,#4476,#2973,.T.);
#5874=EDGE_CURVE('',#4475,#4473,#2384,.T.);
#5875=EDGE_CURVE('',#4474,#4476,#2385,.T.);
#5876=EDGE_CURVE('',#4477,#4478,#2974,.T.);
#5877=EDGE_CURVE('',#4477,#4475,#2386,.T.);
#5878=EDGE_CURVE('',#4476,#4478,#2387,.T.);
#5879=EDGE_CURVE('',#4479,#4480,#2975,.T.);
#5880=EDGE_CURVE('',#4479,#4477,#2388,.T.);
#5881=EDGE_CURVE('',#4478,#4480,#2389,.T.);
#5882=EDGE_CURVE('',#4481,#4482,#2976,.T.);
#5883=EDGE_CURVE('',#4481,#4479,#2390,.T.);
#5884=EDGE_CURVE('',#4480,#4482,#2391,.T.);
#5885=EDGE_CURVE('',#4483,#4484,#2977,.T.);
#5886=EDGE_CURVE('',#4483,#4481,#2392,.T.);
#5887=EDGE_CURVE('',#4482,#4484,#2393,.T.);
#5888=EDGE_CURVE('',#4485,#4486,#2978,.T.);
#5889=EDGE_CURVE('',#4485,#4483,#2394,.T.);
#5890=EDGE_CURVE('',#4484,#4486,#2395,.T.);
#5891=EDGE_CURVE('',#4487,#4488,#2979,.T.);
#5892=EDGE_CURVE('',#4487,#4485,#2396,.T.);
#5893=EDGE_CURVE('',#4486,#4488,#2397,.T.);
#5894=EDGE_CURVE('',#4489,#4490,#2980,.T.);
#5895=EDGE_CURVE('',#4489,#4487,#2398,.T.);
#5896=EDGE_CURVE('',#4488,#4490,#2399,.T.);
#5897=EDGE_CURVE('',#4491,#4492,#2981,.T.);
#5898=EDGE_CURVE('',#4491,#4493,#2400,.T.);
#5899=EDGE_CURVE('',#4493,#4494,#1732,.T.);
#5900=EDGE_CURVE('',#4492,#4494,#2401,.T.);
#5901=EDGE_CURVE('',#4495,#4496,#2982,.T.);
#5902=EDGE_CURVE('',#4495,#4491,#2402,.T.);
#5903=EDGE_CURVE('',#4496,#4492,#2403,.T.);
#5904=EDGE_CURVE('',#4497,#4498,#2983,.T.);
#5905=EDGE_CURVE('',#4497,#4495,#2404,.T.);
#5906=EDGE_CURVE('',#4498,#4496,#2405,.T.);
#5907=EDGE_CURVE('',#4499,#4500,#2984,.T.);
#5908=EDGE_CURVE('',#4499,#4497,#2406,.T.);
#5909=EDGE_CURVE('',#4500,#4498,#2407,.T.);
#5910=EDGE_CURVE('',#4501,#4502,#2985,.T.);
#5911=EDGE_CURVE('',#4501,#4499,#2408,.T.);
#5912=EDGE_CURVE('',#4502,#4500,#2409,.T.);
#5913=EDGE_CURVE('',#4503,#4504,#2986,.T.);
#5914=EDGE_CURVE('',#4503,#4501,#2410,.T.);
#5915=EDGE_CURVE('',#4504,#4502,#2411,.T.);
#5916=EDGE_CURVE('',#4505,#4506,#2987,.T.);
#5917=EDGE_CURVE('',#4505,#4503,#2412,.T.);
#5918=EDGE_CURVE('',#4506,#4504,#2413,.T.);
#5919=EDGE_CURVE('',#4507,#4508,#2988,.T.);
#5920=EDGE_CURVE('',#4507,#4505,#2414,.T.);
#5921=EDGE_CURVE('',#4508,#4506,#2415,.T.);
#5922=EDGE_CURVE('',#4509,#4510,#2989,.T.);
#5923=EDGE_CURVE('',#4509,#4507,#2416,.T.);
#5924=EDGE_CURVE('',#4510,#4508,#2417,.T.);
#5925=EDGE_CURVE('',#4511,#4512,#2990,.T.);
#5926=EDGE_CURVE('',#4511,#4509,#2418,.T.);
#5927=EDGE_CURVE('',#4512,#4510,#2419,.T.);
#5928=EDGE_CURVE('',#4513,#4514,#2991,.T.);
#5929=EDGE_CURVE('',#4513,#4511,#2420,.T.);
#5930=EDGE_CURVE('',#4514,#4512,#2421,.T.);
#5931=EDGE_CURVE('',#4515,#4516,#2992,.T.);
#5932=EDGE_CURVE('',#4515,#4513,#2422,.T.);
#5933=EDGE_CURVE('',#4516,#4514,#2423,.T.);
#5934=EDGE_CURVE('',#4517,#4518,#2993,.T.);
#5935=EDGE_CURVE('',#4517,#4515,#2424,.T.);
#5936=EDGE_CURVE('',#4518,#4516,#2425,.T.);
#5937=EDGE_CURVE('',#4519,#4520,#2994,.T.);
#5938=EDGE_CURVE('',#4519,#4517,#2426,.T.);
#5939=EDGE_CURVE('',#4520,#4518,#2427,.T.);
#5940=EDGE_CURVE('',#4521,#4522,#2995,.T.);
#5941=EDGE_CURVE('',#4521,#4519,#2428,.T.);
#5942=EDGE_CURVE('',#4522,#4520,#2429,.T.);
#5943=EDGE_CURVE('',#4523,#4524,#2996,.T.);
#5944=EDGE_CURVE('',#4523,#4521,#2430,.T.);
#5945=EDGE_CURVE('',#4524,#4522,#2431,.T.);
#5946=EDGE_CURVE('',#4525,#4526,#2997,.T.);
#5947=EDGE_CURVE('',#4525,#4523,#2432,.T.);
#5948=EDGE_CURVE('',#4526,#4524,#2433,.T.);
#5949=EDGE_CURVE('',#4527,#4528,#2998,.T.);
#5950=EDGE_CURVE('',#4527,#4525,#2434,.T.);
#5951=EDGE_CURVE('',#4528,#4526,#2435,.T.);
#5952=EDGE_CURVE('',#4494,#4529,#2436,.T.);
#5953=EDGE_CURVE('',#4530,#4493,#2437,.T.);
#5954=EDGE_CURVE('',#4531,#4530,#1733,.T.);
#5955=EDGE_CURVE('',#4529,#4531,#2438,.T.);
#5956=EDGE_CURVE('',#4529,#4532,#2999,.T.);
#5957=EDGE_CURVE('',#4532,#4532,#1734,.T.);
#5958=EDGE_CURVE('',#4533,#4527,#2439,.T.);
#5959=EDGE_CURVE('',#4455,#4533,#2440,.T.);
#5960=EDGE_CURVE('',#4530,#4489,#2441,.T.);
#5961=EDGE_CURVE('',#4534,#4528,#2442,.T.);
#5962=EDGE_CURVE('',#4533,#4534,#1735,.T.);
#5963=EDGE_CURVE('',#4490,#4531,#2443,.T.);
#5964=EDGE_CURVE('',#4534,#4456,#2444,.T.);
#5965=EDGE_CURVE('',#4535,#4536,#3000,.T.);
#5966=EDGE_CURVE('',#4535,#4537,#3001,.T.);
#5967=EDGE_CURVE('',#4537,#4538,#3002,.T.);
#5968=EDGE_CURVE('',#4536,#4538,#3003,.T.);
#5969=EDGE_CURVE('',#4539,#4535,#3004,.T.);
#5970=EDGE_CURVE('',#4539,#4540,#3005,.T.);
#5971=EDGE_CURVE('',#4540,#4537,#3006,.T.);
#5972=EDGE_CURVE('',#4541,#4539,#3007,.T.);
#5973=EDGE_CURVE('',#4541,#4542,#3008,.T.);
#5974=EDGE_CURVE('',#4542,#4540,#3009,.T.);
#5975=EDGE_CURVE('',#4543,#4541,#3010,.T.);
#5976=EDGE_CURVE('',#4543,#4544,#3011,.T.);
#5977=EDGE_CURVE('',#4544,#4542,#3012,.T.);
#5978=EDGE_CURVE('',#4545,#4543,#3013,.T.);
#5979=EDGE_CURVE('',#4545,#4546,#3014,.T.);
#5980=EDGE_CURVE('',#4546,#4544,#3015,.T.);
#5981=EDGE_CURVE('',#4536,#4545,#3016,.T.);
#5982=EDGE_CURVE('',#4538,#4546,#3017,.T.);
#5983=EDGE_CURVE('',#4547,#4547,#1736,.T.);
#5984=EDGE_CURVE('',#4547,#4548,#3018,.T.);
#5985=EDGE_CURVE('',#4548,#4548,#1737,.T.);
#8572=ORIENTED_EDGE('',*,*,#5842,.F.);
#8573=ORIENTED_EDGE('',*,*,#5843,.T.);
#8574=ORIENTED_EDGE('',*,*,#5844,.T.);
#8575=ORIENTED_EDGE('',*,*,#5845,.T.);
#8576=ORIENTED_EDGE('',*,*,#5846,.F.);
#8577=ORIENTED_EDGE('',*,*,#5847,.T.);
#8578=ORIENTED_EDGE('',*,*,#5842,.T.);
#8579=ORIENTED_EDGE('',*,*,#5848,.T.);
#8580=ORIENTED_EDGE('',*,*,#5849,.F.);
#8581=ORIENTED_EDGE('',*,*,#5850,.T.);
#8582=ORIENTED_EDGE('',*,*,#5846,.T.);
#8583=ORIENTED_EDGE('',*,*,#5851,.T.);
#8584=ORIENTED_EDGE('',*,*,#5852,.F.);
#8585=ORIENTED_EDGE('',*,*,#5853,.T.);
#8586=ORIENTED_EDGE('',*,*,#5849,.T.);
#8587=ORIENTED_EDGE('',*,*,#5854,.T.);
#8588=ORIENTED_EDGE('',*,*,#5855,.F.);
#8589=ORIENTED_EDGE('',*,*,#5856,.T.);
#8590=ORIENTED_EDGE('',*,*,#5852,.T.);
#8591=ORIENTED_EDGE('',*,*,#5857,.T.);
#8592=ORIENTED_EDGE('',*,*,#5858,.F.);
#8593=ORIENTED_EDGE('',*,*,#5859,.T.);
#8594=ORIENTED_EDGE('',*,*,#5855,.T.);
#8595=ORIENTED_EDGE('',*,*,#5860,.T.);
#8596=ORIENTED_EDGE('',*,*,#5861,.F.);
#8597=ORIENTED_EDGE('',*,*,#5862,.T.);
#8598=ORIENTED_EDGE('',*,*,#5858,.T.);
#8599=ORIENTED_EDGE('',*,*,#5863,.T.);
#8600=ORIENTED_EDGE('',*,*,#5864,.F.);
#8601=ORIENTED_EDGE('',*,*,#5865,.T.);
#8602=ORIENTED_EDGE('',*,*,#5861,.T.);
#8603=ORIENTED_EDGE('',*,*,#5866,.T.);
#8604=ORIENTED_EDGE('',*,*,#5867,.F.);
#8605=ORIENTED_EDGE('',*,*,#5868,.T.);
#8606=ORIENTED_EDGE('',*,*,#5864,.T.);
#8607=ORIENTED_EDGE('',*,*,#5869,.T.);
#8608=ORIENTED_EDGE('',*,*,#5870,.F.);
#8609=ORIENTED_EDGE('',*,*,#5871,.T.);
#8610=ORIENTED_EDGE('',*,*,#5867,.T.);
#8611=ORIENTED_EDGE('',*,*,#5872,.T.);
#8612=ORIENTED_EDGE('',*,*,#5873,.F.);
#8613=ORIENTED_EDGE('',*,*,#5874,.T.);
#8614=ORIENTED_EDGE('',*,*,#5870,.T.);
#8615=ORIENTED_EDGE('',*,*,#5875,.T.);
#8616=ORIENTED_EDGE('',*,*,#5876,.F.);
#8617=ORIENTED_EDGE('',*,*,#5877,.T.);
#8618=ORIENTED_EDGE('',*,*,#5873,.T.);
#8619=ORIENTED_EDGE('',*,*,#5878,.T.);
#8620=ORIENTED_EDGE('',*,*,#5879,.F.);
#8621=ORIENTED_EDGE('',*,*,#5880,.T.);
#8622=ORIENTED_EDGE('',*,*,#5876,.T.);
#8623=ORIENTED_EDGE('',*,*,#5881,.T.);
#8624=ORIENTED_EDGE('',*,*,#5882,.F.);
#8625=ORIENTED_EDGE('',*,*,#5883,.T.);
#8626=ORIENTED_EDGE('',*,*,#5879,.T.);
#8627=ORIENTED_EDGE('',*,*,#5884,.T.);
#8628=ORIENTED_EDGE('',*,*,#5885,.F.);
#8629=ORIENTED_EDGE('',*,*,#5886,.T.);
#8630=ORIENTED_EDGE('',*,*,#5882,.T.);
#8631=ORIENTED_EDGE('',*,*,#5887,.T.);
#8632=ORIENTED_EDGE('',*,*,#5888,.F.);
#8633=ORIENTED_EDGE('',*,*,#5889,.T.);
#8634=ORIENTED_EDGE('',*,*,#5885,.T.);
#8635=ORIENTED_EDGE('',*,*,#5890,.T.);
#8636=ORIENTED_EDGE('',*,*,#5891,.F.);
#8637=ORIENTED_EDGE('',*,*,#5892,.T.);
#8638=ORIENTED_EDGE('',*,*,#5888,.T.);
#8639=ORIENTED_EDGE('',*,*,#5893,.T.);
#8640=ORIENTED_EDGE('',*,*,#5894,.F.);
#8641=ORIENTED_EDGE('',*,*,#5895,.T.);
#8642=ORIENTED_EDGE('',*,*,#5891,.T.);
#8643=ORIENTED_EDGE('',*,*,#5896,.T.);
#8644=ORIENTED_EDGE('',*,*,#5897,.F.);
#8645=ORIENTED_EDGE('',*,*,#5898,.T.);
#8646=ORIENTED_EDGE('',*,*,#5899,.T.);
#8647=ORIENTED_EDGE('',*,*,#5900,.F.);
#8648=ORIENTED_EDGE('',*,*,#5901,.F.);
#8649=ORIENTED_EDGE('',*,*,#5902,.T.);
#8650=ORIENTED_EDGE('',*,*,#5897,.T.);
#8651=ORIENTED_EDGE('',*,*,#5903,.F.);
#8652=ORIENTED_EDGE('',*,*,#5904,.F.);
#8653=ORIENTED_EDGE('',*,*,#5905,.T.);
#8654=ORIENTED_EDGE('',*,*,#5901,.T.);
#8655=ORIENTED_EDGE('',*,*,#5906,.F.);
#8656=ORIENTED_EDGE('',*,*,#5907,.F.);
#8657=ORIENTED_EDGE('',*,*,#5908,.T.);
#8658=ORIENTED_EDGE('',*,*,#5904,.T.);
#8659=ORIENTED_EDGE('',*,*,#5909,.F.);
#8660=ORIENTED_EDGE('',*,*,#5910,.F.);
#8661=ORIENTED_EDGE('',*,*,#5911,.T.);
#8662=ORIENTED_EDGE('',*,*,#5907,.T.);
#8663=ORIENTED_EDGE('',*,*,#5912,.F.);
#8664=ORIENTED_EDGE('',*,*,#5913,.F.);
#8665=ORIENTED_EDGE('',*,*,#5914,.T.);
#8666=ORIENTED_EDGE('',*,*,#5910,.T.);
#8667=ORIENTED_EDGE('',*,*,#5915,.F.);
#8668=ORIENTED_EDGE('',*,*,#5916,.F.);
#8669=ORIENTED_EDGE('',*,*,#5917,.T.);
#8670=ORIENTED_EDGE('',*,*,#5913,.T.);
#8671=ORIENTED_EDGE('',*,*,#5918,.F.);
#8672=ORIENTED_EDGE('',*,*,#5919,.F.);
#8673=ORIENTED_EDGE('',*,*,#5920,.T.);
#8674=ORIENTED_EDGE('',*,*,#5916,.T.);
#8675=ORIENTED_EDGE('',*,*,#5921,.F.);
#8676=ORIENTED_EDGE('',*,*,#5922,.F.);
#8677=ORIENTED_EDGE('',*,*,#5923,.T.);
#8678=ORIENTED_EDGE('',*,*,#5919,.T.);
#8679=ORIENTED_EDGE('',*,*,#5924,.F.);
#8680=ORIENTED_EDGE('',*,*,#5925,.F.);
#8681=ORIENTED_EDGE('',*,*,#5926,.T.);
#8682=ORIENTED_EDGE('',*,*,#5922,.T.);
#8683=ORIENTED_EDGE('',*,*,#5927,.F.);
#8684=ORIENTED_EDGE('',*,*,#5928,.F.);
#8685=ORIENTED_EDGE('',*,*,#5929,.T.);
#8686=ORIENTED_EDGE('',*,*,#5925,.T.);
#8687=ORIENTED_EDGE('',*,*,#5930,.F.);
#8688=ORIENTED_EDGE('',*,*,#5931,.F.);
#8689=ORIENTED_EDGE('',*,*,#5932,.T.);
#8690=ORIENTED_EDGE('',*,*,#5928,.T.);
#8691=ORIENTED_EDGE('',*,*,#5933,.F.);
#8692=ORIENTED_EDGE('',*,*,#5934,.F.);
#8693=ORIENTED_EDGE('',*,*,#5935,.T.);
#8694=ORIENTED_EDGE('',*,*,#5931,.T.);
#8695=ORIENTED_EDGE('',*,*,#5936,.F.);
#8696=ORIENTED_EDGE('',*,*,#5937,.F.);
#8697=ORIENTED_EDGE('',*,*,#5938,.T.);
#8698=ORIENTED_EDGE('',*,*,#5934,.T.);
#8699=ORIENTED_EDGE('',*,*,#5939,.F.);
#8700=ORIENTED_EDGE('',*,*,#5940,.F.);
#8701=ORIENTED_EDGE('',*,*,#5941,.T.);
#8702=ORIENTED_EDGE('',*,*,#5937,.T.);
#8703=ORIENTED_EDGE('',*,*,#5942,.F.);
#8704=ORIENTED_EDGE('',*,*,#5943,.F.);
#8705=ORIENTED_EDGE('',*,*,#5944,.T.);
#8706=ORIENTED_EDGE('',*,*,#5940,.T.);
#8707=ORIENTED_EDGE('',*,*,#5945,.F.);
#8708=ORIENTED_EDGE('',*,*,#5946,.F.);
#8709=ORIENTED_EDGE('',*,*,#5947,.T.);
#8710=ORIENTED_EDGE('',*,*,#5943,.T.);
#8711=ORIENTED_EDGE('',*,*,#5948,.F.);
#8712=ORIENTED_EDGE('',*,*,#5949,.F.);
#8713=ORIENTED_EDGE('',*,*,#5950,.T.);
#8714=ORIENTED_EDGE('',*,*,#5946,.T.);
#8715=ORIENTED_EDGE('',*,*,#5951,.F.);
#8716=ORIENTED_EDGE('',*,*,#5952,.F.);
#8717=ORIENTED_EDGE('',*,*,#5899,.F.);
#8718=ORIENTED_EDGE('',*,*,#5953,.F.);
#8719=ORIENTED_EDGE('',*,*,#5954,.F.);
#8720=ORIENTED_EDGE('',*,*,#5955,.F.);
#8721=ORIENTED_EDGE('',*,*,#5956,.T.);
#8722=ORIENTED_EDGE('',*,*,#5957,.F.);
#8723=ORIENTED_EDGE('',*,*,#5956,.F.);
#8724=ORIENTED_EDGE('',*,*,#5953,.T.);
#8725=ORIENTED_EDGE('',*,*,#5898,.F.);
#8726=ORIENTED_EDGE('',*,*,#5902,.F.);
#8727=ORIENTED_EDGE('',*,*,#5905,.F.);
#8728=ORIENTED_EDGE('',*,*,#5908,.F.);
#8729=ORIENTED_EDGE('',*,*,#5911,.F.);
#8730=ORIENTED_EDGE('',*,*,#5914,.F.);
#8731=ORIENTED_EDGE('',*,*,#5917,.F.);
#8732=ORIENTED_EDGE('',*,*,#5920,.F.);
#8733=ORIENTED_EDGE('',*,*,#5923,.F.);
#8734=ORIENTED_EDGE('',*,*,#5926,.F.);
#8735=ORIENTED_EDGE('',*,*,#5929,.F.);
#8736=ORIENTED_EDGE('',*,*,#5932,.F.);
#8737=ORIENTED_EDGE('',*,*,#5935,.F.);
#8738=ORIENTED_EDGE('',*,*,#5938,.F.);
#8739=ORIENTED_EDGE('',*,*,#5941,.F.);
#8740=ORIENTED_EDGE('',*,*,#5944,.F.);
#8741=ORIENTED_EDGE('',*,*,#5947,.F.);
#8742=ORIENTED_EDGE('',*,*,#5950,.F.);
#8743=ORIENTED_EDGE('',*,*,#5958,.F.);
#8744=ORIENTED_EDGE('',*,*,#5959,.F.);
#8745=ORIENTED_EDGE('',*,*,#5843,.F.);
#8746=ORIENTED_EDGE('',*,*,#5847,.F.);
#8747=ORIENTED_EDGE('',*,*,#5850,.F.);
#8748=ORIENTED_EDGE('',*,*,#5853,.F.);
#8749=ORIENTED_EDGE('',*,*,#5856,.F.);
#8750=ORIENTED_EDGE('',*,*,#5859,.F.);
#8751=ORIENTED_EDGE('',*,*,#5862,.F.);
#8752=ORIENTED_EDGE('',*,*,#5865,.F.);
#8753=ORIENTED_EDGE('',*,*,#5868,.F.);
#8754=ORIENTED_EDGE('',*,*,#5871,.F.);
#8755=ORIENTED_EDGE('',*,*,#5874,.F.);
#8756=ORIENTED_EDGE('',*,*,#5877,.F.);
#8757=ORIENTED_EDGE('',*,*,#5880,.F.);
#8758=ORIENTED_EDGE('',*,*,#5883,.F.);
#8759=ORIENTED_EDGE('',*,*,#5886,.F.);
#8760=ORIENTED_EDGE('',*,*,#5889,.F.);
#8761=ORIENTED_EDGE('',*,*,#5892,.F.);
#8762=ORIENTED_EDGE('',*,*,#5895,.F.);
#8763=ORIENTED_EDGE('',*,*,#5960,.F.);
#8764=ORIENTED_EDGE('',*,*,#5949,.T.);
#8765=ORIENTED_EDGE('',*,*,#5961,.F.);
#8766=ORIENTED_EDGE('',*,*,#5962,.F.);
#8767=ORIENTED_EDGE('',*,*,#5958,.T.);
#8768=ORIENTED_EDGE('',*,*,#5952,.T.);
#8769=ORIENTED_EDGE('',*,*,#5955,.T.);
#8770=ORIENTED_EDGE('',*,*,#5963,.F.);
#8771=ORIENTED_EDGE('',*,*,#5896,.F.);
#8772=ORIENTED_EDGE('',*,*,#5893,.F.);
#8773=ORIENTED_EDGE('',*,*,#5890,.F.);
#8774=ORIENTED_EDGE('',*,*,#5887,.F.);
#8775=ORIENTED_EDGE('',*,*,#5884,.F.);
#8776=ORIENTED_EDGE('',*,*,#5881,.F.);
#8777=ORIENTED_EDGE('',*,*,#5878,.F.);
#8778=ORIENTED_EDGE('',*,*,#5875,.F.);
#8779=ORIENTED_EDGE('',*,*,#5872,.F.);
#8780=ORIENTED_EDGE('',*,*,#5869,.F.);
#8781=ORIENTED_EDGE('',*,*,#5866,.F.);
#8782=ORIENTED_EDGE('',*,*,#5863,.F.);
#8783=ORIENTED_EDGE('',*,*,#5860,.F.);
#8784=ORIENTED_EDGE('',*,*,#5857,.F.);
#8785=ORIENTED_EDGE('',*,*,#5854,.F.);
#8786=ORIENTED_EDGE('',*,*,#5851,.F.);
#8787=ORIENTED_EDGE('',*,*,#5848,.F.);
#8788=ORIENTED_EDGE('',*,*,#5845,.F.);
#8789=ORIENTED_EDGE('',*,*,#5964,.F.);
#8790=ORIENTED_EDGE('',*,*,#5961,.T.);
#8791=ORIENTED_EDGE('',*,*,#5951,.T.);
#8792=ORIENTED_EDGE('',*,*,#5948,.T.);
#8793=ORIENTED_EDGE('',*,*,#5945,.T.);
#8794=ORIENTED_EDGE('',*,*,#5942,.T.);
#8795=ORIENTED_EDGE('',*,*,#5939,.T.);
#8796=ORIENTED_EDGE('',*,*,#5936,.T.);
#8797=ORIENTED_EDGE('',*,*,#5933,.T.);
#8798=ORIENTED_EDGE('',*,*,#5930,.T.);
#8799=ORIENTED_EDGE('',*,*,#5927,.T.);
#8800=ORIENTED_EDGE('',*,*,#5924,.T.);
#8801=ORIENTED_EDGE('',*,*,#5921,.T.);
#8802=ORIENTED_EDGE('',*,*,#5918,.T.);
#8803=ORIENTED_EDGE('',*,*,#5915,.T.);
#8804=ORIENTED_EDGE('',*,*,#5912,.T.);
#8805=ORIENTED_EDGE('',*,*,#5909,.T.);
#8806=ORIENTED_EDGE('',*,*,#5906,.T.);
#8807=ORIENTED_EDGE('',*,*,#5903,.T.);
#8808=ORIENTED_EDGE('',*,*,#5900,.T.);
#8809=ORIENTED_EDGE('',*,*,#5894,.T.);
#8810=ORIENTED_EDGE('',*,*,#5963,.T.);
#8811=ORIENTED_EDGE('',*,*,#5954,.T.);
#8812=ORIENTED_EDGE('',*,*,#5960,.T.);
#8813=ORIENTED_EDGE('',*,*,#5965,.F.);
#8814=ORIENTED_EDGE('',*,*,#5966,.T.);
#8815=ORIENTED_EDGE('',*,*,#5967,.T.);
#8816=ORIENTED_EDGE('',*,*,#5968,.F.);
#8817=ORIENTED_EDGE('',*,*,#5969,.F.);
#8818=ORIENTED_EDGE('',*,*,#5970,.T.);
#8819=ORIENTED_EDGE('',*,*,#5971,.T.);
#8820=ORIENTED_EDGE('',*,*,#5966,.F.);
#8821=ORIENTED_EDGE('',*,*,#5972,.F.);
#8822=ORIENTED_EDGE('',*,*,#5973,.T.);
#8823=ORIENTED_EDGE('',*,*,#5974,.T.);
#8824=ORIENTED_EDGE('',*,*,#5970,.F.);
#8825=ORIENTED_EDGE('',*,*,#5975,.F.);
#8826=ORIENTED_EDGE('',*,*,#5976,.T.);
#8827=ORIENTED_EDGE('',*,*,#5977,.T.);
#8828=ORIENTED_EDGE('',*,*,#5973,.F.);
#8829=ORIENTED_EDGE('',*,*,#5978,.F.);
#8830=ORIENTED_EDGE('',*,*,#5979,.T.);
#8831=ORIENTED_EDGE('',*,*,#5980,.T.);
#8832=ORIENTED_EDGE('',*,*,#5976,.F.);
#8833=ORIENTED_EDGE('',*,*,#5981,.F.);
#8834=ORIENTED_EDGE('',*,*,#5968,.T.);
#8835=ORIENTED_EDGE('',*,*,#5982,.T.);
#8836=ORIENTED_EDGE('',*,*,#5979,.F.);
#8837=ORIENTED_EDGE('',*,*,#5982,.F.);
#8838=ORIENTED_EDGE('',*,*,#5967,.F.);
#8839=ORIENTED_EDGE('',*,*,#5971,.F.);
#8840=ORIENTED_EDGE('',*,*,#5974,.F.);
#8841=ORIENTED_EDGE('',*,*,#5977,.F.);
#8842=ORIENTED_EDGE('',*,*,#5980,.F.);
#8843=ORIENTED_EDGE('',*,*,#5983,.T.);
#8844=ORIENTED_EDGE('',*,*,#5959,.T.);
#8845=ORIENTED_EDGE('',*,*,#5962,.T.);
#8846=ORIENTED_EDGE('',*,*,#5964,.T.);
#8847=ORIENTED_EDGE('',*,*,#5844,.F.);
#8848=ORIENTED_EDGE('',*,*,#5983,.F.);
#8849=ORIENTED_EDGE('',*,*,#5984,.T.);
#8850=ORIENTED_EDGE('',*,*,#5985,.T.);
#8851=ORIENTED_EDGE('',*,*,#5984,.F.);
#8852=ORIENTED_EDGE('',*,*,#5985,.F.);
#8853=ORIENTED_EDGE('',*,*,#5965,.T.);
#8854=ORIENTED_EDGE('',*,*,#5981,.T.);
#8855=ORIENTED_EDGE('',*,*,#5978,.T.);
#8856=ORIENTED_EDGE('',*,*,#5975,.T.);
#8857=ORIENTED_EDGE('',*,*,#5972,.T.);
#8858=ORIENTED_EDGE('',*,*,#5969,.T.);
#8859=ORIENTED_EDGE('',*,*,#5957,.T.);
#9190=CYLINDRICAL_SURFACE('',#10602,0.14635);
#9191=CYLINDRICAL_SURFACE('',#10604,0.14635);
#9192=CYLINDRICAL_SURFACE('',#10605,0.14635);
#9193=CYLINDRICAL_SURFACE('',#10606,0.14635);
#9194=CYLINDRICAL_SURFACE('',#10607,0.14635);
#9195=CYLINDRICAL_SURFACE('',#10608,0.14635);
#9196=CYLINDRICAL_SURFACE('',#10609,0.14635);
#9197=CYLINDRICAL_SURFACE('',#10610,0.14635);
#9198=CYLINDRICAL_SURFACE('',#10611,0.14635);
#9199=CYLINDRICAL_SURFACE('',#10612,0.14635);
#9200=CYLINDRICAL_SURFACE('',#10613,0.14635);
#9201=CYLINDRICAL_SURFACE('',#10614,0.14635);
#9202=CYLINDRICAL_SURFACE('',#10615,0.14635);
#9203=CYLINDRICAL_SURFACE('',#10616,0.14635);
#9204=CYLINDRICAL_SURFACE('',#10617,0.14635);
#9205=CYLINDRICAL_SURFACE('',#10618,0.14635);
#9206=CYLINDRICAL_SURFACE('',#10619,0.14635);
#9207=CYLINDRICAL_SURFACE('',#10620,0.14635);
#9208=CYLINDRICAL_SURFACE('',#10621,0.117775);
#9209=CYLINDRICAL_SURFACE('',#10623,0.117775);
#9210=CYLINDRICAL_SURFACE('',#10624,0.117775);
#9211=CYLINDRICAL_SURFACE('',#10625,0.117775);
#9212=CYLINDRICAL_SURFACE('',#10626,0.117775);
#9213=CYLINDRICAL_SURFACE('',#10627,0.117775);
#9214=CYLINDRICAL_SURFACE('',#10628,0.117775);
#9215=CYLINDRICAL_SURFACE('',#10629,0.117775);
#9216=CYLINDRICAL_SURFACE('',#10630,0.117775);
#9217=CYLINDRICAL_SURFACE('',#10631,0.117775);
#9218=CYLINDRICAL_SURFACE('',#10632,0.117775);
#9219=CYLINDRICAL_SURFACE('',#10633,0.117775);
#9220=CYLINDRICAL_SURFACE('',#10634,0.117775);
#9221=CYLINDRICAL_SURFACE('',#10635,0.117775);
#9222=CYLINDRICAL_SURFACE('',#10636,0.117775);
#9223=CYLINDRICAL_SURFACE('',#10637,0.117775);
#9224=CYLINDRICAL_SURFACE('',#10638,0.117775);
#9225=CYLINDRICAL_SURFACE('',#10639,0.117775);
#9226=CYLINDRICAL_SURFACE('',#10643,0.117775);
#9227=CYLINDRICAL_SURFACE('',#10645,0.14635);
#9228=CYLINDRICAL_SURFACE('',#10655,0.3);
#9715=ADVANCED_FACE('',(#925),#9190,.T.);
#9716=ADVANCED_FACE('',(#926),#9191,.T.);
#9717=ADVANCED_FACE('',(#927),#9192,.T.);
#9718=ADVANCED_FACE('',(#928),#9193,.T.);
#9719=ADVANCED_FACE('',(#929),#9194,.T.);
#9720=ADVANCED_FACE('',(#930),#9195,.T.);
#9721=ADVANCED_FACE('',(#931),#9196,.T.);
#9722=ADVANCED_FACE('',(#932),#9197,.T.);
#9723=ADVANCED_FACE('',(#933),#9198,.T.);
#9724=ADVANCED_FACE('',(#934),#9199,.T.);
#9725=ADVANCED_FACE('',(#935),#9200,.T.);
#9726=ADVANCED_FACE('',(#936),#9201,.T.);
#9727=ADVANCED_FACE('',(#937),#9202,.T.);
#9728=ADVANCED_FACE('',(#938),#9203,.T.);
#9729=ADVANCED_FACE('',(#939),#9204,.T.);
#9730=ADVANCED_FACE('',(#940),#9205,.T.);
#9731=ADVANCED_FACE('',(#941),#9206,.T.);
#9732=ADVANCED_FACE('',(#942),#9207,.T.);
#9733=ADVANCED_FACE('',(#943),#9208,.T.);
#9734=ADVANCED_FACE('',(#944),#9209,.T.);
#9735=ADVANCED_FACE('',(#945),#9210,.T.);
#9736=ADVANCED_FACE('',(#946),#9211,.T.);
#9737=ADVANCED_FACE('',(#947),#9212,.T.);
#9738=ADVANCED_FACE('',(#948),#9213,.T.);
#9739=ADVANCED_FACE('',(#949),#9214,.T.);
#9740=ADVANCED_FACE('',(#950),#9215,.T.);
#9741=ADVANCED_FACE('',(#951),#9216,.T.);
#9742=ADVANCED_FACE('',(#952),#9217,.T.);
#9743=ADVANCED_FACE('',(#953),#9218,.T.);
#9744=ADVANCED_FACE('',(#954),#9219,.T.);
#9745=ADVANCED_FACE('',(#955),#9220,.T.);
#9746=ADVANCED_FACE('',(#956),#9221,.T.);
#9747=ADVANCED_FACE('',(#957),#9222,.T.);
#9748=ADVANCED_FACE('',(#958),#9223,.T.);
#9749=ADVANCED_FACE('',(#959),#9224,.T.);
#9750=ADVANCED_FACE('',(#960),#9225,.T.);
#9751=ADVANCED_FACE('',(#961),#141,.T.);
#9752=ADVANCED_FACE('',(#962),#233,.F.);
#9753=ADVANCED_FACE('',(#963),#9226,.T.);
#9754=ADVANCED_FACE('',(#964),#234,.F.);
#9755=ADVANCED_FACE('',(#965),#9227,.T.);
#9756=ADVANCED_FACE('',(#966),#429,.F.);
#9757=ADVANCED_FACE('',(#967),#430,.F.);
#9758=ADVANCED_FACE('',(#968),#431,.F.);
#9759=ADVANCED_FACE('',(#969),#432,.F.);
#9760=ADVANCED_FACE('',(#970),#433,.F.);
#9761=ADVANCED_FACE('',(#971),#434,.F.);
#9762=ADVANCED_FACE('',(#972),#435,.F.);
#9763=ADVANCED_FACE('',(#973,#300),#436,.T.);
#9764=ADVANCED_FACE('',(#974),#9228,.T.);
#9765=ADVANCED_FACE('',(#975,#301),#437,.F.);
#9766=ADVANCED_FACE('',(#976),#438,.T.);
#9783=CLOSED_SHELL('',(#9715,#9716,#9717,#9718,#9719,#9720,#9721,#9722,
#9723,#9724,#9725,#9726,#9727,#9728,#9729,#9730,#9731,#9732,#9733,#9734,
#9735,#9736,#9737,#9738,#9739,#9740,#9741,#9742,#9743,#9744,#9745,#9746,
#9747,#9748,#9749,#9750,#9751,#9752,#9753,#9754,#9755,#9756,#9757,#9758,
#9759,#9760,#9761,#9762,#9763,#9764,#9765,#9766));
#10601=AXIS2_PLACEMENT_3D('',#33731,#12466,#12467);
#10602=AXIS2_PLACEMENT_3D('',#33732,#12468,#12469);
#10603=AXIS2_PLACEMENT_3D('',#33748,#12471,#12472);
#10604=AXIS2_PLACEMENT_3D('',#33756,#12473,#12474);
#10605=AXIS2_PLACEMENT_3D('',#33804,#12476,#12477);
#10606=AXIS2_PLACEMENT_3D('',#33852,#12479,#12480);
#10607=AXIS2_PLACEMENT_3D('',#33906,#12482,#12483);
#10608=AXIS2_PLACEMENT_3D('',#33954,#12485,#12486);
#10609=AXIS2_PLACEMENT_3D('',#34002,#12488,#12489);
#10610=AXIS2_PLACEMENT_3D('',#34056,#12491,#12492);
#10611=AXIS2_PLACEMENT_3D('',#34104,#12494,#12495);
#10612=AXIS2_PLACEMENT_3D('',#34152,#12497,#12498);
#10613=AXIS2_PLACEMENT_3D('',#34206,#12500,#12501);
#10614=AXIS2_PLACEMENT_3D('',#34254,#12503,#12504);
#10615=AXIS2_PLACEMENT_3D('',#34302,#12506,#12507);
#10616=AXIS2_PLACEMENT_3D('',#34356,#12509,#12510);
#10617=AXIS2_PLACEMENT_3D('',#34404,#12512,#12513);
#10618=AXIS2_PLACEMENT_3D('',#34452,#12515,#12516);
#10619=AXIS2_PLACEMENT_3D('',#34503,#12518,#12519);
#10620=AXIS2_PLACEMENT_3D('',#34551,#12521,#12522);
#10621=AXIS2_PLACEMENT_3D('',#34599,#12524,#12525);
#10622=AXIS2_PLACEMENT_3D('',#34615,#12527,#12528);
#10623=AXIS2_PLACEMENT_3D('',#34625,#12529,#12530);
#10624=AXIS2_PLACEMENT_3D('',#34649,#12532,#12533);
#10625=AXIS2_PLACEMENT_3D('',#34673,#12535,#12536);
#10626=AXIS2_PLACEMENT_3D('',#34699,#12538,#12539);
#10627=AXIS2_PLACEMENT_3D('',#34723,#12541,#12542);
#10628=AXIS2_PLACEMENT_3D('',#34747,#12544,#12545);
#10629=AXIS2_PLACEMENT_3D('',#34772,#12547,#12548);
#10630=AXIS2_PLACEMENT_3D('',#34797,#12550,#12551);
#10631=AXIS2_PLACEMENT_3D('',#34821,#12553,#12554);
#10632=AXIS2_PLACEMENT_3D('',#34846,#12556,#12557);
#10633=AXIS2_PLACEMENT_3D('',#34871,#12559,#12560);
#10634=AXIS2_PLACEMENT_3D('',#34895,#12562,#12563);
#10635=AXIS2_PLACEMENT_3D('',#34920,#12565,#12566);
#10636=AXIS2_PLACEMENT_3D('',#34945,#12568,#12569);
#10637=AXIS2_PLACEMENT_3D('',#34969,#12571,#12572);
#10638=AXIS2_PLACEMENT_3D('',#34994,#12574,#12575);
#10639=AXIS2_PLACEMENT_3D('',#35019,#12577,#12578);
#10640=AXIS2_PLACEMENT_3D('',#35043,#12580,#12581);
#10641=AXIS2_PLACEMENT_3D('',#35202,#12582,#12583);
#10642=AXIS2_PLACEMENT_3D('',#35221,#12585,#12586);
#10643=AXIS2_PLACEMENT_3D('',#35789,#12587,#12588);
#10644=AXIS2_PLACEMENT_3D('',#35800,#12589,#12590);
#10645=AXIS2_PLACEMENT_3D('',#36367,#12591,#12592);
#10646=AXIS2_PLACEMENT_3D('',#36368,#12593,#12594);
#10647=AXIS2_PLACEMENT_3D('',#36377,#12599,#12600);
#10648=AXIS2_PLACEMENT_3D('',#36383,#12604,#12605);
#10649=AXIS2_PLACEMENT_3D('',#36389,#12609,#12610);
#10650=AXIS2_PLACEMENT_3D('',#36395,#12614,#12615);
#10651=AXIS2_PLACEMENT_3D('',#36401,#12619,#12620);
#10652=AXIS2_PLACEMENT_3D('',#36404,#12623,#12624);
#10653=AXIS2_PLACEMENT_3D('',#36405,#12625,#12626);
#10654=AXIS2_PLACEMENT_3D('',#36407,#12627,#12628);
#10655=AXIS2_PLACEMENT_3D('',#36408,#12629,#12630);
#10656=AXIS2_PLACEMENT_3D('',#36411,#12632,#12633);
#10657=AXIS2_PLACEMENT_3D('',#36412,#12634,#12635);
#10658=AXIS2_PLACEMENT_3D('',#36413,#12636,#12637);
#12466=DIRECTION('axis',(0.,0.,1.));
#12467=DIRECTION('refdir',(1.,0.,0.));
#12468=DIRECTION('center_axis',(0.,0.,1.));
#12469=DIRECTION('ref_axis',(1.,0.,0.));
#12470=DIRECTION('',(0.,0.,-1.));
#12471=DIRECTION('center_axis',(0.,0.,-1.));
#12472=DIRECTION('ref_axis',(1.,0.,0.));
#12473=DIRECTION('center_axis',(0.,0.,1.));
#12474=DIRECTION('ref_axis',(1.,0.,0.));
#12475=DIRECTION('',(0.,0.,-1.));
#12476=DIRECTION('center_axis',(0.,0.,1.));
#12477=DIRECTION('ref_axis',(1.,0.,0.));
#12478=DIRECTION('',(0.,0.,-1.));
#12479=DIRECTION('center_axis',(0.,0.,1.));
#12480=DIRECTION('ref_axis',(1.,0.,0.));
#12481=DIRECTION('',(0.,0.,-1.));
#12482=DIRECTION('center_axis',(0.,0.,1.));
#12483=DIRECTION('ref_axis',(1.,0.,0.));
#12484=DIRECTION('',(0.,0.,-1.));
#12485=DIRECTION('center_axis',(0.,0.,1.));
#12486=DIRECTION('ref_axis',(1.,0.,0.));
#12487=DIRECTION('',(0.,0.,-1.));
#12488=DIRECTION('center_axis',(0.,0.,1.));
#12489=DIRECTION('ref_axis',(1.,0.,0.));
#12490=DIRECTION('',(0.,0.,-1.));
#12491=DIRECTION('center_axis',(0.,0.,1.));
#12492=DIRECTION('ref_axis',(1.,0.,0.));
#12493=DIRECTION('',(0.,0.,-1.));
#12494=DIRECTION('center_axis',(0.,0.,1.));
#12495=DIRECTION('ref_axis',(1.,0.,0.));
#12496=DIRECTION('',(0.,0.,-1.));
#12497=DIRECTION('center_axis',(0.,0.,1.));
#12498=DIRECTION('ref_axis',(1.,0.,0.));
#12499=DIRECTION('',(0.,0.,-1.));
#12500=DIRECTION('center_axis',(0.,0.,1.));
#12501=DIRECTION('ref_axis',(1.,0.,0.));
#12502=DIRECTION('',(0.,0.,-1.));
#12503=DIRECTION('center_axis',(0.,0.,1.));
#12504=DIRECTION('ref_axis',(1.,0.,0.));
#12505=DIRECTION('',(0.,0.,-1.));
#12506=DIRECTION('center_axis',(0.,0.,1.));
#12507=DIRECTION('ref_axis',(1.,0.,0.));
#12508=DIRECTION('',(0.,0.,-1.));
#12509=DIRECTION('center_axis',(0.,0.,1.));
#12510=DIRECTION('ref_axis',(1.,0.,0.));
#12511=DIRECTION('',(0.,0.,-1.));
#12512=DIRECTION('center_axis',(0.,0.,1.));
#12513=DIRECTION('ref_axis',(1.,0.,0.));
#12514=DIRECTION('',(0.,0.,-1.));
#12515=DIRECTION('center_axis',(0.,0.,1.));
#12516=DIRECTION('ref_axis',(1.,0.,0.));
#12517=DIRECTION('',(0.,0.,-1.));
#12518=DIRECTION('center_axis',(0.,0.,1.));
#12519=DIRECTION('ref_axis',(1.,0.,0.));
#12520=DIRECTION('',(0.,0.,-1.));
#12521=DIRECTION('center_axis',(0.,0.,1.));
#12522=DIRECTION('ref_axis',(1.,0.,0.));
#12523=DIRECTION('',(0.,0.,-1.));
#12524=DIRECTION('center_axis',(0.,0.,1.));
#12525=DIRECTION('ref_axis',(1.,1.10671505702589E-13,0.));
#12526=DIRECTION('',(0.,0.,1.));
#12527=DIRECTION('center_axis',(0.,0.,-1.));
#12528=DIRECTION('ref_axis',(1.,1.10671505702589E-13,0.));
#12529=DIRECTION('center_axis',(0.,0.,1.));
#12530=DIRECTION('ref_axis',(1.,1.10671505702589E-13,0.));
#12531=DIRECTION('',(0.,0.,1.));
#12532=DIRECTION('center_axis',(0.,0.,1.));
#12533=DIRECTION('ref_axis',(1.,1.10671505702589E-13,0.));
#12534=DIRECTION('',(0.,0.,1.));
#12535=DIRECTION('center_axis',(0.,0.,1.));
#12536=DIRECTION('ref_axis',(1.,1.10671505702589E-13,0.));
#12537=DIRECTION('',(0.,0.,1.));
#12538=DIRECTION('center_axis',(0.,0.,1.));
#12539=DIRECTION('ref_axis',(1.,1.10671505702589E-13,0.));
#12540=DIRECTION('',(0.,0.,1.));
#12541=DIRECTION('center_axis',(0.,0.,1.));
#12542=DIRECTION('ref_axis',(1.,1.10671505702589E-13,0.));
#12543=DIRECTION('',(0.,0.,1.));
#12544=DIRECTION('center_axis',(0.,0.,1.));
#12545=DIRECTION('ref_axis',(1.,1.10671505702589E-13,0.));
#12546=DIRECTION('',(0.,0.,1.));
#12547=DIRECTION('center_axis',(0.,0.,1.));
#12548=DIRECTION('ref_axis',(1.,1.10671505702589E-13,0.));
#12549=DIRECTION('',(0.,0.,1.));
#12550=DIRECTION('center_axis',(0.,0.,1.));
#12551=DIRECTION('ref_axis',(1.,1.10671505702589E-13,0.));
#12552=DIRECTION('',(0.,0.,1.));
#12553=DIRECTION('center_axis',(0.,0.,1.));
#12554=DIRECTION('ref_axis',(1.,1.10671505702589E-13,0.));
#12555=DIRECTION('',(0.,0.,1.));
#12556=DIRECTION('center_axis',(0.,0.,1.));
#12557=DIRECTION('ref_axis',(1.,1.10671505702589E-13,0.));
#12558=DIRECTION('',(0.,0.,1.));
#12559=DIRECTION('center_axis',(0.,0.,1.));
#12560=DIRECTION('ref_axis',(1.,1.10671505702589E-13,0.));
#12561=DIRECTION('',(0.,0.,1.));
#12562=DIRECTION('center_axis',(0.,0.,1.));
#12563=DIRECTION('ref_axis',(1.,1.10671505702589E-13,0.));
#12564=DIRECTION('',(0.,0.,1.));
#12565=DIRECTION('center_axis',(0.,0.,1.));
#12566=DIRECTION('ref_axis',(1.,1.10671505702589E-13,0.));
#12567=DIRECTION('',(0.,0.,1.));
#12568=DIRECTION('center_axis',(0.,0.,1.));
#12569=DIRECTION('ref_axis',(1.,1.10671505702589E-13,0.));
#12570=DIRECTION('',(0.,0.,1.));
#12571=DIRECTION('center_axis',(0.,0.,1.));
#12572=DIRECTION('ref_axis',(1.,1.10671505702589E-13,0.));
#12573=DIRECTION('',(0.,0.,1.));
#12574=DIRECTION('center_axis',(0.,0.,1.));
#12575=DIRECTION('ref_axis',(1.,1.10671505702589E-13,0.));
#12576=DIRECTION('',(0.,0.,1.));
#12577=DIRECTION('center_axis',(0.,0.,1.));
#12578=DIRECTION('ref_axis',(1.,1.10671505702589E-13,0.));
#12579=DIRECTION('',(0.,0.,1.));
#12580=DIRECTION('center_axis',(0.,0.,-1.));
#12581=DIRECTION('ref_axis',(1.,0.,0.));
#12582=DIRECTION('center_axis',(0.,0.,-1.));
#12583=DIRECTION('ref_axis',(1.,0.,0.));
#12584=DIRECTION('',(0.707106781186548,8.65956056235493E-17,0.707106781186547));
#12585=DIRECTION('center_axis',(0.,0.,1.));
#12586=DIRECTION('ref_axis',(1.,0.,0.));
#12587=DIRECTION('center_axis',(0.,0.,1.));
#12588=DIRECTION('ref_axis',(1.,1.10671505702589E-13,0.));
#12589=DIRECTION('center_axis',(0.,0.,-1.));
#12590=DIRECTION('ref_axis',(1.,1.10671505702589E-13,0.));
#12591=DIRECTION('center_axis',(0.,0.,1.));
#12592=DIRECTION('ref_axis',(1.,0.,0.));
#12593=DIRECTION('center_axis',(-2.40370335797945E-16,-1.,0.));
#12594=DIRECTION('ref_axis',(1.,-2.40370335797945E-16,0.));
#12595=DIRECTION('',(1.,-2.40370335797945E-16,0.));
#12596=DIRECTION('',(0.,0.,1.));
#12597=DIRECTION('',(1.,-2.40370335797945E-16,0.));
#12598=DIRECTION('',(0.,0.,1.));
#12599=DIRECTION('center_axis',(-0.866025403784439,-0.5,0.));
#12600=DIRECTION('ref_axis',(0.5,-0.866025403784439,0.));
#12601=DIRECTION('',(0.5,-0.866025403784439,0.));
#12602=DIRECTION('',(0.,0.,1.));
#12603=DIRECTION('',(0.5,-0.866025403784439,0.));
#12604=DIRECTION('center_axis',(-0.866025403784439,0.5,0.));
#12605=DIRECTION('ref_axis',(-0.5,-0.866025403784439,0.));
#12606=DIRECTION('',(-0.5,-0.866025403784439,0.));
#12607=DIRECTION('',(0.,0.,1.));
#12608=DIRECTION('',(-0.5,-0.866025403784439,0.));
#12609=DIRECTION('center_axis',(1.20185167898973E-16,1.,0.));
#12610=DIRECTION('ref_axis',(-1.,1.20185167898973E-16,0.));
#12611=DIRECTION('',(-1.,1.20185167898973E-16,0.));
#12612=DIRECTION('',(0.,0.,1.));
#12613=DIRECTION('',(-1.,1.20185167898973E-16,0.));
#12614=DIRECTION('center_axis',(0.866025403784439,0.5,0.));
#12615=DIRECTION('ref_axis',(-0.5,0.866025403784439,0.));
#12616=DIRECTION('',(-0.5,0.866025403784439,0.));
#12617=DIRECTION('',(0.,0.,1.));
#12618=DIRECTION('',(-0.5,0.866025403784439,0.));
#12619=DIRECTION('center_axis',(0.866025403784439,-0.5,0.));
#12620=DIRECTION('ref_axis',(0.5,0.866025403784439,0.));
#12621=DIRECTION('',(0.5,0.866025403784439,0.));
#12622=DIRECTION('',(0.5,0.866025403784439,0.));
#12623=DIRECTION('center_axis',(0.,0.,1.));
#12624=DIRECTION('ref_axis',(1.,0.,0.));
#12625=DIRECTION('center_axis',(0.,0.,1.));
#12626=DIRECTION('ref_axis',(1.,0.,0.));
#12627=DIRECTION('center_axis',(0.,0.,1.));
#12628=DIRECTION('ref_axis',(1.,0.,0.));
#12629=DIRECTION('center_axis',(0.,0.,1.));
#12630=DIRECTION('ref_axis',(1.,0.,0.));
#12631=DIRECTION('',(0.,0.,-1.));
#12632=DIRECTION('center_axis',(0.,0.,1.));
#12633=DIRECTION('ref_axis',(1.,0.,0.));
#12634=DIRECTION('center_axis',(0.,0.,1.));
#12635=DIRECTION('ref_axis',(1.,0.,0.));
#12636=DIRECTION('center_axis',(0.,0.,1.));
#12637=DIRECTION('ref_axis',(1.,0.,0.));
#33731=CARTESIAN_POINT('',(0.,0.,0.));
#33732=CARTESIAN_POINT('Origin',(0.,0.,0.));
#33733=CARTESIAN_POINT('',(-0.146500586129689,0.000104807665585484,0.0160655045842905));
#33734=CARTESIAN_POINT('',(-0.146471000393815,0.000161627070721384,0.00893449541570859));
#33735=CARTESIAN_POINT('',(-0.14635,-1.79227059055215E-17,0.));
#33736=CARTESIAN_POINT('',(0.0634007094575212,0.131904027763685,0.));
#33737=CARTESIAN_POINT('Ctrl Pts',(-0.146500586129689,0.000104807665585484,
0.0160655045842905));
#33738=CARTESIAN_POINT('Ctrl Pts',(-0.14654494062996,0.00598698351314685,
0.0157446908947048));
#33739=CARTESIAN_POINT('Ctrl Pts',(-0.146221105349753,0.0118639507829193,
0.0154238772051191));
#33740=CARTESIAN_POINT('Ctrl Pts',(-0.145512600887712,0.0176938044004412,
0.0151030635155334));
#33741=CARTESIAN_POINT('Ctrl Pts',(-0.139696831446137,0.0655482447521769,
0.0124696595607311));
#33742=CARTESIAN_POINT('Ctrl Pts',(-0.107962161373412,0.110228180545907,
0.00983625560592885));
#33743=CARTESIAN_POINT('Ctrl Pts',(-0.06469522132477,0.13152107817143,0.0072028516511266));
#33744=CARTESIAN_POINT('Ctrl Pts',(-0.0252475006917791,0.150934428781716,
0.00480190110075107));
#33745=CARTESIAN_POINT('Ctrl Pts',(0.0237864150713563,0.150907312609249,
0.00240095055037554));
#33746=CARTESIAN_POINT('Ctrl Pts',(0.0635538308725811,0.132076982143462,
1.66967134562768E-17));
#33747=CARTESIAN_POINT('',(-0.063400709457524,0.131904027763684,0.));
#33748=CARTESIAN_POINT('Origin',(0.,0.,0.));
#33749=CARTESIAN_POINT('Ctrl Pts',(-0.0634007094575239,0.131904027763684,
1.49186218934005E-16));
#33750=CARTESIAN_POINT('Ctrl Pts',(-0.107082934395073,0.110907822426531,
0.00263534106650592));
#33751=CARTESIAN_POINT('Ctrl Pts',(-0.139152358317953,0.0667027373135744,
0.00527068213301169));
#33752=CARTESIAN_POINT('Ctrl Pts',(-0.145347393378452,0.0189333151714045,
0.00790602319951745));
#33753=CARTESIAN_POINT('Ctrl Pts',(-0.146153287982764,0.0127191260377668,
0.00824884727158116));
#33754=CARTESIAN_POINT('Ctrl Pts',(-0.14652131876894,0.00644461879462582,
0.00859167134364488));
#33755=CARTESIAN_POINT('Ctrl Pts',(-0.146471000393815,0.000161627070721384,
0.00893449541570859));
#33756=CARTESIAN_POINT('Origin',(0.,0.,0.));
#33757=CARTESIAN_POINT('',(-0.146124286466753,3.81045546672121E-5,0.0660655045842905));
#33758=CARTESIAN_POINT('',(-0.146121893894205,3.63833482308178E-5,0.0589344954157087));
#33759=CARTESIAN_POINT('',(-0.14635,-1.79227059055215E-17,0.));
#33760=CARTESIAN_POINT('Ctrl Pts',(-0.146124286466753,3.81045546672121E-5,
0.0660655045842905));
#33761=CARTESIAN_POINT('Ctrl Pts',(-0.146175624225919,0.0219480700681356,
0.0648784479568517));
#33762=CARTESIAN_POINT('Ctrl Pts',(-0.141554683648142,0.0438374299905643,
0.0636913913294129));
#33763=CARTESIAN_POINT('Ctrl Pts',(-0.132150173022132,0.0634306246655632,
0.062504334701974));
#33764=CARTESIAN_POINT('Ctrl Pts',(-0.111286909296501,0.106896787232447,
0.0598709307471717));
#33765=CARTESIAN_POINT('Ctrl Pts',(-0.0668815981213141,0.139062512957816,
0.0572375267923695));
#33766=CARTESIAN_POINT('Ctrl Pts',(-0.0190775358903001,0.145337701034954,
0.0546041228375673));
#33767=CARTESIAN_POINT('Ctrl Pts',(0.028726526340714,0.151612889112092,
0.051970718882765));
#33768=CARTESIAN_POINT('Ctrl Pts',(0.0799293396275551,0.131997539540999,
0.0493373149279628));
#33769=CARTESIAN_POINT('Ctrl Pts',(0.111303508306999,0.0953874982726326,
0.0467039109731605));
#33770=CARTESIAN_POINT('Ctrl Pts',(0.142677676986443,0.0587774570042668,
0.0440705070183582));
#33771=CARTESIAN_POINT('Ctrl Pts',(0.154223201058489,0.00517272403862895,
0.041437103063556));
#33772=CARTESIAN_POINT('Ctrl Pts',(0.14070340769012,-0.0411058697401277,
0.0388036991087537));
#33773=CARTESIAN_POINT('Ctrl Pts',(0.12718361432175,-0.0873844635188848,
0.0361702951539514));
#33774=CARTESIAN_POINT('Ctrl Pts',(0.0885985035129631,-0.12633691811076,
0.0335368911991492));
#33775=CARTESIAN_POINT('Ctrl Pts',(0.0424500313328507,-0.140301337584722,
0.030903487244347));
#33776=CARTESIAN_POINT('Ctrl Pts',(-0.00369844084726173,-0.154265757058684,
0.0282700832895447));
#33777=CARTESIAN_POINT('Ctrl Pts',(-0.0574102743986997,-0.143242141414731,
0.0256366793347424));
#33778=CARTESIAN_POINT('Ctrl Pts',(-0.0943177567692062,-0.112215861137884,
0.0230032753799401));
#33779=CARTESIAN_POINT('Ctrl Pts',(-0.126728995572139,-0.0849693486522956,
0.0206906851147236));
#33780=CARTESIAN_POINT('Ctrl Pts',(-0.146180856053097,-0.0422969446440751,
0.0183780948495071));
#33781=CARTESIAN_POINT('Ctrl Pts',(-0.146500586129689,0.000104807665585484,
0.0160655045842905));
#33782=CARTESIAN_POINT('Ctrl Pts',(-0.146471000393815,0.000161627070721384,
0.00893449541570859));
#33783=CARTESIAN_POINT('Ctrl Pts',(-0.146134513724681,-0.0418536993801969,
0.0112270124101507));
#33784=CARTESIAN_POINT('Ctrl Pts',(-0.127090283331881,-0.0842484349621326,
0.0135195294045928));
#33785=CARTESIAN_POINT('Ctrl Pts',(-0.0951738980203006,-0.111522448354846,
0.0158120463990349));
#33786=CARTESIAN_POINT('Ctrl Pts',(-0.0584847214035319,-0.142875030567541,
0.0184473874655407));
#33787=CARTESIAN_POINT('Ctrl Pts',(-0.00478572197187679,-0.154246435821546,
0.0210827285320465));
#33788=CARTESIAN_POINT('Ctrl Pts',(0.0414949714453012,-0.140576153089947,
0.0237180695985523));
#33789=CARTESIAN_POINT('Ctrl Pts',(0.0877756648624791,-0.126905870358348,
0.0263534106650582));
#33790=CARTESIAN_POINT('Ctrl Pts',(0.12663805226518,-0.0881938996411451,
0.028988751731564));
#33791=CARTESIAN_POINT('Ctrl Pts',(0.140447863117085,-0.0419714582064656,
0.0316240927980698));
#33792=CARTESIAN_POINT('Ctrl Pts',(0.154257673968991,0.00425098322821388,
0.0342594338645756));
#33793=CARTESIAN_POINT('Ctrl Pts',(0.143014908270101,0.0579838953803693,
0.0368947749310814));
#33794=CARTESIAN_POINT('Ctrl Pts',(0.111816739036639,0.0947918176848183,
0.0395301159975872));
#33795=CARTESIAN_POINT('Ctrl Pts',(0.0806185698031766,0.131599739989267,
0.042165457064093));
#33796=CARTESIAN_POINT('Ctrl Pts',(0.0294649970351413,0.15148267244601,
0.0448007981305989));
#33797=CARTESIAN_POINT('Ctrl Pts',(-0.0184028717348104,0.145423626667293,
0.0474361391971047));
#33798=CARTESIAN_POINT('Ctrl Pts',(-0.0662707405047621,0.139364580888577,
0.0500714802636105));
#33799=CARTESIAN_POINT('Ctrl Pts',(-0.11085290527663,0.107363556874401,
0.0527068213301163));
#33800=CARTESIAN_POINT('Ctrl Pts',(-0.131901071754926,0.0639489919997987,
0.0553421623966221));
#33801=CARTESIAN_POINT('Ctrl Pts',(-0.141464922191872,0.0442223138744639,
0.0565396067363176));
#33802=CARTESIAN_POINT('Ctrl Pts',(-0.146169931163403,0.0221391901971212,
0.0577370510760131));
#33803=CARTESIAN_POINT('Ctrl Pts',(-0.146121893894205,3.63833482308178E-5,
0.0589344954157087));
#33804=CARTESIAN_POINT('Origin',(0.,0.,0.));
#33805=CARTESIAN_POINT('',(-0.146368002745976,-0.000129372869328834,0.116065504584291));
#33806=CARTESIAN_POINT('',(-0.146366557616609,-0.000129983413451606,0.108934495415709));
#33807=CARTESIAN_POINT('',(-0.14635,-1.79227059055215E-17,0.));
#33808=CARTESIAN_POINT('Ctrl Pts',(-0.146368002745976,-0.000129372869328834,
0.116065504584291));
#33809=CARTESIAN_POINT('Ctrl Pts',(-0.146025111950034,0.0376095209348488,
0.114012205018999));
#33810=CARTESIAN_POINT('Ctrl Pts',(-0.131097704503774,0.0755892522017571,
0.111958905453707));
#33811=CARTESIAN_POINT('Ctrl Pts',(-0.104818007194008,0.1024708903805,0.109905605888415));
#33812=CARTESIAN_POINT('Ctrl Pts',(-0.0711136904949951,0.136947210099294,
0.107272201933612));
#33813=CARTESIAN_POINT('Ctrl Pts',(-0.0187363862257596,0.153168661700715,
0.10463879797881));
#33814=CARTESIAN_POINT('Ctrl Pts',(0.0285541005041433,0.143776766284718,
0.102005394024008));
#33815=CARTESIAN_POINT('Ctrl Pts',(0.0758445872340461,0.134384870868722,
0.0993719900692057));
#33816=CARTESIAN_POINT('Ctrl Pts',(0.118048256424616,0.0993796284353078,
0.0967385861144034));
#33817=CARTESIAN_POINT('Ctrl Pts',(0.136020336225278,0.0546403479960236,
0.0941051821596012));
#33818=CARTESIAN_POINT('Ctrl Pts',(0.153992416025939,0.00990106755673973,
0.0914717782047989));
#33819=CARTESIAN_POINT('Ctrl Pts',(0.147732906436694,-0.0445722508884142,
0.0888383742499967));
#33820=CARTESIAN_POINT('Ctrl Pts',(0.120081310876684,-0.0840688974447852,
0.0862049702951944));
#33821=CARTESIAN_POINT('Ctrl Pts',(0.092429715316675,-0.123565544001157,
0.0835715663403921));
#33822=CARTESIAN_POINT('Ctrl Pts',(0.0433860337859016,-0.148085518668745,
0.0809381623855898));
#33823=CARTESIAN_POINT('Ctrl Pts',(-0.00480217723865872,-0.146506046566169,
0.0783047584307875));
#33824=CARTESIAN_POINT('Ctrl Pts',(-0.0529903882632186,-0.144926574463593,
0.0756713544759853));
#33825=CARTESIAN_POINT('Ctrl Pts',(-0.100323128781565,-0.117247655590855,
0.0730379505211831));
#33826=CARTESIAN_POINT('Ctrl Pts',(-0.125328890902702,-0.0760248964502869,
0.0704045465663809));
#33827=CARTESIAN_POINT('Ctrl Pts',(-0.139062832915904,-0.053384075469981,
0.0689581992390174));
#33828=CARTESIAN_POINT('Ctrl Pts',(-0.146061734917782,-0.0266576901787336,
0.067511851911654));
#33829=CARTESIAN_POINT('Ctrl Pts',(-0.146124286466753,3.81045546672121E-5,
0.0660655045842905));
#33830=CARTESIAN_POINT('Ctrl Pts',(-0.146121893894205,3.63833482308178E-5,
0.0589344954157087));
#33831=CARTESIAN_POINT('Ctrl Pts',(-0.146064210518155,-0.026504769812526,
0.060372392142519));
#33832=CARTESIAN_POINT('Ctrl Pts',(-0.139152958627323,-0.0530743047642348,
0.0618102888693293));
#33833=CARTESIAN_POINT('Ctrl Pts',(-0.125571320368441,-0.0756261679111494,
0.0632481855961396));
#33834=CARTESIAN_POINT('Ctrl Pts',(-0.100679234318938,-0.116958657212465,
0.0658835266626455));
#33835=CARTESIAN_POINT('Ctrl Pts',(-0.0533808940352117,-0.144795530080065,
0.0685188677291512));
#33836=CARTESIAN_POINT('Ctrl Pts',(-0.00516183231960515,-0.146494306755382,
0.071154208795657));
#33837=CARTESIAN_POINT('Ctrl Pts',(0.0430572293960016,-0.148193083430699,
0.0737895498621628));
#33838=CARTESIAN_POINT('Ctrl Pts',(0.0921970125434883,-0.123753763913733,
0.0764248909286687));
#33839=CARTESIAN_POINT('Ctrl Pts',(0.119936668638416,-0.0842765346784538,
0.0790602319951745));
#33840=CARTESIAN_POINT('Ctrl Pts',(0.147676324733344,-0.0447993054431753,
0.0816955730616803));
#33841=CARTESIAN_POINT('Ctrl Pts',(0.154015853775713,0.00971583351041531,
0.0843309141281861));
#33842=CARTESIAN_POINT('Ctrl Pts',(0.136075382627054,0.0545053485317346,
0.0869662551946919));
#33843=CARTESIAN_POINT('Ctrl Pts',(0.118134911478395,0.0992948635530542,
0.0896015962611977));
#33844=CARTESIAN_POINT('Ctrl Pts',(0.0759144401387073,0.134358754642102,
0.0922369373277035));
#33845=CARTESIAN_POINT('Ctrl Pts',(0.0285922932904845,0.143769920707126,
0.0948722783942094));
#33846=CARTESIAN_POINT('Ctrl Pts',(-0.0187298535577381,0.15318108677215,
0.0975076194607152));
#33847=CARTESIAN_POINT('Ctrl Pts',(-0.0711536759144954,0.13693952781315,
0.100142960527221));
#33848=CARTESIAN_POINT('Ctrl Pts',(-0.104866248150923,0.102422641268563,
0.102778301593727));
#33849=CARTESIAN_POINT('Ctrl Pts',(-0.131117262559492,0.0755453303453163,
0.104830366201054));
#33850=CARTESIAN_POINT('Ctrl Pts',(-0.146023101823344,0.0375871567885092,
0.106882430808381));
#33851=CARTESIAN_POINT('Ctrl Pts',(-0.146366557616609,-0.000129983413451606,
0.108934495415709));
#33852=CARTESIAN_POINT('Origin',(0.,0.,0.));
#33853=CARTESIAN_POINT('',(-0.14651736545536,8.65668654492988E-5,0.166065504584291));
#33854=CARTESIAN_POINT('',(-0.146524127737672,8.31850724179233E-5,0.158934495415709));
#33855=CARTESIAN_POINT('',(-0.14635,-1.79227059055215E-17,0.));
#33856=CARTESIAN_POINT('Ctrl Pts',(-0.14651736545536,8.65668654492988E-5,
0.166065504584291));
#33857=CARTESIAN_POINT('Ctrl Pts',(-0.146554285531508,0.00533178393548585,
0.165779366035948));
#33858=CARTESIAN_POINT('Ctrl Pts',(-0.146296777197391,0.0105733383781062,
0.165493227487605));
#33859=CARTESIAN_POINT('Ctrl Pts',(-0.145732753046151,0.0157816995937671,
0.165207088939262));
#33860=CARTESIAN_POINT('Ctrl Pts',(-0.140541899038255,0.0637155382981208,
0.16257368498446));
#33861=CARTESIAN_POINT('Ctrl Pts',(-0.109389226009343,0.108837918334108,
0.159940281029658));
#33862=CARTESIAN_POINT('Ctrl Pts',(-0.0664064572564633,0.130680066597967,
0.157306877074855));
#33863=CARTESIAN_POINT('Ctrl Pts',(-0.0234236885035836,0.152522214861825,
0.154673473120053));
#33864=CARTESIAN_POINT('Ctrl Pts',(0.031389175973264,0.151084131353554,
0.152040069165251));
#33865=CARTESIAN_POINT('Ctrl Pts',(0.073167488832194,0.12701817148098,0.149406665210449));
#33866=CARTESIAN_POINT('Ctrl Pts',(0.114945801691124,0.102952211608407,
0.146773261255646));
#33867=CARTESIAN_POINT('Ctrl Pts',(0.143689562932137,0.0562583753715299,
0.144139857300844));
#33868=CARTESIAN_POINT('Ctrl Pts',(0.146359798857064,0.00811829104130666,
0.141506453346042));
#33869=CARTESIAN_POINT('Ctrl Pts',(0.149030034781992,-0.0400217932889162,
0.13887304939124));
#33870=CARTESIAN_POINT('Ctrl Pts',(0.125626745390835,-0.0896081257124856,
0.136239645436437));
#33871=CARTESIAN_POINT('Ctrl Pts',(0.0867663172267087,-0.118146957909964,
0.133606241481635));
#33872=CARTESIAN_POINT('Ctrl Pts',(0.0479058890625822,-0.146685790107443,
0.130972837526833));
#33873=CARTESIAN_POINT('Ctrl Pts',(-0.00641167787451363,-0.154177122078832,
0.128339433572031));
#33874=CARTESIAN_POINT('Ctrl Pts',(-0.0515464175662268,-0.13722267989126,
0.125706029617228));
#33875=CARTESIAN_POINT('Ctrl Pts',(-0.0966811572579399,-0.120268237703689,
0.123072625662426));
#33876=CARTESIAN_POINT('Ctrl Pts',(-0.13263306970427,-0.0788680213571585,
0.120439221707624));
#33877=CARTESIAN_POINT('Ctrl Pts',(-0.143093361363041,-0.0318023192658095,
0.117805817752821));
#33878=CARTESIAN_POINT('Ctrl Pts',(-0.145397626569199,-0.0214343617297895,
0.117225713363311));
#33879=CARTESIAN_POINT('Ctrl Pts',(-0.146464877288401,-0.0107914790330514,
0.116645608973801));
#33880=CARTESIAN_POINT('Ctrl Pts',(-0.146368002745976,-0.000129372869328834,
0.116065504584291));
#33881=CARTESIAN_POINT('Ctrl Pts',(-0.146366557616609,-0.000129983413451606,
0.108934495415709));
#33882=CARTESIAN_POINT('Ctrl Pts',(-0.146464181092139,-0.0108506595114597,
0.109517771874887));
#33883=CARTESIAN_POINT('Ctrl Pts',(-0.145385284604313,-0.0215518621108894,
0.110101048334066));
#33884=CARTESIAN_POINT('Ctrl Pts',(-0.143055987718722,-0.0319735935649507,
0.110684324793244));
#33885=CARTESIAN_POINT('Ctrl Pts',(-0.132531832933994,-0.0790607277237021,
0.11331966585975));
#33886=CARTESIAN_POINT('Ctrl Pts',(-0.0964822012484396,-0.12044278191103,
0.115955006926256));
#33887=CARTESIAN_POINT('Ctrl Pts',(-0.0512822836387571,-0.13732242834474,
0.118590347992762));
#33888=CARTESIAN_POINT('Ctrl Pts',(-0.00608236602907434,-0.154202074778449,
0.121225689059267));
#33889=CARTESIAN_POINT('Ctrl Pts',(0.0482678375047366,-0.14657931345854,
0.123861030125773));
#33890=CARTESIAN_POINT('Ctrl Pts',(0.0870803134198012,-0.117916681520738,
0.126496371192279));
#33891=CARTESIAN_POINT('Ctrl Pts',(0.125892789334866,-0.089254049582936,
0.129131712258785));
#33892=CARTESIAN_POINT('Ctrl Pts',(0.149167537631184,-0.0395515470272406,
0.131767053325291));
#33893=CARTESIAN_POINT('Ctrl Pts',(0.146332238452734,0.00861396207485353,
0.134402394391797));
#33894=CARTESIAN_POINT('Ctrl Pts',(0.143496939274284,0.0567794711769477,
0.137037735458302));
#33895=CARTESIAN_POINT('Ctrl Pts',(0.114551592621066,0.103407986825441,
0.139673076524808));
#33896=CARTESIAN_POINT('Ctrl Pts',(0.0726443273415577,0.127318991170589,
0.142308417591314));
#33897=CARTESIAN_POINT('Ctrl Pts',(0.0307370620620493,0.151229995515737,
0.14494375865782));
#33898=CARTESIAN_POINT('Ctrl Pts',(-0.0241321218437492,0.152423488557541,
0.147579099724326));
#33899=CARTESIAN_POINT('Ctrl Pts',(-0.067039462170215,0.130357334843671,
0.150214440790831));
#33900=CARTESIAN_POINT('Ctrl Pts',(-0.109946802496681,0.108291181129802,
0.152849781857337));
#33901=CARTESIAN_POINT('Ctrl Pts',(-0.140892299243814,0.0629653806602592,
0.155485122923843));
#33902=CARTESIAN_POINT('Ctrl Pts',(-0.145819277598255,0.0149687147614827,
0.158120463990349));
#33903=CARTESIAN_POINT('Ctrl Pts',(-0.1463265762883,0.0100268124462353,
0.158391807798802));
#33904=CARTESIAN_POINT('Ctrl Pts',(-0.146558040382541,0.0050565950257616,
0.158663151607255));
#33905=CARTESIAN_POINT('Ctrl Pts',(-0.146524127737672,8.31850724179233E-5,
0.158934495415709));
#33906=CARTESIAN_POINT('Origin',(0.,0.,0.));
#33907=CARTESIAN_POINT('',(-0.146129957599089,4.76874783713124E-5,0.21606550458429));
#33908=CARTESIAN_POINT('',(-0.146134590291164,5.53529746073057E-5,0.208934495415709));
#33909=CARTESIAN_POINT('',(-0.14635,-1.79227059055215E-17,0.));
#33910=CARTESIAN_POINT('Ctrl Pts',(-0.146129957599089,4.76874783713124E-5,
0.21606550458429));
#33911=CARTESIAN_POINT('Ctrl Pts',(-0.146192738333019,0.0213155226117273,
0.214913123098095));
#33912=CARTESIAN_POINT('Ctrl Pts',(-0.14184845306411,0.0425589323614883,
0.213760741611899));
#33913=CARTESIAN_POINT('Ctrl Pts',(-0.132968065125987,0.0616975770053832,
0.212608360125703));
#33914=CARTESIAN_POINT('Ctrl Pts',(-0.11267474299563,0.105432905191852,
0.2099749561709));
#33915=CARTESIAN_POINT('Ctrl Pts',(-0.0686935897650435,0.13817700942041,
0.207341552216098));
#33916=CARTESIAN_POINT('Ctrl Pts',(-0.0209756858809845,0.145076248759314,
0.204708148261296));
#33917=CARTESIAN_POINT('Ctrl Pts',(0.0267422180030747,0.151975488098219,
0.202074744306494));
#33918=CARTESIAN_POINT('Ctrl Pts',(0.0781968725406062,0.13302986254747,
0.199441340351692));
#33919=CARTESIAN_POINT('Ctrl Pts',(0.110047008199114,0.0968336374273772,
0.196807936396889));
#33920=CARTESIAN_POINT('Ctrl Pts',(0.141897143857622,0.0606374123072843,
0.194174532442087));
#33921=CARTESIAN_POINT('Ctrl Pts',(0.154142760637107,0.00719058761784734,
0.191541128487285));
#33922=CARTESIAN_POINT('Ctrl Pts',(0.141228904479148,-0.0392618630629832,
0.188907724532483));
#33923=CARTESIAN_POINT('Ctrl Pts',(0.128315048321188,-0.0857143137438141,
0.18627432057768));
#33924=CARTESIAN_POINT('Ctrl Pts',(0.0902417192257834,-0.125172390416039,
0.183640916622878));
#33925=CARTESIAN_POINT('Ctrl Pts',(0.0442800434850501,-0.139736806546778,
0.181007512668076));
#33926=CARTESIAN_POINT('Ctrl Pts',(-0.00168163225568323,-0.154301222677517,
0.178374108713273));
#33927=CARTESIAN_POINT('Ctrl Pts',(-0.0555316546417454,-0.143971978266771,
0.175740704758471));
#33928=CARTESIAN_POINT('Ctrl Pts',(-0.0928421483413364,-0.113434707375038,
0.173107300803669));
#33929=CARTESIAN_POINT('Ctrl Pts',(-0.126098584749153,-0.0862155337115625,
0.17076003539721));
#33930=CARTESIAN_POINT('Ctrl Pts',(-0.146214500923306,-0.0429412483281845,
0.16841276999075));
#33931=CARTESIAN_POINT('Ctrl Pts',(-0.14651736545536,8.65668654492988E-5,
0.166065504584291));
#33932=CARTESIAN_POINT('Ctrl Pts',(-0.146524127737672,8.31850724179233E-5,
0.158934495415709));
#33933=CARTESIAN_POINT('Ctrl Pts',(-0.146228674526712,-0.043246078859919,
0.161298492673761));
#33934=CARTESIAN_POINT('Ctrl Pts',(-0.125790555024919,-0.0868176629158599,
0.163662489931814));
#33935=CARTESIAN_POINT('Ctrl Pts',(-0.0921252733308782,-0.11401867430555,
0.166026487189866));
#33936=CARTESIAN_POINT('Ctrl Pts',(-0.0545958307473115,-0.144341866145796,
0.168661828256372));
#33937=CARTESIAN_POINT('Ctrl Pts',(-0.000628485618429035,-0.154320718498276,
0.171297169322878));
#33938=CARTESIAN_POINT('Ctrl Pts',(0.0452626498105411,-0.139422439628514,
0.173932510389384));
#33939=CARTESIAN_POINT('Ctrl Pts',(0.0911537852395115,-0.124524160758753,
0.17656785145589));
#33940=CARTESIAN_POINT('Ctrl Pts',(0.128968710968569,-0.0847487506667484,
0.179203192522395));
#33941=CARTESIAN_POINT('Ctrl Pts',(0.141530385150016,-0.0381637812674535,
0.181838533588901));
#33942=CARTESIAN_POINT('Ctrl Pts',(0.154092059331463,0.00842118813184087,
0.184473874655407));
#33943=CARTESIAN_POINT('Ctrl Pts',(0.141400481965299,0.0618157168384256,
0.187109215721913));
#33944=CARTESIAN_POINT('Ctrl Pts',(0.109220671810841,0.0977658885483793,
0.189744556788419));
#33945=CARTESIAN_POINT('Ctrl Pts',(0.0770408616563825,0.133716060258333,
0.192379897854925));
#33946=CARTESIAN_POINT('Ctrl Pts',(0.025372818713629,0.152221874971656,
0.19501523892143));
#33947=CARTESIAN_POINT('Ctrl Pts',(-0.022313779030084,0.144877256285936,
0.197650579987936));
#33948=CARTESIAN_POINT('Ctrl Pts',(-0.0700003767737975,0.137532637600217,
0.200285921054442));
#33949=CARTESIAN_POINT('Ctrl Pts',(-0.113705529318471,0.104337585515455,
0.202921262120948));
#33950=CARTESIAN_POINT('Ctrl Pts',(-0.133576619842631,0.0603706116554267,
0.205556603187454));
#33951=CARTESIAN_POINT('Ctrl Pts',(-0.142066653397378,0.041585478402751,
0.206682567263539));
#33952=CARTESIAN_POINT('Ctrl Pts',(-0.146205843323087,0.0208339599326467,
0.207808531339624));
#33953=CARTESIAN_POINT('Ctrl Pts',(-0.146134590291164,5.53529746073057E-5,
0.208934495415709));
#33954=CARTESIAN_POINT('Origin',(0.,0.,0.));
#33955=CARTESIAN_POINT('',(-0.146348968946192,-0.000130334789587572,0.266065504584291));
#33956=CARTESIAN_POINT('',(-0.146327394052832,-0.000130859996972892,0.258934495415708));
#33957=CARTESIAN_POINT('',(-0.14635,-1.79227059055215E-17,0.));
#33958=CARTESIAN_POINT('Ctrl Pts',(-0.146348968946192,-0.000130334789587572,
0.266065504584291));
#33959=CARTESIAN_POINT('Ctrl Pts',(-0.146013620606683,0.0369836123692833,
0.264046880160242));
#33960=CARTESIAN_POINT('Ctrl Pts',(-0.131636768783893,0.074328824870482,
0.262028255736193));
#33961=CARTESIAN_POINT('Ctrl Pts',(-0.106148536005423,0.10109196632601,
0.260009631312144));
#33962=CARTESIAN_POINT('Ctrl Pts',(-0.072897767709896,0.136005921449249,
0.257376227357342));
#33963=CARTESIAN_POINT('Ctrl Pts',(-0.020736980756812,0.152910669462462,
0.254742823402539));
#33964=CARTESIAN_POINT('Ctrl Pts',(0.0266722339182632,0.144137744153214,
0.252109419447737));
#33965=CARTESIAN_POINT('Ctrl Pts',(0.0740814485933381,0.135364818843967,
0.249476015492935));
#33966=CARTESIAN_POINT('Ctrl Pts',(0.116739090990404,0.100914220212258,
0.246842611538132));
#33967=CARTESIAN_POINT('Ctrl Pts',(0.135294462171964,0.056413702744499,
0.24420920758333));
#33968=CARTESIAN_POINT('Ctrl Pts',(0.153849833353525,0.0119131852767396,
0.241575803628528));
#33969=CARTESIAN_POINT('Ctrl Pts',(0.148302933319579,-0.0426372510270706,
0.238942399673726));
#33970=CARTESIAN_POINT('Ctrl Pts',(0.121169990969772,-0.082492003492008,
0.236308995718923));
#33971=CARTESIAN_POINT('Ctrl Pts',(0.094037048619966,-0.122346755956945,
0.233675591764121));
#33972=CARTESIAN_POINT('Ctrl Pts',(0.0453180639542996,-0.14750582458301,
0.231042187809319));
#33973=CARTESIAN_POINT('Ctrl Pts',(-0.00288666981273841,-0.146556352606171,
0.228408783854516));
#33974=CARTESIAN_POINT('Ctrl Pts',(-0.0510914035797761,-0.145606880629331,
0.225775379899714));
#33975=CARTESIAN_POINT('Ctrl Pts',(-0.0987818864481854,-0.118548868049589,
0.223141975944912));
#33976=CARTESIAN_POINT('Ctrl Pts',(-0.124324382367327,-0.0776565856875276,
0.22050857199011));
#33977=CARTESIAN_POINT('Ctrl Pts',(-0.138689444093445,-0.0546588268893121,
0.219027549521503));
#33978=CARTESIAN_POINT('Ctrl Pts',(-0.146049272792313,-0.0272853980218952,
0.217546527052897));
#33979=CARTESIAN_POINT('Ctrl Pts',(-0.146129957599089,4.76874783713124E-5,
0.21606550458429));
#33980=CARTESIAN_POINT('Ctrl Pts',(-0.146134590291164,5.53529746073057E-5,
0.208934495415709));
#33981=CARTESIAN_POINT('Ctrl Pts',(-0.146039074200404,-0.0277987783441389,
0.210443872406129));
#33982=CARTESIAN_POINT('Ctrl Pts',(-0.138377421661147,-0.055701587485614,
0.21195324939655));
#33983=CARTESIAN_POINT('Ctrl Pts',(-0.123487844473835,-0.0789814939515912,
0.213462626386971));
#33984=CARTESIAN_POINT('Ctrl Pts',(-0.0974909500772326,-0.119627730063286,
0.216097967453477));
#33985=CARTESIAN_POINT('Ctrl Pts',(-0.0494601327803805,-0.146181306651382,
0.218733308519983));
#33986=CARTESIAN_POINT('Ctrl Pts',(-0.00121289818784218,-0.14658053417448,
0.221368649586488));
#33987=CARTESIAN_POINT('Ctrl Pts',(0.047034336404696,-0.146979761697578,
0.224003990652994));
#33988=CARTESIAN_POINT('Ctrl Pts',(0.0954979882929203,-0.121224640155678,
0.2266393317195));
#33989=CARTESIAN_POINT('Ctrl Pts',(0.122163941197393,-0.0810141690783142,
0.229274672786006));
#33990=CARTESIAN_POINT('Ctrl Pts',(0.148829894101866,-0.0408036980009502,
0.231910013852512));
#33991=CARTESIAN_POINT('Ctrl Pts',(0.153698148022588,0.0138621226118777,
0.234545354919018));
#33992=CARTESIAN_POINT('Ctrl Pts',(0.134557348601142,0.0581519050223658,
0.237180695985524));
#33993=CARTESIAN_POINT('Ctrl Pts',(0.115416549179696,0.102441687432854,
0.239816037052029));
#33994=CARTESIAN_POINT('Ctrl Pts',(0.0722666964160822,0.136355431641002,
0.242451378118535));
#33995=CARTESIAN_POINT('Ctrl Pts',(0.0247081678934101,0.144488167542617,
0.245086719185041));
#33996=CARTESIAN_POINT('Ctrl Pts',(-0.0228503606292616,0.152620903444231,
0.247722060251547));
#33997=CARTESIAN_POINT('Ctrl Pts',(-0.0748175649109913,0.134972631039312,
0.250357401318053));
#33998=CARTESIAN_POINT('Ctrl Pts',(-0.107587875971466,0.0995598968678148,
0.252992742384558));
#33999=CARTESIAN_POINT('Ctrl Pts',(-0.132216325719399,0.072945540282363,
0.254973326728275));
#34000=CARTESIAN_POINT('Ctrl Pts',(-0.146001912399175,0.0362973920726889,
0.256953911071992));
#34001=CARTESIAN_POINT('Ctrl Pts',(-0.146327394052832,-0.000130859996972892,
0.258934495415708));
#34002=CARTESIAN_POINT('Origin',(0.,0.,0.));
#34003=CARTESIAN_POINT('',(-0.146531331768327,7.78185235384022E-5,0.316065504584291));
#34004=CARTESIAN_POINT('',(-0.146550416329645,6.385150607816E-5,0.308934495415709));
#34005=CARTESIAN_POINT('',(-0.14635,-1.79227059055215E-17,0.));
#34006=CARTESIAN_POINT('Ctrl Pts',(-0.146531331768327,7.78185235384022E-5,
0.316065504584291));
#34007=CARTESIAN_POINT('Ctrl Pts',(-0.14656115307709,0.00468624689283061,
0.315814041177191));
#34008=CARTESIAN_POINT('Ctrl Pts',(-0.14636239679671,0.00929207042467623,
0.315562577770091));
#34009=CARTESIAN_POINT('Ctrl Pts',(-0.145926597573945,0.0138753548512781,
0.315311114362991));
#34010=CARTESIAN_POINT('Ctrl Pts',(-0.14136277093227,0.0618729520929492,
0.312677710408189));
#34011=CARTESIAN_POINT('Ctrl Pts',(-0.110802592512226,0.10739869970775,
0.310044306453387));
#34012=CARTESIAN_POINT('Ctrl Pts',(-0.0681090134487845,0.12980084606346,
0.307410902498584));
#34013=CARTESIAN_POINT('Ctrl Pts',(-0.0254154343853437,0.152202992419171,
0.304777498543782));
#34014=CARTESIAN_POINT('Ctrl Pts',(0.0294115453214934,0.151481537515791,
0.30214409458898));
#34015=CARTESIAN_POINT('Ctrl Pts',(0.0715008751789212,0.127963753463258,
0.299510690634177));
#34016=CARTESIAN_POINT('Ctrl Pts',(0.113590205036349,0.104445969410725,
0.296877286679375));
#34017=CARTESIAN_POINT('Ctrl Pts',(0.142941885044368,0.0581318562090376,
0.294243882724573));
#34018=CARTESIAN_POINT('Ctrl Pts',(0.146241172727074,0.0100307901566561,
0.291610478769771));
#34019=CARTESIAN_POINT('Ctrl Pts',(0.149540460409781,-0.038070275895725,
0.288977074814969));
#34020=CARTESIAN_POINT('Ctrl Pts',(0.126787355767176,-0.0879582947988004,
0.286343670860166));
#34021=CARTESIAN_POINT('Ctrl Pts',(0.0883033030491544,-0.117002666731855,
0.283710266905364));
#34022=CARTESIAN_POINT('Ctrl Pts',(0.0498192503311324,-0.14604703866491,
0.281076862950562));
#34023=CARTESIAN_POINT('Ctrl Pts',(-0.00439575046230666,-0.154247763627944,
0.27844345899576));
#34024=CARTESIAN_POINT('Ctrl Pts',(-0.0497482595792165,-0.137884763554925,
0.275810055040957));
#34025=CARTESIAN_POINT('Ctrl Pts',(-0.0951007686961262,-0.121521763481905,
0.273176651086155));
#34026=CARTESIAN_POINT('Ctrl Pts',(-0.131590786136507,-0.0805950383728307,
0.270543247131353));
#34027=CARTESIAN_POINT('Ctrl Pts',(-0.142665420037712,-0.0336700947016615,
0.26790984317655));
#34028=CARTESIAN_POINT('Ctrl Pts',(-0.145250841169412,-0.0227152638644948,
0.267295063645797));
#34029=CARTESIAN_POINT('Ctrl Pts',(-0.146451100522698,-0.0114335245988962,
0.266680284115044));
#34030=CARTESIAN_POINT('Ctrl Pts',(-0.146348968946192,-0.000130334789587572,
0.266065504584291));
#34031=CARTESIAN_POINT('Ctrl Pts',(-0.146327394052832,-0.000130859996972892,
0.258934495415708));
#34032=CARTESIAN_POINT('Ctrl Pts',(-0.146434994267663,-0.0121735902233998,
0.259589252138497));
#34033=CARTESIAN_POINT('Ctrl Pts',(-0.145071563913279,-0.0241922883978194,
0.260244008861286));
#34034=CARTESIAN_POINT('Ctrl Pts',(-0.142142543798705,-0.0358164956803284,
0.260898765584076));
#34035=CARTESIAN_POINT('Ctrl Pts',(-0.130353482726251,-0.0826029581188991,
0.263534106650581));
#34036=CARTESIAN_POINT('Ctrl Pts',(-0.0932019427421253,-0.122998687057965,
0.266169447717088));
#34037=CARTESIAN_POINT('Ctrl Pts',(-0.0475636294365445,-0.138654337383406,
0.268804788783593));
#34038=CARTESIAN_POINT('Ctrl Pts',(-0.00192531613096394,-0.154309987708848,
0.271440129850099));
#34039=CARTESIAN_POINT('Ctrl Pts',(0.0521997704960722,-0.145225559420664,
0.274075470916605));
#34040=CARTESIAN_POINT('Ctrl Pts',(0.090225865564854,-0.115527560795972,
0.27671081198311));
#34041=CARTESIAN_POINT('Ctrl Pts',(0.128251960633635,-0.0858295621712801,
0.279346153049616));
#34042=CARTESIAN_POINT('Ctrl Pts',(0.150179064144164,-0.0355179932100797,
0.281981494116122));
#34043=CARTESIAN_POINT('Ctrl Pts',(0.14604701445983,0.0125536324530514,
0.284616835182628));
#34044=CARTESIAN_POINT('Ctrl Pts',(0.141914964775496,0.0606252581161832,
0.287252176249134));
#34045=CARTESIAN_POINT('Ctrl Pts',(0.1117237618963,0.106456940481245,0.28988751731564));
#34046=CARTESIAN_POINT('Ctrl Pts',(0.0691874497467596,0.129230108403338,
0.292522858382145));
#34047=CARTESIAN_POINT('Ctrl Pts',(0.02665113759722,0.152003276325431,0.295158199448651));
#34048=CARTESIAN_POINT('Ctrl Pts',(-0.0282302838226635,0.151717929804555,
0.297793540515157));
#34049=CARTESIAN_POINT('Ctrl Pts',(-0.0705274923191129,0.128503684568086,
0.300428881581663));
#34050=CARTESIAN_POINT('Ctrl Pts',(-0.112824700815562,0.105289439331617,
0.303064222648169));
#34051=CARTESIAN_POINT('Ctrl Pts',(-0.142537696388578,0.0591462953795561,
0.305699563714675));
#34052=CARTESIAN_POINT('Ctrl Pts',(-0.146169655872548,0.0110343020847702,
0.30833490478118));
#34053=CARTESIAN_POINT('Ctrl Pts',(-0.146445102685266,0.00738550168790281,
0.308534768326023));
#34054=CARTESIAN_POINT('Ctrl Pts',(-0.146570540139926,0.00372537713102106,
0.308734631870866));
#34055=CARTESIAN_POINT('Ctrl Pts',(-0.146550416329645,6.385150607816E-5,
0.308934495415709));
#34056=CARTESIAN_POINT('Origin',(0.,0.,0.));
#34057=CARTESIAN_POINT('',(-0.146136883584905,5.71367125724795E-5,0.366065504584291));
#34058=CARTESIAN_POINT('',(-0.14615227160514,7.39083677616704E-5,0.358934495415709));
#34059=CARTESIAN_POINT('',(-0.14635,-1.79227059055215E-17,0.));
#34060=CARTESIAN_POINT('Ctrl Pts',(-0.146136883584905,5.71367125724795E-5,
0.366065504584291));
#34061=CARTESIAN_POINT('Ctrl Pts',(-0.14621004407594,0.0206825763459024,
0.364947798239338));
#34062=CARTESIAN_POINT('Ctrl Pts',(-0.142132997319362,0.0412803999606639,
0.363830091894385));
#34063=CARTESIAN_POINT('Ctrl Pts',(-0.133763205647759,0.0599541672162359,
0.362712385549432));
#34064=CARTESIAN_POINT('Ctrl Pts',(-0.114043318945497,0.10395102986619,
0.360078981594629));
#34065=CARTESIAN_POINT('Ctrl Pts',(-0.070493949429046,0.137267251375705,
0.357445577639827));
#34066=CARTESIAN_POINT('Ctrl Pts',(-0.0228703083824292,0.144789662428813,
0.354812173685025));
#34067=CARTESIAN_POINT('Ctrl Pts',(0.0247533326641879,0.15231207348192,
0.352178769730223));
#34068=CARTESIAN_POINT('Ctrl Pts',(0.0764512452409704,0.13404067407862,
0.34954536577542));
#34069=CARTESIAN_POINT('Ctrl Pts',(0.108771811167509,0.0982638817017563,
0.346911961820618));
#34070=CARTESIAN_POINT('Ctrl Pts',(0.141092377094047,0.0624870893248929,
0.344278557865816));
#34071=CARTESIAN_POINT('Ctrl Pts',(0.154035596370341,0.00920490397446603,
0.341645153911014));
#34072=CARTESIAN_POINT('Ctrl Pts',(0.141730062949927,-0.0374123857561472,
0.339011749956212));
#34073=CARTESIAN_POINT('Ctrl Pts',(0.129424529529512,-0.0840296754867619,
0.336378346001409));
#34074=CARTESIAN_POINT('Ctrl Pts',(0.0918702434123863,-0.123982069597563,
0.333744942046607));
#34075=CARTESIAN_POINT('Ctrl Pts',(0.0461028784809079,-0.139146045389481,
0.331111538091804));
#34076=CARTESIAN_POINT('Ctrl Pts',(0.000335513549430837,-0.154310021181399,
0.328478134137002));
#34077=CARTESIAN_POINT('Ctrl Pts',(-0.0536449301963988,-0.144685578654437,
0.3258447301822));
#34078=CARTESIAN_POINT('Ctrl Pts',(-0.0913514146376612,-0.114638633956686,
0.323211326227398));
#34079=CARTESIAN_POINT('Ctrl Pts',(-0.125457311698448,-0.0874608681681781,
0.320829385679696));
#34080=CARTESIAN_POINT('Ctrl Pts',(-0.146248854944573,-0.043574665631504,
0.318447445131993));
#34081=CARTESIAN_POINT('Ctrl Pts',(-0.146531331768327,7.78185235384022E-5,
0.316065504584291));
#34082=CARTESIAN_POINT('Ctrl Pts',(-0.146550416329645,6.385150607816E-5,
0.308934495415709));
#34083=CARTESIAN_POINT('Ctrl Pts',(-0.146305193582165,-0.0445544072241828,
0.311369972937372));
#34084=CARTESIAN_POINT('Ctrl Pts',(-0.1244453858937,-0.0893807124057277,
0.313805450459035));
#34085=CARTESIAN_POINT('Ctrl Pts',(-0.0890196886128741,-0.116459517256704,
0.316240927980698));
#34086=CARTESIAN_POINT('Ctrl Pts',(-0.0506868384743053,-0.145760500665881,
0.318876269047204));
#34087=CARTESIAN_POINT('Ctrl Pts',(0.00352978519775653,-0.154281624846726,
0.321511610113709));
#34088=CARTESIAN_POINT('Ctrl Pts',(0.0490028377607838,-0.138152256629371,
0.324146951180215));
#34089=CARTESIAN_POINT('Ctrl Pts',(0.0944758903238113,-0.122022888412016,
0.326782292246721));
#34090=CARTESIAN_POINT('Ctrl Pts',(0.131205371777804,-0.0812430277964604,
0.329417633313227));
#34091=CARTESIAN_POINT('Ctrl Pts',(0.142507292286359,-0.034336507766627,
0.332052974379733));
#34092=CARTESIAN_POINT('Ctrl Pts',(0.153809212794913,0.0125700122632054,
0.334688315446239));
#34093=CARTESIAN_POINT('Ctrl Pts',(0.139683572358031,0.0656031917073164,
0.337323656512744));
#34094=CARTESIAN_POINT('Ctrl Pts',(0.106546798111412,0.1006732533129,0.33995899757925));
#34095=CARTESIAN_POINT('Ctrl Pts',(0.0734100238647925,0.135743314918485,
0.342594338645756));
#34096=CARTESIAN_POINT('Ctrl Pts',(0.0212621158084357,0.152850258685541,
0.345229679712262));
#34097=CARTESIAN_POINT('Ctrl Pts',(-0.026209274243358,0.144223431050692,
0.347865020778768));
#34098=CARTESIAN_POINT('Ctrl Pts',(-0.0736806642951504,0.135596603415843,
0.350500361845274));
#34099=CARTESIAN_POINT('Ctrl Pts',(-0.11647553634238,0.10123600437909,0.353135702911779));
#34100=CARTESIAN_POINT('Ctrl Pts',(-0.135154759147093,0.056749583260925,
0.355771043978285));
#34101=CARTESIAN_POINT('Ctrl Pts',(-0.142628910530197,0.0389491506944377,
0.356825527790759));
#34102=CARTESIAN_POINT('Ctrl Pts',(-0.146242014510603,0.0195275186049996,
0.357880011603234));
#34103=CARTESIAN_POINT('Ctrl Pts',(-0.14615227160514,7.39083677616704E-5,
0.358934495415709));
#34104=CARTESIAN_POINT('Origin',(0.,0.,0.));
#34105=CARTESIAN_POINT('',(-0.146330070388523,-0.000130413829425732,0.416065504584291));
#34106=CARTESIAN_POINT('',(-0.146289342453438,-0.000128032530387096,0.408934495415709));
#34107=CARTESIAN_POINT('',(-0.14635,-1.79227059055215E-17,0.));
#34108=CARTESIAN_POINT('Ctrl Pts',(-0.146330070388523,-0.000130413829425732,
0.416065504584291));
#34109=CARTESIAN_POINT('Ctrl Pts',(-0.146004163689088,0.0363580550473478,
0.414081555301485));
#34110=CARTESIAN_POINT('Ctrl Pts',(-0.13216535679172,0.0730671490760677,
0.412097606018678));
#34111=CARTESIAN_POINT('Ctrl Pts',(-0.107460925463154,0.0996957714768259,
0.410113656735872));
#34112=CARTESIAN_POINT('Ctrl Pts',(-0.0746693880354573,0.135041392531165,
0.40748025278107));
#34113=CARTESIAN_POINT('Ctrl Pts',(-0.0227340340094623,0.152626534075836,
0.404846848826268));
#34114=CARTESIAN_POINT('Ctrl Pts',(0.0247858083562081,0.144474084374625,
0.402213444871466));
#34115=CARTESIAN_POINT('Ctrl Pts',(0.0723056507218785,0.136321634673413,
0.399580040916663));
#34116=CARTESIAN_POINT('Ctrl Pts',(0.115409981427224,0.102431593726319,
0.396946636961861));
#34117=CARTESIAN_POINT('Ctrl Pts',(0.134545471232452,0.0581774313853258,
0.394313233007059));
#34118=CARTESIAN_POINT('Ctrl Pts',(0.15368096103768,0.0139232690443328,
0.391679829052256));
#34119=CARTESIAN_POINT('Ctrl Pts',(0.14884760994279,-0.0406950146905586,
0.389046425097455));
#34120=CARTESIAN_POINT('Ctrl Pts',(0.122237961103967,-0.0809010396527884,
0.386413021142652));
#34121=CARTESIAN_POINT('Ctrl Pts',(0.0956283122651433,-0.121107064615018,
0.38377961718785));
#34122=CARTESIAN_POINT('Ctrl Pts',(0.0472423656823864,-0.146900830804586,
0.381146213233048));
#34123=CARTESIAN_POINT('Ctrl Pts',(-0.000970660813290544,-0.146581564902762,
0.378512809278245));
#34124=CARTESIAN_POINT('Ctrl Pts',(-0.0491836873089679,-0.146262299000937,
0.375879405323443));
#34125=CARTESIAN_POINT('Ctrl Pts',(-0.0972237937175652,-0.11983000100772,
0.373246001368641));
#34126=CARTESIAN_POINT('Ctrl Pts',(-0.123298644977828,-0.0792751001159155,
0.370612597413839));
#34127=CARTESIAN_POINT('Ctrl Pts',(-0.138306441127099,-0.0559330806595814,
0.369096899803989));
#34128=CARTESIAN_POINT('Ctrl Pts',(-0.146037672211633,-0.0279125797478292,
0.36758120219414));
#34129=CARTESIAN_POINT('Ctrl Pts',(-0.146136883584905,5.71367125724795E-5,
0.366065504584291));
#34130=CARTESIAN_POINT('Ctrl Pts',(-0.14615227160514,7.39083677616704E-5,
0.358934495415709));
#34131=CARTESIAN_POINT('Ctrl Pts',(-0.146017731158506,-0.0290904851457483,
0.36051535266974));
#34132=CARTESIAN_POINT('Ctrl Pts',(-0.137560931614845,-0.0583267505026361,
0.362096209923772));
#34133=CARTESIAN_POINT('Ctrl Pts',(-0.121314920725415,-0.0822800955868649,
0.363677067177803));
#34134=CARTESIAN_POINT('Ctrl Pts',(-0.0942322859368278,-0.122211110116912,
0.366312408244309));
#34135=CARTESIAN_POINT('Ctrl Pts',(-0.0455034427974572,-0.147460895977431,
0.368947749310814));
#34136=CARTESIAN_POINT('Ctrl Pts',(0.00273703201223555,-0.146559997189415,
0.37158309037732));
#34137=CARTESIAN_POINT('Ctrl Pts',(0.050977506821928,-0.145659098401399,
0.374218431443826));
#34138=CARTESIAN_POINT('Ctrl Pts',(0.0987296133019425,-0.11860751496485,
0.376853772510332));
#34139=CARTESIAN_POINT('Ctrl Pts',(0.124302447370845,-0.0776931509080149,
0.379489113576838));
#34140=CARTESIAN_POINT('Ctrl Pts',(0.149875281439748,-0.0367787868511801,
0.382124454643343));
#34141=CARTESIAN_POINT('Ctrl Pts',(0.153268843097537,0.0179983578259404,
0.384759795709849));
#34142=CARTESIAN_POINT('Ctrl Pts',(0.132941641804014,0.0617563275693305,
0.387395136776355));
#34143=CARTESIAN_POINT('Ctrl Pts',(0.112614440510491,0.10551429731272,0.39003047784286));
#34144=CARTESIAN_POINT('Ctrl Pts',(0.0685664762656556,0.13825309212238,
0.392665818909367));
#34145=CARTESIAN_POINT('Ctrl Pts',(0.0208060845723004,0.145101450596359,
0.395301159975872));
#34146=CARTESIAN_POINT('Ctrl Pts',(-0.0269543071210555,0.151949809070337,
0.397936501042378));
#34147=CARTESIAN_POINT('Ctrl Pts',(-0.0784271262629304,0.132907731208634,
0.400571842108884));
#34148=CARTESIAN_POINT('Ctrl Pts',(-0.110231373247062,0.0966248853684404,
0.40320718317539));
#34149=CARTESIAN_POINT('Ctrl Pts',(-0.133271130208243,0.0703407243117375,
0.405116287255496));
#34150=CARTESIAN_POINT('Ctrl Pts',(-0.145989017153952,0.0350087805988431,
0.407025391335602));
#34151=CARTESIAN_POINT('Ctrl Pts',(-0.146289342453438,-0.000128032530387096,
0.408934495415709));
#34152=CARTESIAN_POINT('Origin',(0.,0.,0.));
#34153=CARTESIAN_POINT('',(-0.146544022497492,6.84377374728824E-5,0.466065504584291));
#34154=CARTESIAN_POINT('',(-0.146570300119817,4.22437972465385E-5,0.458934495415709));
#34155=CARTESIAN_POINT('',(-0.14635,-1.79227059055215E-17,0.));
#34156=CARTESIAN_POINT('Ctrl Pts',(-0.146544022497492,6.84377374728824E-5,
0.466065504584291));
#34157=CARTESIAN_POINT('Ctrl Pts',(-0.146567170791634,0.00404048499144927,
0.465848716318434));
#34158=CARTESIAN_POINT('Ctrl Pts',(-0.146419528859516,0.00801078566506452,
0.465631928052577));
#34159=CARTESIAN_POINT('Ctrl Pts',(-0.146095506097533,0.0119666390378655,
0.46541513978672));
#34160=CARTESIAN_POINT('Ctrl Pts',(-0.142159486684863,0.0600197930006592,
0.462781735831918));
#34161=CARTESIAN_POINT('Ctrl Pts',(-0.112197024986195,0.105941128890497,
0.460148331877115));
#34162=CARTESIAN_POINT('Ctrl Pts',(-0.0697999311245908,0.128899445176305,
0.457514927922313));
#34163=CARTESIAN_POINT('Ctrl Pts',(-0.0274028372629858,0.151857761462114,
0.454881523967511));
#34164=CARTESIAN_POINT('Ctrl Pts',(0.0274288887615551,0.151853058143892,
0.452248120012709));
#34165=CARTESIAN_POINT('Ctrl Pts',(0.0698220433938502,0.12888746877825,
0.449614716057906));
#34166=CARTESIAN_POINT('Ctrl Pts',(0.112215198026145,0.105921879412608,
0.446981312103104));
#34167=CARTESIAN_POINT('Ctrl Pts',(0.142169781266193,0.0599954039995453,
0.444347908148302));
#34168=CARTESIAN_POINT('Ctrl Pts',(0.146097556879977,0.0119415755015296,
0.441714504193499));
#34169=CARTESIAN_POINT('Ctrl Pts',(0.150025332493762,-0.036112252996486,
0.439081100238697));
#34170=CARTESIAN_POINT('Ctrl Pts',(0.127926300481281,-0.0862934345794555,
0.436447696283895));
#34171=CARTESIAN_POINT('Ctrl Pts',(0.0898251994650805,-0.11583838264071,
0.433814292329093));
#34172=CARTESIAN_POINT('Ctrl Pts',(0.0517240984488793,-0.145383330701964,
0.431180888374291));
#34173=CARTESIAN_POINT('Ctrl Pts',(-0.00237907157104229,-0.154292045241502,
0.428547484419488));
#34174=CARTESIAN_POINT('Ctrl Pts',(-0.0479416004074503,-0.138523284332019,
0.425914080464686));
#34175=CARTESIAN_POINT('Ctrl Pts',(-0.0935041292438574,-0.122754523422536,
0.423280676509884));
#34176=CARTESIAN_POINT('Ctrl Pts',(-0.130526016896751,-0.0823082870640309,
0.420647272555081));
#34177=CARTESIAN_POINT('Ctrl Pts',(-0.142213100308499,-0.0355321186027758,
0.418013868600279));
#34178=CARTESIAN_POINT('Ctrl Pts',(-0.145095389184054,-0.0239960984301615,
0.417364413928283));
#34179=CARTESIAN_POINT('Ctrl Pts',(-0.146436757404375,-0.0120750773303437,
0.416714959256287));
#34180=CARTESIAN_POINT('Ctrl Pts',(-0.146330070388523,-0.000130413829425732,
0.416065504584291));
#34181=CARTESIAN_POINT('Ctrl Pts',(-0.146289342453438,-0.000128032530387096,
0.408934495415709));
#34182=CARTESIAN_POINT('Ctrl Pts',(-0.146403588367378,-0.0134943301275472,
0.409660732402108));
#34183=CARTESIAN_POINT('Ctrl Pts',(-0.144720893191604,-0.0268323904448261,
0.410386969388508));
#34184=CARTESIAN_POINT('Ctrl Pts',(-0.141125892037436,-0.0396334040556115,
0.411113206374907));
#34185=CARTESIAN_POINT('Ctrl Pts',(-0.128080489017291,-0.0860852338207874,
0.413748547441413));
#34186=CARTESIAN_POINT('Ctrl Pts',(-0.0898540081506159,-0.125465279532456,
0.416383888507919));
#34187=CARTESIAN_POINT('Ctrl Pts',(-0.0438104358868217,-0.139885559754408,
0.419019229574425));
#34188=CARTESIAN_POINT('Ctrl Pts',(0.00223313637697255,-0.15430583997636,
0.42165457064093));
#34189=CARTESIAN_POINT('Ctrl Pts',(0.0560938000378854,-0.143766354708596,
0.424289911707436));
#34190=CARTESIAN_POINT('Ctrl Pts',(0.0933059016336915,-0.11305455692152,
0.426925252773942));
#34191=CARTESIAN_POINT('Ctrl Pts',(0.130518003229497,-0.082342759134444,
0.429560593840448));
#34192=CARTESIAN_POINT('Ctrl Pts',(0.151081542760197,-0.0314586488280562,
0.432195934906954));
#34193=CARTESIAN_POINT('Ctrl Pts',(0.145655743526821,0.0164841893354265,
0.434831275973459));
#34194=CARTESIAN_POINT('Ctrl Pts',(0.140229944293446,0.06442702749891,0.437466617039965));
#34195=CARTESIAN_POINT('Ctrl Pts',(0.108814806295994,0.109428593519488,
0.440101958106471));
#34196=CARTESIAN_POINT('Ctrl Pts',(0.0656803334199076,0.131047388078691,
0.442737299172977));
#34197=CARTESIAN_POINT('Ctrl Pts',(0.022545860543821,0.152666182637894,
0.445372640239483));
#34198=CARTESIAN_POINT('Ctrl Pts',(-0.032307947210901,0.150902205735721,
0.448007981305989));
#34199=CARTESIAN_POINT('Ctrl Pts',(-0.0739643108743681,0.126556725768634,
0.450643322372494));
#34200=CARTESIAN_POINT('Ctrl Pts',(-0.115620674537836,0.102211245801546,
0.453278663439));
#34201=CARTESIAN_POINT('Ctrl Pts',(-0.144079594110048,0.0552842627695439,
0.455914004505506));
#34202=CARTESIAN_POINT('Ctrl Pts',(-0.14641389757273,0.0070918768996262,
0.458549345572012));
#34203=CARTESIAN_POINT('Ctrl Pts',(-0.146527615505388,0.00474413652285832,
0.458677728853244));
#34204=CARTESIAN_POINT('Ctrl Pts',(-0.146579333222338,0.00239339303023303,
0.458806112134477));
#34205=CARTESIAN_POINT('Ctrl Pts',(-0.146570300119817,4.22437972465385E-5,
0.458934495415709));
#34206=CARTESIAN_POINT('Origin',(0.,0.,0.));
#34207=CARTESIAN_POINT('',(-0.146145057762853,6.62388175271394E-5,0.516065504584291));
#34208=CARTESIAN_POINT('',(-0.146174937959923,9.05479403153491E-5,0.508934495415709));
#34209=CARTESIAN_POINT('',(-0.14635,-1.79227059055215E-17,0.));
#34210=CARTESIAN_POINT('Ctrl Pts',(-0.146145057762853,6.62388175271395E-5,
0.516065504584291));
#34211=CARTESIAN_POINT('Ctrl Pts',(-0.146227515408595,0.0200490060336265,
0.514982473380581));
#34212=CARTESIAN_POINT('Ctrl Pts',(-0.142408399519226,0.0400016020167204,
0.513899442176871));
#34213=CARTESIAN_POINT('Ctrl Pts',(-0.134535488644935,0.0582005124275171,
0.512816410973161));
#34214=CARTESIAN_POINT('Ctrl Pts',(-0.115392407114926,0.102451391335448,
0.510183007018359));
#34215=CARTESIAN_POINT('Ctrl Pts',(-0.0722822630505052,0.136334037036404,
0.507549603063556));
#34216=CARTESIAN_POINT('Ctrl Pts',(-0.0247610227936349,0.144478334368756,
0.504916199108754));
#34217=CARTESIAN_POINT('Ctrl Pts',(0.0227602174632348,0.152622631701108,
0.502282795153951));
#34218=CARTESIAN_POINT('Ctrl Pts',(0.0746925539125539,0.135028580664858,
0.49964939119915));
#34219=CARTESIAN_POINT('Ctrl Pts',(0.107478027152826,0.0996773345906346,
0.497015987244347));
#34220=CARTESIAN_POINT('Ctrl Pts',(0.140263500393099,0.06432608851641,0.494382583289545));
#34221=CARTESIAN_POINT('Ctrl Pts',(0.153902110424324,0.0112176474042102,
0.491749179334742));
#34222=CARTESIAN_POINT('Ctrl Pts',(0.142207002516364,-0.0355565153954619,
0.48911577537994));
#34223=CARTESIAN_POINT('Ctrl Pts',(0.130511894608405,-0.0823306781951331,
0.486482371425138));
#34224=CARTESIAN_POINT('Ctrl Pts',(0.0934830687612624,-0.122770562682277,
0.483848967470336));
#34225=CARTESIAN_POINT('Ctrl Pts',(0.0479178353914133,-0.138531506897017,
0.481215563515534));
#34226=CARTESIAN_POINT('Ctrl Pts',(0.00235260202156486,-0.154292451111757,
0.478582159560731));
#34227=CARTESIAN_POINT('Ctrl Pts',(-0.0517490388709899,-0.145374455054093,
0.475948755605929));
#34228=CARTESIAN_POINT('Ctrl Pts',(-0.0898450707539318,-0.115822971007387,
0.473315351651126));
#34229=CARTESIAN_POINT('Ctrl Pts',(-0.124804943950367,-0.0887042375336795,
0.470898735962181));
#34230=CARTESIAN_POINT('Ctrl Pts',(-0.146285980252562,-0.044209381789552,
0.468482120273236));
#34231=CARTESIAN_POINT('Ctrl Pts',(-0.146544022497492,6.84377374728824E-5,
0.466065504584291));
#34232=CARTESIAN_POINT('Ctrl Pts',(-0.146570300119817,4.22437972465385E-5,
0.458934495415709));
#34233=CARTESIAN_POINT('Ctrl Pts',(-0.14639390949893,-0.0458689668946884,
0.461441453200982));
#34234=CARTESIAN_POINT('Ctrl Pts',(-0.123052682342738,-0.0919348900534666,
0.463948410986256));
#34235=CARTESIAN_POINT('Ctrl Pts',(-0.0858494648887911,-0.118815796503266,
0.466455368771529));
#34236=CARTESIAN_POINT('Ctrl Pts',(-0.0467410413890165,-0.147073295328412,
0.469090709838035));
#34237=CARTESIAN_POINT('Ctrl Pts',(0.00768549296368549,-0.154130504270872,
0.471726050904541));
#34238=CARTESIAN_POINT('Ctrl Pts',(0.0527074437553312,-0.136781758627296,
0.474361391971047));
#34239=CARTESIAN_POINT('Ctrl Pts',(0.0977293945469769,-0.11943301298372,
0.476996733037553));
#34240=CARTESIAN_POINT('Ctrl Pts',(0.133346761777566,-0.0776783127541087,
0.479632074104058));
#34241=CARTESIAN_POINT('Ctrl Pts',(0.143380722078222,-0.0304843018080604,
0.482267415170564));
#34242=CARTESIAN_POINT('Ctrl Pts',(0.153414682378878,0.0167097091379873,
0.48490275623707));
#34243=CARTESIAN_POINT('Ctrl Pts',(0.137865235749601,0.0693430308004717,
0.487538097303576));
#34244=CARTESIAN_POINT('Ctrl Pts',(0.103795558670285,0.103507517218417,
0.490173438370082));
#34245=CARTESIAN_POINT('Ctrl Pts',(0.0697258815909678,0.137672003636362,
0.492808779436588));
#34246=CARTESIAN_POINT('Ctrl Pts',(0.0171359740616113,0.153367654809767,
0.495444120503093));
#34247=CARTESIAN_POINT('Ctrl Pts',(-0.0300857383810333,0.143464882345699,
0.498079461569599));
#34248=CARTESIAN_POINT('Ctrl Pts',(-0.0773074508236773,0.133562109881631,
0.500714802636104));
#34249=CARTESIAN_POINT('Ctrl Pts',(-0.11916096817961,0.09806091378009,0.503350143702611));
#34250=CARTESIAN_POINT('Ctrl Pts',(-0.136634759914189,0.0530873478673518,
0.505985484769117));
#34251=CARTESIAN_POINT('Ctrl Pts',(-0.143152625668081,0.0363118437555022,
0.506968488317981));
#34252=CARTESIAN_POINT('Ctrl Pts',(-0.146278417362408,0.0182184011065993,
0.507951491866845));
#34253=CARTESIAN_POINT('Ctrl Pts',(-0.146174937959923,9.05479403153491E-5,
0.508934495415709));
#34254=CARTESIAN_POINT('Origin',(0.,0.,0.));
#34255=CARTESIAN_POINT('',(-0.146311419053965,-0.000129619860865307,0.566065504584291));
#34256=CARTESIAN_POINT('',(-0.146253314944083,-0.00012165943743628,0.558934495415709));
#34257=CARTESIAN_POINT('',(-0.14635,-1.79227059055215E-17,0.));
#34258=CARTESIAN_POINT('Ctrl Pts',(-0.146311419053965,-0.000129619860865307,
0.566065504584291));
#34259=CARTESIAN_POINT('Ctrl Pts',(-0.145996667082224,0.0357327735863427,
0.564116230442728));
#34260=CARTESIAN_POINT('Ctrl Pts',(-0.132683527872108,0.0718042758553121,
0.562166956301165));
#34261=CARTESIAN_POINT('Ctrl Pts',(-0.10875495194318,0.0982825405633859,
0.560217682159602));
#34262=CARTESIAN_POINT('Ctrl Pts',(-0.0764282488179375,0.134053787671104,
0.557584278204799));
#34263=CARTESIAN_POINT('Ctrl Pts',(-0.0247272024587828,0.152316317789357,
0.554950874249997));
#34264=CARTESIAN_POINT('Ctrl Pts',(0.022895147382597,0.144785736790908,
0.552317470295194));
#34265=CARTESIAN_POINT('Ctrl Pts',(0.0705174972239762,0.13725515579246,
0.549684066340392));
#34266=CARTESIAN_POINT('Ctrl Pts',(0.11406115054758,0.103931463677311,0.54705066238559));
#34267=CARTESIAN_POINT('Ctrl Pts',(0.133773489094236,0.0599312186369601,
0.544417258430788));
#34268=CARTESIAN_POINT('Ctrl Pts',(0.153485827640893,0.0159309735966095,
0.541783854475986));
#34269=CARTESIAN_POINT('Ctrl Pts',(0.149366851410602,-0.038745824368944,
0.539150450521183));
#34270=CARTESIAN_POINT('Ctrl Pts',(0.123285043153097,-0.0792962514025479,
0.536517046566381));
#34271=CARTESIAN_POINT('Ctrl Pts',(0.097203234895591,-0.119846678436152,
0.533883642611579));
#34272=CARTESIAN_POINT('Ctrl Pts',(0.0491585946108714,-0.146270734537808,
0.531250238656777));
#34273=CARTESIAN_POINT('Ctrl Pts',(0.000945514053129371,-0.146581729267096,
0.528616834701974));
#34274=CARTESIAN_POINT('Ctrl Pts',(-0.0472675665046126,-0.146892723996384,
0.525983430747172));
#34275=CARTESIAN_POINT('Ctrl Pts',(-0.0956490873353763,-0.121090657353305,
0.523350026792369));
#34276=CARTESIAN_POINT('Ctrl Pts',(-0.122251838252959,-0.0808800679743115,
0.520716622837567));
#34277=CARTESIAN_POINT('Ctrl Pts',(-0.137913765110592,-0.057206752695483,
0.519166250086475));
#34278=CARTESIAN_POINT('Ctrl Pts',(-0.146027018608819,-0.0285393430688772,
0.517615877335383));
#34279=CARTESIAN_POINT('Ctrl Pts',(-0.146145057762853,6.62388175271395E-5,
0.516065504584291));
#34280=CARTESIAN_POINT('Ctrl Pts',(-0.146174937959923,9.05479403153491E-5,
0.508934495415709));
#34281=CARTESIAN_POINT('Ctrl Pts',(-0.146000998710948,-0.0303806868131737,
0.510586832933351));
#34282=CARTESIAN_POINT('Ctrl Pts',(-0.136702921110135,-0.060949146702594,
0.512239170450992));
#34283=CARTESIAN_POINT('Ctrl Pts',(-0.119053907816366,-0.0855189520167866,
0.513891507968634));
#34284=CARTESIAN_POINT('Ctrl Pts',(-0.0909051978707368,-0.124705750264253,
0.51652684903514));
#34285=CARTESIAN_POINT('Ctrl Pts',(-0.041513711866252,-0.148633411035251,
0.519162190101645));
#34286=CARTESIAN_POINT('Ctrl Pts',(0.00668497479873183,-0.146433040097983,
0.521797531168151));
#34287=CARTESIAN_POINT('Ctrl Pts',(0.0548836614637157,-0.144232669160716,
0.524432872234657));
#34288=CARTESIAN_POINT('Ctrl Pts',(0.101889548789197,-0.115904266515181,
0.527068213301163));
#34289=CARTESIAN_POINT('Ctrl Pts',(0.126350695083001,-0.0743157182057725,
0.529703554367669));
#34290=CARTESIAN_POINT('Ctrl Pts',(0.150811841376805,-0.0327271698963649,
0.532338895434175));
#34291=CARTESIAN_POINT('Ctrl Pts',(0.152728246638932,0.0221215240769157,
0.53497423650068));
#34292=CARTESIAN_POINT('Ctrl Pts',(0.131229403455446,0.0653159076268943,
0.537609577567186));
#34293=CARTESIAN_POINT('Ctrl Pts',(0.10973056027196,0.108510291176874,0.540244918633692));
#34294=CARTESIAN_POINT('Ctrl Pts',(0.0648164686428582,0.140050364303552,
0.542880259700198));
#34295=CARTESIAN_POINT('Ctrl Pts',(0.0168888935424139,0.145609372621787,
0.545515600766704));
#34296=CARTESIAN_POINT('Ctrl Pts',(-0.0310386815580289,0.151168380940021,
0.54815094183321));
#34297=CARTESIAN_POINT('Ctrl Pts',(-0.0819797401298146,0.130746324449814,
0.550786282899715));
#34298=CARTESIAN_POINT('Ctrl Pts',(-0.112794829345876,0.093619712631646,
0.553421623966221));
#34299=CARTESIAN_POINT('Ctrl Pts',(-0.134282196795419,0.0677313192961588,
0.555259247782717));
#34300=CARTESIAN_POINT('Ctrl Pts',(-0.145983763479016,0.0337207109540846,
0.557096871599213));
#34301=CARTESIAN_POINT('Ctrl Pts',(-0.146253314944083,-0.00012165943743628,
0.558934495415709));
#34302=CARTESIAN_POINT('Origin',(0.,0.,0.));
#34303=CARTESIAN_POINT('',(-0.146555285157174,5.84873774584615E-5,0.616065504584291));
#34304=CARTESIAN_POINT('',(-0.146582406651585,1.90495679610238E-5,0.608934495415709));
#34305=CARTESIAN_POINT('',(-0.14635,-1.79227059055215E-17,0.));
#34306=CARTESIAN_POINT('Ctrl Pts',(-0.146555285157174,5.84873774584615E-5,
0.616065504584291));
#34307=CARTESIAN_POINT('Ctrl Pts',(-0.146572323774182,0.00339452825839206,
0.615883391459677));
#34308=CARTESIAN_POINT('Ctrl Pts',(-0.146468182740347,0.00672948697362643,
0.615701278335063));
#34309=CARTESIAN_POINT('Ctrl Pts',(-0.146239449746585,0.0100558783590757,
0.615519165210449));
#34310=CARTESIAN_POINT('Ctrl Pts',(-0.142931910151921,0.0581563776955572,
0.612885761255647));
#34311=CARTESIAN_POINT('Ctrl Pts',(-0.113572285175357,0.10446545479915,
0.610252357300844));
#34312=CARTESIAN_POINT('Ctrl Pts',(-0.0714789213525946,0.127976017886268,
0.607618953346042));
#34313=CARTESIAN_POINT('Ctrl Pts',(-0.0293855575298321,0.151486580973386,
0.60498554939124));
#34314=CARTESIAN_POINT('Ctrl Pts',(0.0254415451391293,0.15219863004403,
0.602352145436437));
#34315=CARTESIAN_POINT('Ctrl Pts',(0.068131280382423,0.129789159736893,
0.599718741481635));
#34316=CARTESIAN_POINT('Ctrl Pts',(0.110821015625717,0.107379689429756,
0.597085337526833));
#34317=CARTESIAN_POINT('Ctrl Pts',(0.141373383443343,0.0618486997448399,
0.594451933572031));
#34318=CARTESIAN_POINT('Ctrl Pts',(0.145928975807906,0.0138503202638931,
0.591818529617228));
#34319=CARTESIAN_POINT('Ctrl Pts',(0.150484568172469,-0.0341480592170517,
0.589185125662426));
#34320=CARTESIAN_POINT('Ctrl Pts',(0.129043385083969,-0.0846138284940251,
0.586551721707624));
#34321=CARTESIAN_POINT('Ctrl Pts',(0.0913317465051492,-0.114654304027699,
0.583918317752822));
#34322=CARTESIAN_POINT('Ctrl Pts',(0.0536201079263286,-0.144694779561374,
0.58128491379802));
#34323=CARTESIAN_POINT('Ctrl Pts',(-0.000361986142813277,-0.154309961351749,
0.578651509843217));
#34324=CARTESIAN_POINT('Ctrl Pts',(-0.0461267489505717,-0.139138134179699,
0.576018105888415));
#34325=CARTESIAN_POINT('Ctrl Pts',(-0.0918915117583307,-0.123966307007649,
0.573384701933613));
#34326=CARTESIAN_POINT('Ctrl Pts',(-0.129438943304707,-0.0840074708731724,
0.57075129797881));
#34327=CARTESIAN_POINT('Ctrl Pts',(-0.141736479132229,-0.0373880707573429,
0.568117894024008));
#34328=CARTESIAN_POINT('Ctrl Pts',(-0.14493124569041,-0.0252768557512302,
0.567433764210769));
#34329=CARTESIAN_POINT('Ctrl Pts',(-0.146421886434131,-0.0127161165512012,
0.56674963439753));
#34330=CARTESIAN_POINT('Ctrl Pts',(-0.146311419053965,-0.000129619860865307,
0.566065504584291));
#34331=CARTESIAN_POINT('Ctrl Pts',(-0.146253314944083,-0.00012165943743628,
0.558934495415709));
#34332=CARTESIAN_POINT('Ctrl Pts',(-0.146370327932007,-0.0148127199255511,
0.559732212665719));
#34333=CARTESIAN_POINT('Ctrl Pts',(-0.144333034185812,-0.0294720768038573,
0.560529929915728));
#34334=CARTESIAN_POINT('Ctrl Pts',(-0.140006765979157,-0.0434215338335114,
0.561327647165738));
#34335=CARTESIAN_POINT('Ctrl Pts',(-0.125714493536039,-0.089505001334368,
0.563962988232244));
#34336=CARTESIAN_POINT('Ctrl Pts',(-0.0864408287894652,-0.127840769189951,
0.56659832929875));
#34337=CARTESIAN_POINT('Ctrl Pts',(-0.0400254307145004,-0.141015208458223,
0.569233670365256));
#34338=CARTESIAN_POINT('Ctrl Pts',(0.00638996736046498,-0.154189647726494,
0.571869011431762));
#34339=CARTESIAN_POINT('Ctrl Pts',(0.0599470987638218,-0.142202758407454,
0.574504352498268));
#34340=CARTESIAN_POINT('Ctrl Pts',(0.0963181864448715,-0.110499461900809,
0.577139693564773));
#34341=CARTESIAN_POINT('Ctrl Pts',(0.132689274125921,-0.0787961653941636,
0.579775034631279));
#34342=CARTESIAN_POINT('Ctrl Pts',(0.151874318084663,-0.0273764616999143,
0.582410375697785));
#34343=CARTESIAN_POINT('Ctrl Pts',(0.145158709082207,0.0204027767224063,
0.585045716764291));
#34344=CARTESIAN_POINT('Ctrl Pts',(0.138443100079752,0.0681820151447277,
0.587681057830797));
#34345=CARTESIAN_POINT('Ctrl Pts',(0.1058268381161,0.112320788295119,0.590316398897302));
#34346=CARTESIAN_POINT('Ctrl Pts',(0.0621255253059884,0.132769511657806,
0.592951739963808));
#34347=CARTESIAN_POINT('Ctrl Pts',(0.0184242124958778,0.153218235020492,
0.595587081030314));
#34348=CARTESIAN_POINT('Ctrl Pts',(-0.0363621511606923,0.149976908595474,
0.59822242209682));
#34349=CARTESIAN_POINT('Ctrl Pts',(-0.0773474224829438,0.124517871631514,
0.600857763163326));
#34350=CARTESIAN_POINT('Ctrl Pts',(-0.118332693805197,0.0990588346675542,
0.603493104229832));
#34351=CARTESIAN_POINT('Ctrl Pts',(-0.145516872793131,0.0513820871646532,
0.606128445296338));
#34352=CARTESIAN_POINT('Ctrl Pts',(-0.146551825250685,0.00314430216262847,
0.608763786362843));
#34353=CARTESIAN_POINT('Ctrl Pts',(-0.146574172232136,0.00210273848614761,
0.608820689380465));
#34354=CARTESIAN_POINT('Ctrl Pts',(-0.146584327751734,0.00106091323912811,
0.608877592398087));
#34355=CARTESIAN_POINT('Ctrl Pts',(-0.146582406651585,1.90495679610238E-5,
0.608934495415709));
#34356=CARTESIAN_POINT('Origin',(0.,0.,0.));
#34357=CARTESIAN_POINT('',(-0.146154441698478,7.49371236435786E-5,0.666065504584291));
#34358=CARTESIAN_POINT('',(-0.14620212788816,0.000104817362006062,0.658934495415709));
#34359=CARTESIAN_POINT('',(-0.14635,-1.79227059055215E-17,0.));
#34360=CARTESIAN_POINT('Ctrl Pts',(-0.146154441698478,7.49371236435786E-5,
0.666065504584291));
#34361=CARTESIAN_POINT('Ctrl Pts',(-0.146245091243546,0.019414808211501,
0.665017148521823));
#34362=CARTESIAN_POINT('Ctrl Pts',(-0.142674700046404,0.0387225584902945,
0.663968792459356));
#34363=CARTESIAN_POINT('Ctrl Pts',(-0.135284782149148,0.0564369123056677,
0.662920436396889));
#34364=CARTESIAN_POINT('Ctrl Pts',(-0.116721776970831,0.100934245858918,
0.660287032442087));
#34365=CARTESIAN_POINT('Ctrl Pts',(-0.074058225042023,0.13537752586737,
0.657653628487285));
#34366=CARTESIAN_POINT('Ctrl Pts',(-0.0266475060286977,0.144142317777245,
0.655020224532483));
#34367=CARTESIAN_POINT('Ctrl Pts',(0.020763212984627,0.15290710968712,0.652386820577681));
#34368=CARTESIAN_POINT('Ctrl Pts',(0.0729210990824686,0.13599341349842,
0.649753416622878));
#34369=CARTESIAN_POINT('Ctrl Pts',(0.106165877238123,0.101073754565802,
0.647120012668076));
#34370=CARTESIAN_POINT('Ctrl Pts',(0.139410655393777,0.0661540956331838,
0.644486608713273));
#34371=CARTESIAN_POINT('Ctrl Pts',(0.153742325607243,0.0132284739566488,
0.641853204758471));
#34372=CARTESIAN_POINT('Ctrl Pts',(0.142659641677727,-0.0336945691193152,
0.639219800803669));
#34373=CARTESIAN_POINT('Ctrl Pts',(0.13157695774821,-0.0806176121952798,
0.636586396848867));
#34374=CARTESIAN_POINT('Ctrl Pts',(0.09507991967571,-0.121538076670673,
0.633952992894065));
#34375=CARTESIAN_POINT('Ctrl Pts',(0.049724604077795,-0.137893296070049,
0.631319588939263));
#34376=CARTESIAN_POINT('Ctrl Pts',(0.00436928847988189,-0.154248515469425,
0.62868618498446));
#34377=CARTESIAN_POINT('Ctrl Pts',(-0.0498443046434454,-0.146038489792785,
0.626052781029658));
#34378=CARTESIAN_POINT('Ctrl Pts',(-0.0883233740987275,-0.116987516169781,
0.623419377074855));
#34379=CARTESIAN_POINT('Ctrl Pts',(-0.1241414224228,-0.0899455634453427,
0.620968086244667));
#34380=CARTESIAN_POINT('Ctrl Pts',(-0.146325940865162,-0.0448455053352938,
0.618516795414479));
#34381=CARTESIAN_POINT('Ctrl Pts',(-0.146555285157174,5.84873774584615E-5,
0.616065504584291));
#34382=CARTESIAN_POINT('Ctrl Pts',(-0.146582406651585,1.90495679610238E-5,
0.608934495415709));
#34383=CARTESIAN_POINT('Ctrl Pts',(-0.146495356123754,-0.0471907653725723,
0.611512933464593));
#34384=CARTESIAN_POINT('Ctrl Pts',(-0.121611930441545,-0.0944794748712001,
0.614091371513477));
#34385=CARTESIAN_POINT('Ctrl Pts',(-0.0826169041730041,-0.121085801253764,
0.616669809562361));
#34386=CARTESIAN_POINT('Ctrl Pts',(-0.042761304710591,-0.148279297166989,
0.619305150628866));
#34387=CARTESIAN_POINT('Ctrl Pts',(0.0118356201414113,-0.153867466492291,
0.621940491695373));
#34388=CARTESIAN_POINT('Ctrl Pts',(0.0563737778341691,-0.135311940689286,
0.624575832761878));
#34389=CARTESIAN_POINT('Ctrl Pts',(0.100911935526926,-0.116756414886282,
0.627211173828384));
#34390=CARTESIAN_POINT('Ctrl Pts',(0.135391326060439,-0.0740571939549723,
0.62984651489489));
#34391=CARTESIAN_POINT('Ctrl Pts',(0.144150040296483,-0.0266099605959858,
0.632481855961396));
#34392=CARTESIAN_POINT('Ctrl Pts',(0.152908754532526,0.0208372727630014,
0.635117197027901));
#34393=CARTESIAN_POINT('Ctrl Pts',(0.135946792471101,0.0730325185496646,
0.637752538094407));
#34394=CARTESIAN_POINT('Ctrl Pts',(0.100968951224381,0.106266622271745,
0.640387879160913));
#34395=CARTESIAN_POINT('Ctrl Pts',(0.0659911099776614,0.139500725993825,
0.643023220227419));
#34396=CARTESIAN_POINT('Ctrl Pts',(0.0129973895456473,0.153773687651321,
0.645658561293925));
#34397=CARTESIAN_POINT('Ctrl Pts',(-0.0339403566699702,0.14260216095667,
0.648293902360431));
#34398=CARTESIAN_POINT('Ctrl Pts',(-0.0808781028855877,0.131430634262018,
0.650929243426936));
#34399=CARTESIAN_POINT('Ctrl Pts',(-0.121759874884809,0.0948146192152183,
0.653564584493442));
#34400=CARTESIAN_POINT('Ctrl Pts',(-0.138015547484023,0.0493865647021963,
0.656199925559948));
#34401=CARTESIAN_POINT('Ctrl Pts',(-0.143638130564433,0.0336737106740469,
0.657111448845201));
#34402=CARTESIAN_POINT('Ctrl Pts',(-0.146314545676077,0.0169066195134479,
0.658022972130455));
#34403=CARTESIAN_POINT('Ctrl Pts',(-0.14620212788816,0.000104817362006062,
0.658934495415709));
#34404=CARTESIAN_POINT('Origin',(0.,0.,0.));
#34405=CARTESIAN_POINT('',(-0.146293122286189,-0.000127967976324597,0.716065504584291));
#34406=CARTESIAN_POINT('',(-0.146220133725287,-0.000111981377959844,0.708934495415709));
#34407=CARTESIAN_POINT('',(-0.14635,-1.79227059055215E-17,0.));
#34408=CARTESIAN_POINT('Ctrl Pts',(-0.146293122286189,-0.000127967976324597,
0.716065504584291));
#34409=CARTESIAN_POINT('Ctrl Pts',(-0.145991055868361,0.035107698155652,
0.714150905583971));
#34410=CARTESIAN_POINT('Ctrl Pts',(-0.133191339997662,0.0705402609933279,
0.71223630658365));
#34411=CARTESIAN_POINT('Ctrl Pts',(-0.110030394316881,0.0968525150836482,
0.71032170758333));
#34412=CARTESIAN_POINT('Ctrl Pts',(-0.0781740494934874,0.133043275639576,
0.707688303628528));
#34413=CARTESIAN_POINT('Ctrl Pts',(-0.0267161455114648,0.151980073612578,
0.705054899673726));
#34414=CARTESIAN_POINT('Ctrl Pts',(0.0210005740720494,0.145072648144428,
0.702421495718924));
#34415=CARTESIAN_POINT('Ctrl Pts',(0.0687172936555642,0.138165222676278,
0.699788091764121));
#34416=CARTESIAN_POINT('Ctrl Pts',(0.112692828840571,0.105413573766977,
0.697154687809319));
#34417=CARTESIAN_POINT('Ctrl Pts',(0.132978647675338,0.0616747648126076,
0.694521283854517));
#34418=CARTESIAN_POINT('Ctrl Pts',(0.153264466510106,0.0179359558582386,
0.691887879899714));
#34419=CARTESIAN_POINT('Ctrl Pts',(0.149860568994636,-0.0367900131411976,
0.689254475944912));
#34420=CARTESIAN_POINT('Ctrl Pts',(0.124311058190535,-0.0776779129690893,
0.68662107199011));
#34421=CARTESIAN_POINT('Ctrl Pts',(0.0987615473864338,-0.11856581279698,
0.683987668035308));
#34422=CARTESIAN_POINT('Ctrl Pts',(0.0510664232937013,-0.145615643453328,
0.681354264080505));
#34423=CARTESIAN_POINT('Ctrl Pts',(0.00286152734998743,-0.146556845670501,
0.678720860125703));
#34424=CARTESIAN_POINT('Ctrl Pts',(-0.0453433685937279,-0.147498047887674,
0.6760874561709));
#34425=CARTESIAN_POINT('Ctrl Pts',(-0.094058036388424,-0.122330621665673,
0.673454052216099));
#34426=CARTESIAN_POINT('Ctrl Pts',(-0.121184141071859,-0.082471215005648,
0.670820648261296));
#34427=CARTESIAN_POINT('Ctrl Pts',(-0.137511364617388,-0.0584798070786627,
0.669235600368961));
#34428=CARTESIAN_POINT('Ctrl Pts',(-0.146017385334238,-0.0291657216594994,
0.667650552476626));
#34429=CARTESIAN_POINT('Ctrl Pts',(-0.146154441698478,7.49371236435786E-5,
0.666065504584291));
#34430=CARTESIAN_POINT('Ctrl Pts',(-0.14620212788816,0.000104817362006062,
0.658934495415709));
#34431=CARTESIAN_POINT('Ctrl Pts',(-0.145989530157664,-0.0316697360413935,
0.660658313196961));
#34432=CARTESIAN_POINT('Ctrl Pts',(-0.135802925380645,-0.0635684301444077,
0.662382130978214));
#34433=CARTESIAN_POINT('Ctrl Pts',(-0.116706447513916,-0.088695711446933,
0.664105948759466));
#34434=CARTESIAN_POINT('Ctrl Pts',(-0.0875121017453893,-0.127109839103795,
0.666741289825971));
#34435=CARTESIAN_POINT('Ctrl Pts',(-0.0374938370091297,-0.149698000438276,
0.669376630892477));
#34436=CARTESIAN_POINT('Ctrl Pts',(0.0106280634930049,-0.146199755084551,
0.672011971958983));
#34437=CARTESIAN_POINT('Ctrl Pts',(0.0587499639951401,-0.142701509730827,
0.674647313025488));
#34438=CARTESIAN_POINT('Ctrl Pts',(0.104975500263151,-0.113116857688896,
0.677282654091995));
#34439=CARTESIAN_POINT('Ctrl Pts',(0.128307197060476,-0.0708843233930653,
0.679917995158501));
#34440=CARTESIAN_POINT('Ctrl Pts',(0.1516388938578,-0.0286517890972343,
0.682553336225006));
#34441=CARTESIAN_POINT('Ctrl Pts',(0.152076751184439,0.0262286274524959,
0.685188677291512));
#34442=CARTESIAN_POINT('Ctrl Pts',(0.129421876845612,0.06882806051419,0.687824018358017));
#34443=CARTESIAN_POINT('Ctrl Pts',(0.106767002506784,0.111427493575885,
0.690459359424523));
#34444=CARTESIAN_POINT('Ctrl Pts',(0.0610193965024891,0.141745943149541,
0.69309470049103));
#34445=CARTESIAN_POINT('Ctrl Pts',(0.0129594391535466,0.146011564806377,
0.695730041557535));
#34446=CARTESIAN_POINT('Ctrl Pts',(-0.0351005181953946,0.150277186463213,
0.698365382624041));
#34447=CARTESIAN_POINT('Ctrl Pts',(-0.0854728268889839,0.128489980203229,
0.701000723690547));
#34448=CARTESIAN_POINT('Ctrl Pts',(-0.115276382892,0.0905465607729482,0.703636064757053));
#34449=CARTESIAN_POINT('Ctrl Pts',(-0.135250024617843,0.0651177741718751,
0.705402208309938));
#34450=CARTESIAN_POINT('Ctrl Pts',(-0.145985488943994,0.0324326426859288,
0.707168351862824));
#34451=CARTESIAN_POINT('Ctrl Pts',(-0.146220133725287,-0.000111981377959844,
0.708934495415709));
#34452=CARTESIAN_POINT('Origin',(0.,0.,0.));
#34453=CARTESIAN_POINT('',(-0.146564965442509,4.80374956639621E-5,0.766065504584291));
#34454=CARTESIAN_POINT('',(-0.14658533994215,-4.90005960534454E-6,0.758934495415709));
#34455=CARTESIAN_POINT('',(-0.14635,-1.79227059055215E-17,0.));
#34456=CARTESIAN_POINT('Ctrl Pts',(-0.146564965442509,4.80374956639621E-5,
0.766065504584291));
#34457=CARTESIAN_POINT('Ctrl Pts',(-0.146576599691724,0.00274840678048242,
0.76591806660092));
#34458=CARTESIAN_POINT('Ctrl Pts',(-0.146508366823243,0.00544817658194007,
0.765770628617549));
#34459=CARTESIAN_POINT('Ctrl Pts',(-0.146358404344074,0.00814339894155673,
0.765623190634177));
#34460=CARTESIAN_POINT('Ctrl Pts',(-0.14367991012782,0.0562830238780745,
0.762989786679375));
#34461=CARTESIAN_POINT('Ctrl Pts',(-0.11492813804623,0.102971929623608,
0.760356382724573));
#34462=CARTESIAN_POINT('Ctrl Pts',(-0.0731456970048765,0.127030722191848,
0.757722978769771));
#34463=CARTESIAN_POINT('Ctrl Pts',(-0.031363255963523,0.151089514760089,
0.755089574814969));
#34464=CARTESIAN_POINT('Ctrl Pts',(0.023449854037593,0.152518194151036,
0.752456170860167));
#34465=CARTESIAN_POINT('Ctrl Pts',(0.0664288749466077,0.130668672151013,
0.749822766905364));
#34466=CARTESIAN_POINT('Ctrl Pts',(0.109407895855622,0.108819150150991,
0.747189362950562));
#34467=CARTESIAN_POINT('Ctrl Pts',(0.140552827672535,0.0636914267599971,
0.744555958995759));
#34468=CARTESIAN_POINT('Ctrl Pts',(0.145735458379408,0.0157566983326864,
0.741922555040957));
#34469=CARTESIAN_POINT('Ctrl Pts',(0.150918089086281,-0.0321780300946251,
0.739289151086155));
#34470=CARTESIAN_POINT('Ctrl Pts',(0.130138418683114,-0.0829197635582554,
0.736655747131352));
#34471=CARTESIAN_POINT('Ctrl Pts',(0.0928226866975336,-0.113450633258391,
0.73402234317655));
#34472=CARTESIAN_POINT('Ctrl Pts',(0.0555069547119538,-0.143981502958525,
0.731388939221748));
#34473=CARTESIAN_POINT('Ctrl Pts',(0.00165516114396223,-0.154301508895166,
0.728755535266946));
#34474=CARTESIAN_POINT('Ctrl Pts',(-0.0443040153143291,-0.139729208016517,
0.726122131312144));
#34475=CARTESIAN_POINT('Ctrl Pts',(-0.0902631917726212,-0.125156907137867,
0.723488727357341));
#34476=CARTESIAN_POINT('Ctrl Pts',(-0.128329751121212,-0.0856922994439281,
0.720855323402539));
#34477=CARTESIAN_POINT('Ctrl Pts',(-0.141235637963126,-0.0392376340275311,
0.718221919447737));
#34478=CARTESIAN_POINT('Ctrl Pts',(-0.144758384781757,-0.0265575271266455,
0.717503114493255));
#34479=CARTESIAN_POINT('Ctrl Pts',(-0.146406528193996,-0.0133566238911661,
0.716784309538773));
#34480=CARTESIAN_POINT('Ctrl Pts',(-0.146293122286189,-0.000127967976324597,
0.716065504584291));
#34481=CARTESIAN_POINT('Ctrl Pts',(-0.146220133725287,-0.000111981377959844,
0.708934495415709));
#34482=CARTESIAN_POINT('Ctrl Pts',(-0.146335612821056,-0.016128633179466,
0.709803692929329));
#34483=CARTESIAN_POINT('Ctrl Pts',(-0.143907730109974,-0.0321112532361818,
0.71067289044295));
#34484=CARTESIAN_POINT('Ctrl Pts',(-0.138785978242991,-0.047178134378496,
0.71154208795657));
#34485=CARTESIAN_POINT('Ctrl Pts',(-0.123257214278523,-0.0928597774990785,
0.714177429023076));
#34486=CARTESIAN_POINT('Ctrl Pts',(-0.0829648830371437,-0.130123431139663,
0.716812770089582));
#34487=CARTESIAN_POINT('Ctrl Pts',(-0.0362113622873864,-0.142042463234138,
0.719448111156088));
#34488=CARTESIAN_POINT('Ctrl Pts',(0.0105421584623702,-0.153961495328613,
0.722083452222593));
#34489=CARTESIAN_POINT('Ctrl Pts',(0.063756868720506,-0.140535905876979,
0.724718793289099));
#34490=CARTESIAN_POINT('Ctrl Pts',(0.0992605327204626,-0.107864131039655,
0.727354134355605));
#34491=CARTESIAN_POINT('Ctrl Pts',(0.13476419672042,-0.075192356202331,
0.729989475422111));
#34492=CARTESIAN_POINT('Ctrl Pts',(0.152556814462199,-0.0232743959793195,
0.732624816488617));
#34493=CARTESIAN_POINT('Ctrl Pts',(0.144556272029555,0.024306549251931,
0.735260157555123));
#34494=CARTESIAN_POINT('Ctrl Pts',(0.136555729596912,0.0718874944831808,
0.737895498621628));
#34495=CARTESIAN_POINT('Ctrl Pts',(0.102762026989844,0.115131424722669,
0.740530839688134));
#34496=CARTESIAN_POINT('Ctrl Pts',(0.058525606626993,0.13439522866968,0.74316618075464));
#34497=CARTESIAN_POINT('Ctrl Pts',(0.0142891862641413,0.15365903261669,
0.745801521821146));
#34498=CARTESIAN_POINT('Ctrl Pts',(-0.0403899518544944,0.148942710271224,
0.748436862887652));
#34499=CARTESIAN_POINT('Ctrl Pts',(-0.0806743706113798,0.122388602614794,
0.751072203954158));
#34500=CARTESIAN_POINT('Ctrl Pts',(-0.120735958293688,0.0959813775627587,
0.753692967774675));
#34501=CARTESIAN_POINT('Ctrl Pts',(-0.146561633397375,0.047977288078364,
0.756313731595192));
#34502=CARTESIAN_POINT('Ctrl Pts',(-0.14658533994215,-4.90005960534454E-6,
0.758934495415709));
#34503=CARTESIAN_POINT('Origin',(0.,0.,0.));
#34504=CARTESIAN_POINT('',(-0.146164975321328,8.31911013993853E-5,0.816065504584291));
#34505=CARTESIAN_POINT('',(-0.146233275186053,0.000116309547457056,0.808934495415709));
#34506=CARTESIAN_POINT('',(-0.14635,-1.79227059055215E-17,0.));
#34507=CARTESIAN_POINT('Ctrl Pts',(-0.146164975321328,8.31911013993853E-5,
0.816065504584291));
#34508=CARTESIAN_POINT('Ctrl Pts',(-0.146262710135629,0.0187799830896948,
0.815051823663067));
#34509=CARTESIAN_POINT('Ctrl Pts',(-0.142931951335767,0.037443276248974,
0.814038142741842));
#34510=CARTESIAN_POINT('Ctrl Pts',(-0.136010977838838,0.054663650141277,
0.813024461820618));
#34511=CARTESIAN_POINT('Ctrl Pts',(-0.118031238261729,0.0993998188524282,
0.810391057865816));
#34512=CARTESIAN_POINT('Ctrl Pts',(-0.0758215305972079,0.13439788253602,
0.807757653911014));
#34513=CARTESIAN_POINT('Ctrl Pts',(-0.028529425342275,0.143781679589591,
0.805124249956212));
#34514=CARTESIAN_POINT('Ctrl Pts',(0.0187626799126572,0.153165476643161,
0.80249084600141));
#34515=CARTESIAN_POINT('Ctrl Pts',(0.0711371827580015,0.136935007066712,
0.799857442046606));
#34516=CARTESIAN_POINT('Ctrl Pts',(0.104835580177757,0.102452897995539,
0.797224038091804));
#34517=CARTESIAN_POINT('Ctrl Pts',(0.138533977597513,0.0679707889243652,
0.794590634137002));
#34518=CARTESIAN_POINT('Ctrl Pts',(0.15355626959168,0.0152370403584678,
0.791957230182201));
#34519=CARTESIAN_POINT('Ctrl Pts',(0.143087905965057,-0.0318268624597296,
0.789323826227399));
#34520=CARTESIAN_POINT('Ctrl Pts',(0.132619542338435,-0.0788907652779263,
0.786690422272596));
#34521=CARTESIAN_POINT('Ctrl Pts',(0.096660523091021,-0.120284822348423,
0.784057018317793));
#34522=CARTESIAN_POINT('Ctrl Pts',(0.0515228742830193,-0.137231523355512,
0.781423614362991));
#34523=CARTESIAN_POINT('Ctrl Pts',(0.00638522547501753,-0.1541782243626,
0.778790210408188));
#34524=CARTESIAN_POINT('Ctrl Pts',(-0.0479310528935715,-0.146677569306282,
0.776156806453387));
#34525=CARTESIAN_POINT('Ctrl Pts',(-0.0867865839024083,-0.118132069714372,
0.773523402498585));
#34526=CARTESIAN_POINT('Ctrl Pts',(-0.123466686745614,-0.0911847643100577,
0.771037436527154));
#34527=CARTESIAN_POINT('Ctrl Pts',(-0.146368799251201,-0.045483147880463,
0.768551470555722));
#34528=CARTESIAN_POINT('Ctrl Pts',(-0.146564965442509,4.80374956639621E-5,
0.766065504584291));
#34529=CARTESIAN_POINT('Ctrl Pts',(-0.14658533994215,-4.90005960534454E-6,
0.758934495415709));
#34530=CARTESIAN_POINT('Ctrl Pts',(-0.146609310208618,-0.0485208624767226,
0.761584413728203));
#34531=CARTESIAN_POINT('Ctrl Pts',(-0.120122621218798,-0.0970137112575841,
0.764234332040698));
#34532=CARTESIAN_POINT('Ctrl Pts',(-0.0793243537302287,-0.123267883191947,
0.766884250353192));
#34533=CARTESIAN_POINT('Ctrl Pts',(-0.0387505182093485,-0.149377630477176,
0.769519591419698));
#34534=CARTESIAN_POINT('Ctrl Pts',(0.0159771533787021,-0.153492702582488,
0.772154932486204));
#34535=CARTESIAN_POINT('Ctrl Pts',(0.0599991778729333,-0.13374387011901,
0.77479027355271));
#34536=CARTESIAN_POINT('Ctrl Pts',(0.104021202367166,-0.113995037655531,
0.777425614619216));
#34537=CARTESIAN_POINT('Ctrl Pts',(0.13733757976758,-0.0703823006232647,
0.780060955685721));
#34538=CARTESIAN_POINT('Ctrl Pts',(0.14481468818493,-0.022716297290398,
0.782696296752227));
#34539=CARTESIAN_POINT('Ctrl Pts',(0.152291796602279,0.0249497060424673,
0.785331637818733));
#34540=CARTESIAN_POINT('Ctrl Pts',(0.133929636036564,0.0766689756759309,
0.787966978885239));
#34541=CARTESIAN_POINT('Ctrl Pts',(0.0980690284933123,0.108948564888508,
0.790602319951745));
#34542=CARTESIAN_POINT('Ctrl Pts',(0.0622084209500598,0.141228154101085,
0.793237661018251));
#34543=CARTESIAN_POINT('Ctrl Pts',(0.00884936642926935,0.154068062892775,
0.795873002084756));
#34544=CARTESIAN_POINT('Ctrl Pts',(-0.0377703306973942,0.141635893595607,
0.798508343151262));
#34545=CARTESIAN_POINT('Ctrl Pts',(-0.084390027824057,0.129203724298439,
0.801143684217768));
#34546=CARTESIAN_POINT('Ctrl Pts',(-0.124270367556593,0.0914994769124139,
0.803779025284273));
#34547=CARTESIAN_POINT('Ctrl Pts',(-0.139296118286606,0.0456499204587224,
0.806414366350779));
#34548=CARTESIAN_POINT('Ctrl Pts',(-0.144085736300807,0.0310348862098803,
0.807254409372422));
#34549=CARTESIAN_POINT('Ctrl Pts',(-0.146349920545361,0.0155922205493257,
0.808094452394066));
#34550=CARTESIAN_POINT('Ctrl Pts',(-0.146233275186053,0.000116309547457056,
0.808934495415709));
#34551=CARTESIAN_POINT('Origin',(0.,0.,0.));
#34552=CARTESIAN_POINT('',(-0.146273246343463,-0.000123611542196964,0.866065504584292));
#34553=CARTESIAN_POINT('',(-0.146190615322833,-9.92620605964336E-5,0.858934495415709));
#34554=CARTESIAN_POINT('',(-0.14635,-1.79227059055215E-17,0.));
#34555=CARTESIAN_POINT('Ctrl Pts',(-0.146273246343463,-0.000123611542196964,
0.866065504584292));
#34556=CARTESIAN_POINT('Ctrl Pts',(-0.14598570205562,0.0344841852260994,
0.864185580725214));
#34557=CARTESIAN_POINT('Ctrl Pts',(-0.13368920007778,0.0692748383916789,
0.862305656866136));
#34558=CARTESIAN_POINT('Ctrl Pts',(-0.111287960012964,0.0954050911579531,
0.860425733007059));
#34559=CARTESIAN_POINT('Ctrl Pts',(-0.0799082241293448,0.13200844115132,
0.857792329052257));
#34560=CARTESIAN_POINT('Ctrl Pts',(-0.0287004609307042,0.151617916172533,
0.855158925097454));
#34561=CARTESIAN_POINT('Ctrl Pts',(0.0191028994225217,0.145335216041435,
0.852525521142652));
#34562=CARTESIAN_POINT('Ctrl Pts',(0.0669062597757476,0.139052515910338,
0.84989211718785));
#34563=CARTESIAN_POINT('Ctrl Pts',(0.111305217283559,0.10687764062693,0.847258713233048));
#34564=CARTESIAN_POINT('Ctrl Pts',(0.132160826244895,0.0634075368078452,
0.844625309278246));
#34565=CARTESIAN_POINT('Ctrl Pts',(0.15301643520623,0.0199374329887607,
0.841991905323443));
#34566=CARTESIAN_POINT('Ctrl Pts',(0.15032869562109,-0.0348278993660004,
0.839358501368641));
#34567=CARTESIAN_POINT('Ctrl Pts',(0.12531596597325,-0.076046177073106,
0.836725097413839));
#34568=CARTESIAN_POINT('Ctrl Pts',(0.10030323632541,-0.117264454780212,
0.834091693459036));
#34569=CARTESIAN_POINT('Ctrl Pts',(0.0529655166148703,-0.144935677839662,
0.831458289504234));
#34570=CARTESIAN_POINT('Ctrl Pts',(0.00477698054298851,-0.14650698356075,
0.828824885549432));
#34571=CARTESIAN_POINT('Ctrl Pts',(-0.0434115555288926,-0.148078289281839,
0.826191481594629));
#34572=CARTESIAN_POINT('Ctrl Pts',(-0.0924509079621152,-0.123549677664568,
0.823558077639828));
#34573=CARTESIAN_POINT('Ctrl Pts',(-0.120095698433879,-0.084048234986577,
0.820924673685025));
#34574=CARTESIAN_POINT('Ctrl Pts',(-0.137099129982578,-0.059752153692848,
0.819304950651447));
#34575=CARTESIAN_POINT('Ctrl Pts',(-0.146008808497438,-0.0297917172680741,
0.817685227617869));
#34576=CARTESIAN_POINT('Ctrl Pts',(-0.146164975321328,8.31911013993853E-5,
0.816065504584291));
#34577=CARTESIAN_POINT('Ctrl Pts',(-0.146233275186053,0.000116309547457056,
0.808934495415709));
#34578=CARTESIAN_POINT('Ctrl Pts',(-0.145983986542363,-0.0329580355137906,
0.810729793460572));
#34579=CARTESIAN_POINT('Ctrl Pts',(-0.134860471440613,-0.0661842257005933,
0.812525091505434));
#34580=CARTESIAN_POINT('Ctrl Pts',(-0.114274246165196,-0.0918080661847913,
0.814320389550297));
#34581=CARTESIAN_POINT('Ctrl Pts',(-0.0840554615862833,-0.129421630853252,
0.816955730616803));
#34582=CARTESIAN_POINT('Ctrl Pts',(-0.0334467307009701,-0.150653894668816,
0.819591071683309));
#34583=CARTESIAN_POINT('Ctrl Pts',(0.0145634383780638,-0.145860313412396,
0.822226412749814));
#34584=CARTESIAN_POINT('Ctrl Pts',(0.0625736074570984,-0.141066732155975,
0.82486175381632));
#34585=CARTESIAN_POINT('Ctrl Pts',(0.107985214729854,-0.110247305827569,
0.827497094882826));
#34586=CARTESIAN_POINT('Ctrl Pts',(0.130170526119325,-0.0674014545208048,
0.830132435949332));
#34587=CARTESIAN_POINT('Ctrl Pts',(0.152355837508797,-0.0245556032140414,
0.832767777015837));
#34588=CARTESIAN_POINT('Ctrl Pts',(0.151314853014986,0.0303166730710795,
0.835403118082343));
#34589=CARTESIAN_POINT('Ctrl Pts',(0.127520386856677,0.0722902292399131,
0.838038459148849));
#34590=CARTESIAN_POINT('Ctrl Pts',(0.103725920698368,0.114263785408748,
0.840673800215355));
#34591=CARTESIAN_POINT('Ctrl Pts',(0.0571779728755602,0.143338621461295,
0.843309141281861));
#34592=CARTESIAN_POINT('Ctrl Pts',(0.00902055110528975,0.146307747926884,
0.845944482348367));
#34593=CARTESIAN_POINT('Ctrl Pts',(-0.0391368706649794,0.149276874392473,
0.848579823414872));
#34594=CARTESIAN_POINT('Ctrl Pts',(-0.088903766382711,0.126140291271107,
0.851215164481378));
#34595=CARTESIAN_POINT('Ctrl Pts',(-0.117674187241089,0.087407636925452,
0.853850505547884));
#34596=CARTESIAN_POINT('Ctrl Pts',(-0.136175085157248,0.0625004974853221,
0.855545168837159));
#34597=CARTESIAN_POINT('Ctrl Pts',(-0.145993587468369,0.0311441202011877,
0.857239832126434));
#34598=CARTESIAN_POINT('Ctrl Pts',(-0.146190615322833,-9.92620605964336E-5,
0.858934495415709));
#34599=CARTESIAN_POINT('Origin',(0.,0.,-0.0924367114736152));
#34600=CARTESIAN_POINT('',(-0.117713232580125,-9.94762513365651E-5,0.882563288526385));
#34601=CARTESIAN_POINT('',(-0.11796233779121,-2.11776828218935E-5,0.892436711473616));
#34602=CARTESIAN_POINT('',(-0.117775,-1.30487598617993E-14,-0.0924367114736152));
#34603=CARTESIAN_POINT('',(-0.11766859746431,0.00500517689819253,0.932224999999999));
#34604=CARTESIAN_POINT('Ctrl Pts',(-0.117713232580125,-9.94762513365794E-5,
0.882563288526385));
#34605=CARTESIAN_POINT('Ctrl Pts',(-0.117805978893427,-0.0112620890991194,
0.88331676862211));
#34606=CARTESIAN_POINT('Ctrl Pts',(-0.111244449407799,-0.0613316426944826,
0.886703652672637));
#34607=CARTESIAN_POINT('Ctrl Pts',(-0.0402800891732956,-0.133026134299755,
0.892723940677965));
#34608=CARTESIAN_POINT('Ctrl Pts',(0.0894243408305711,-0.10638650575871,
0.900624152542373));
#34609=CARTESIAN_POINT('Ctrl Pts',(0.137929356340621,0.0167100404698593,
0.908524364406779));
#34610=CARTESIAN_POINT('Ctrl Pts',(0.0614290966487016,0.124766721395902,
0.916424576271187));
#34611=CARTESIAN_POINT('Ctrl Pts',(-0.0710668305166857,0.11939070761148,
0.924324788135593));
#34612=CARTESIAN_POINT('Ctrl Pts',(-0.116012267804409,0.0439444575637681,
0.929591596045198));
#34613=CARTESIAN_POINT('Ctrl Pts',(-0.11766859746431,0.00500517689817995,
0.932225));
#34614=CARTESIAN_POINT('',(-0.0334019664626758,0.112939183906323,0.932224999999999));
#34615=CARTESIAN_POINT('Origin',(0.,0.,0.932225));
#34616=CARTESIAN_POINT('Ctrl Pts',(-0.11796233779121,-2.11776828218909E-5,
0.892436711473617));
#34617=CARTESIAN_POINT('Ctrl Pts',(-0.117965690360961,-0.00128932424828905,
0.892522768983215));
#34618=CARTESIAN_POINT('Ctrl Pts',(-0.117371901374032,-0.0413888390951994,
0.89524416755932));
#34619=CARTESIAN_POINT('Ctrl Pts',(-0.0720261204166176,-0.118897020856024,
0.90060090720193));
#34620=CARTESIAN_POINT('Ctrl Pts',(0.0602520802431792,-0.125231345176025,
0.908506930401448));
#34621=CARTESIAN_POINT('Ctrl Pts',(0.137949690524835,-0.017881538827179,
0.916412953600965));
#34622=CARTESIAN_POINT('Ctrl Pts',(0.0900118016872842,0.105886249500893,
0.924318976800482));
#34623=CARTESIAN_POINT('Ctrl Pts',(0.00399973323748277,0.12400080376067,
0.929589658933494));
#34624=CARTESIAN_POINT('Ctrl Pts',(-0.0334019664626807,0.112939183906322,
0.932225));
#34625=CARTESIAN_POINT('Origin',(0.,0.,-0.0924367114736152));
#34626=CARTESIAN_POINT('',(-0.117626101595281,6.69479464755203E-5,0.832563288526385));
#34627=CARTESIAN_POINT('',(-0.117646735358023,-7.98810330651378E-5,0.842436711473617));
#34628=CARTESIAN_POINT('',(-0.117775,-1.30487598617993E-14,-0.0924367114736152));
#34629=CARTESIAN_POINT('Ctrl Pts',(-0.117626101595281,6.69479464755242E-5,
0.832563288526385));
#34630=CARTESIAN_POINT('Ctrl Pts',(-0.117500426517155,-0.023974851392196,
0.834183011559963));
#34631=CARTESIAN_POINT('Ctrl Pts',(-0.0986730411655657,-0.0872854052949152,
0.838436138548343));
#34632=CARTESIAN_POINT('Ctrl Pts',(0.00452896330992775,-0.13890521184416,
0.845322669491525));
#34633=CARTESIAN_POINT('Ctrl Pts',(0.118813895436517,-0.0721000537472655,
0.853222881355933));
#34634=CARTESIAN_POINT('Ctrl Pts',(0.125302761776928,0.0601169674638447,
0.861123093220339));
#34635=CARTESIAN_POINT('Ctrl Pts',(0.0181127265090936,0.137795052940508,
0.869023305084746));
#34636=CARTESIAN_POINT('Ctrl Pts',(-0.0937244491952465,0.0949681812626695,
0.876170036853428));
#34637=CARTESIAN_POINT('Ctrl Pts',(-0.11748183163376,0.0277511097711188,
0.880683364667308));
#34638=CARTESIAN_POINT('Ctrl Pts',(-0.117713232580125,-9.94762513365794E-5,
0.882563288526385));
#34639=CARTESIAN_POINT('Ctrl Pts',(-0.117646735358023,-7.9881033065143E-5,
0.842436711473617));
#34640=CARTESIAN_POINT('Ctrl Pts',(-0.117734748084911,-0.0140363608293074,
0.843377389250847));
#34641=CARTESIAN_POINT('Ctrl Pts',(-0.108999987861276,-0.0669858868324248,
0.846953408094583));
#34642=CARTESIAN_POINT('Ctrl Pts',(-0.0306982239304521,-0.135581215292453,
0.853164768004825));
#34643=CARTESIAN_POINT('Ctrl Pts',(0.0968538014257187,-0.0997179081430208,
0.861070791204343));
#34644=CARTESIAN_POINT('Ctrl Pts',(0.136419444538435,0.0267352712365894,
0.86897681440386));
#34645=CARTESIAN_POINT('Ctrl Pts',(0.0520445414416943,0.128903423908239,
0.876882837603378));
#34646=CARTESIAN_POINT('Ctrl Pts',(-0.0781668699995673,0.11412164151165,
0.884702803293296));
#34647=CARTESIAN_POINT('Ctrl Pts',(-0.117863024541527,0.0375451567622119,
0.889887427916709));
#34648=CARTESIAN_POINT('Ctrl Pts',(-0.11796233779121,-2.11776828218909E-5,
0.892436711473617));
#34649=CARTESIAN_POINT('Origin',(0.,0.,-0.0924367114736152));
#34650=CARTESIAN_POINT('',(-0.117947993201171,3.86581212928119E-5,0.782563288526384));
#34651=CARTESIAN_POINT('',(-0.117681065835582,9.35999791555828E-5,0.792436711473616));
#34652=CARTESIAN_POINT('',(-0.117775,-1.30487598617993E-14,-0.0924367114736152));
#34653=CARTESIAN_POINT('Ctrl Pts',(-0.117947993201171,3.86581212928078E-5,
0.782563288526385));
#34654=CARTESIAN_POINT('Ctrl Pts',(-0.117790128676528,-0.0366025127545069,
0.785049254497816));
#34655=CARTESIAN_POINT('Ctrl Pts',(-0.0798361540276521,-0.112340416450435,
0.790168624424051));
#34656=CARTESIAN_POINT('Ctrl Pts',(0.0488494678181175,-0.130110898691923,
0.797921398305084));
#34657=CARTESIAN_POINT('Ctrl Pts',(0.135663410254684,-0.0301754342953877,
0.805821610169492));
#34658=CARTESIAN_POINT('Ctrl Pts',(0.0993958918478579,0.0971368425207782,
0.813721822033898));
#34659=CARTESIAN_POINT('Ctrl Pts',(-0.0270490771841315,0.136321199631122,
0.821622033898304));
#34660=CARTESIAN_POINT('Ctrl Pts',(-0.10806095418056,0.0691504233541856,
0.827902522729134));
#34661=CARTESIAN_POINT('Ctrl Pts',(-0.11770475357857,0.0151131705390384,
0.831549607605161));
#34662=CARTESIAN_POINT('Ctrl Pts',(-0.117626101595281,6.69479464755242E-5,
0.832563288526385));
#34663=CARTESIAN_POINT('Ctrl Pts',(-0.117681065835582,9.35999791555758E-5,
0.792436711473616));
#34664=CARTESIAN_POINT('Ctrl Pts',(-0.117480451076367,-0.0265229424847173,
0.794232009518479));
#34665=CARTESIAN_POINT('Ctrl Pts',(-0.0953885925249484,-0.0925118216380055,
0.798662648629848));
#34666=CARTESIAN_POINT('Ctrl Pts',(0.0138111005924944,-0.138325195186183,
0.80572862880772));
#34667=CARTESIAN_POINT('Ctrl Pts',(0.123445922182148,-0.0639194978340518,
0.813634652007238));
#34668=CARTESIAN_POINT('Ctrl Pts',(0.120932728835538,0.0685557124046954,
0.821540675206756));
#34669=CARTESIAN_POINT('Ctrl Pts',(0.0085545008581314,0.138749538494654,
0.829446698406273));
#34670=CARTESIAN_POINT('Ctrl Pts',(-0.0972993756118875,0.0895381706496827,
0.83641204382856));
#34671=CARTESIAN_POINT('Ctrl Pts',(-0.117488177410916,0.0250631961509614,
0.840742048184341));
#34672=CARTESIAN_POINT('Ctrl Pts',(-0.117646735358023,-7.9881033065143E-5,
0.842436711473617));
#34673=CARTESIAN_POINT('Origin',(0.,0.,-0.0924367114736152));
#34674=CARTESIAN_POINT('',(-0.117729227722965,-0.000102982086865302,0.732563288526385));
#34675=CARTESIAN_POINT('',(-0.117964389557135,-3.94331754086097E-6,0.742436711473616));
#34676=CARTESIAN_POINT('',(-0.117775,-1.30487598617993E-14,-0.0924367114736152));
#34677=CARTESIAN_POINT('Ctrl Pts',(-0.117729227722965,-0.000102982086865302,
0.732563288526385));
#34678=CARTESIAN_POINT('Ctrl Pts',(-0.117820491001352,-0.0107487282458691,
0.733282093480867));
#34679=CARTESIAN_POINT('Ctrl Pts',(-0.111634982628329,-0.060291927513671,
0.73663430239015));
#34680=CARTESIAN_POINT('Ctrl Pts',(-0.0420051819866054,-0.132478981273086,
0.742619915254238));
#34681=CARTESIAN_POINT('Ctrl Pts',(0.0880063312515965,-0.107563941317063,
0.750520127118644));
#34682=CARTESIAN_POINT('Ctrl Pts',(0.1381735813042,0.0149391196739674,0.758420338983051));
#34683=CARTESIAN_POINT('Ctrl Pts',(0.0629820334107182,0.123888575547709,
0.766320550847457));
#34684=CARTESIAN_POINT('Ctrl Pts',(-0.069350334823955,0.120439391087123,
0.774220762711865));
#34685=CARTESIAN_POINT('Ctrl Pts',(-0.116921686943853,0.0431900873220952,
0.77963500860484));
#34686=CARTESIAN_POINT('Ctrl Pts',(-0.117957355850309,0.00221177730489086,
0.782415850543013));
#34687=CARTESIAN_POINT('Ctrl Pts',(-0.117947993201171,3.86581212928078E-5,
0.782563288526385));
#34688=CARTESIAN_POINT('Ctrl Pts',(-0.117964389557135,-3.94331754086175E-6,
0.742436711473616));
#34689=CARTESIAN_POINT('Ctrl Pts',(-0.117964495672005,-0.000218720446770248,
0.742451288719605));
#34690=CARTESIAN_POINT('Ctrl Pts',(-0.117867006535742,-0.039261788207105,
0.745101207032099));
#34691=CARTESIAN_POINT('Ctrl Pts',(-0.0752264694457675,-0.116899882557203,
0.750386466411098));
#34692=CARTESIAN_POINT('Ctrl Pts',(0.0568996293847587,-0.126834681679914,
0.758292489610617));
#34693=CARTESIAN_POINT('Ctrl Pts',(0.137333582544999,-0.0215427765762162,
0.766198512810132));
#34694=CARTESIAN_POINT('Ctrl Pts',(0.0930027975645983,0.103320297856606,
0.774104536009652));
#34695=CARTESIAN_POINT('Ctrl Pts',(-0.035819122070238,0.13431900488649,
0.782010559209168));
#34696=CARTESIAN_POINT('Ctrl Pts',(-0.110236635830862,0.0639621230870467,
0.788121284363823));
#34697=CARTESIAN_POINT('Ctrl Pts',(-0.117774936058969,0.0125478221742061,
0.791596668451973));
#34698=CARTESIAN_POINT('Ctrl Pts',(-0.117681065835582,9.35999791555758E-5,
0.792436711473616));
#34699=CARTESIAN_POINT('Origin',(0.,0.,-0.0924367114736152));
#34700=CARTESIAN_POINT('',(-0.117617624673989,6.03055670430245E-5,0.682563288526385));
#34701=CARTESIAN_POINT('',(-0.117670490259622,-9.01168895870441E-5,0.692436711473616));
#34702=CARTESIAN_POINT('',(-0.117775,-1.30487598617993E-14,-0.0924367114736152));
#34703=CARTESIAN_POINT('Ctrl Pts',(-0.117617624673989,6.03055670430289E-5,
0.682563288526385));
#34704=CARTESIAN_POINT('Ctrl Pts',(-0.117507328717046,-0.0234710821212703,
0.68414833641872));
#34705=CARTESIAN_POINT('Ctrl Pts',(-0.0992894616255371,-0.0862548596187289,
0.688366788265857));
#34706=CARTESIAN_POINT('Ctrl Pts',(0.00271304928865532,-0.138952348570324,
0.695218644067796));
#34707=CARTESIAN_POINT('Ctrl Pts',(0.117860843754417,-0.0736473850127282,
0.703118855932203));
#34708=CARTESIAN_POINT('Ctrl Pts',(0.126078691992566,0.0584746033489104,
0.711019067796611));
#34709=CARTESIAN_POINT('Ctrl Pts',(0.0199109026571207,0.137545162630623,
0.718919279661016));
#34710=CARTESIAN_POINT('Ctrl Pts',(-0.0930178497353151,0.0959867468400004,
0.726100686570943));
#34711=CARTESIAN_POINT('Ctrl Pts',(-0.117486140108619,0.0282528811088558,
0.730648689526065));
#34712=CARTESIAN_POINT('Ctrl Pts',(-0.117729227722965,-0.000102982086865302,
0.732563288526385));
#34713=CARTESIAN_POINT('Ctrl Pts',(-0.117670490259622,-9.01168895870632E-5,
0.692436711473616));
#34714=CARTESIAN_POINT('Ctrl Pts',(-0.117763421933718,-0.0129794996427261,
0.693305908987236));
#34715=CARTESIAN_POINT('Ctrl Pts',(-0.109885703418251,-0.0648380928819097,
0.696810447567362));
#34716=CARTESIAN_POINT('Ctrl Pts',(-0.0343406886760894,-0.134704570618338,
0.702950327213994));
#34717=CARTESIAN_POINT('Ctrl Pts',(0.0941327483034478,-0.102291886006113,
0.710856350413511));
#34718=CARTESIAN_POINT('Ctrl Pts',(0.137088516418336,0.0230508765206803,
0.718762373613029));
#34719=CARTESIAN_POINT('Ctrl Pts',(0.0555021824679276,0.127452391053421,
0.726668396812546));
#34720=CARTESIAN_POINT('Ctrl Pts',(-0.0762633445254468,0.116087019895361,
0.734559842766075));
#34721=CARTESIAN_POINT('Ctrl Pts',(-0.117945311741555,0.0386096693093802,
0.739815947653099));
#34722=CARTESIAN_POINT('Ctrl Pts',(-0.117964389557135,-3.94331754086175E-6,
0.742436711473616));
#34723=CARTESIAN_POINT('Origin',(0.,0.,-0.0924367114736152));
#34724=CARTESIAN_POINT('',(-0.117940203002297,4.70676520639361E-5,0.632563288526384));
#34725=CARTESIAN_POINT('',(-0.117656000082187,8.43516556759474E-5,0.642436711473616));
#34726=CARTESIAN_POINT('',(-0.117775,-1.30487598617993E-14,-0.0924367114736152));
#34727=CARTESIAN_POINT('Ctrl Pts',(-0.117940203002297,4.7067652063935E-5,
0.632563288526384));
#34728=CARTESIAN_POINT('Ctrl Pts',(-0.117755638437952,-0.0360893706242894,
0.635014579356573));
#34729=CARTESIAN_POINT('Ctrl Pts',(-0.0807233593759693,-0.111374211355997,
0.640099274141563));
#34730=CARTESIAN_POINT('Ctrl Pts',(0.0471445089225743,-0.130738330601145,
0.647817372881356));
#34731=CARTESIAN_POINT('Ctrl Pts',(0.135257361515437,-0.0319462355497722,
0.655717584745763));
#34732=CARTESIAN_POINT('Ctrl Pts',(0.100657174442164,0.0958292702846084,
0.66361779661017));
#34733=CARTESIAN_POINT('Ctrl Pts',(-0.0252648283287276,0.136663104967713,
0.671518008474576));
#34734=CARTESIAN_POINT('Ctrl Pts',(-0.107599838532302,0.0701921319068488,
0.677833172446648));
#34735=CARTESIAN_POINT('Ctrl Pts',(-0.11769057479473,0.0156240453509343,
0.681514932463917));
#34736=CARTESIAN_POINT('Ctrl Pts',(-0.117617624673989,6.03055670430289E-5,
0.682563288526385));
#34737=CARTESIAN_POINT('Ctrl Pts',(-0.117656000082187,8.43516556759457E-5,
0.642436711473616));
#34738=CARTESIAN_POINT('Ctrl Pts',(-0.117484912294625,-0.0254861849147704,
0.644160529254868));
#34739=CARTESIAN_POINT('Ctrl Pts',(-0.0967548225821553,-0.0904011202578769,
0.648519688102626));
#34740=CARTESIAN_POINT('Ctrl Pts',(0.0100790193068892,-0.138647097388359,
0.655514188016889));
#34741=CARTESIAN_POINT('Ctrl Pts',(0.121678866262096,-0.0672224497442505,
0.663420211216407));
#34742=CARTESIAN_POINT('Ctrl Pts',(0.122735961854403,0.0652724131012164,
0.671326234415924));
#34743=CARTESIAN_POINT('Ctrl Pts',(0.0122899564463577,0.138468628991968,
0.679232257615441));
#34744=CARTESIAN_POINT('Ctrl Pts',(-0.0959511456548746,0.0916518108144888,
0.686269083301339));
#34745=CARTESIAN_POINT('Ctrl Pts',(-0.117481660132417,0.0261001331898457,
0.69067056792073));
#34746=CARTESIAN_POINT('Ctrl Pts',(-0.117670490259622,-9.01168895870632E-5,
0.692436711473616));
#34747=CARTESIAN_POINT('Origin',(0.,0.,-0.0924367114736152));
#34748=CARTESIAN_POINT('',(-0.117743952026517,-0.000104311439111954,0.582563288526385));
#34749=CARTESIAN_POINT('',(-0.11796202899481,1.53301186523688E-5,0.592436711473616));
#34750=CARTESIAN_POINT('',(-0.117775,-1.30487598617993E-14,-0.0924367114736152));
#34751=CARTESIAN_POINT('Ctrl Pts',(-0.117743952026517,-0.000104311439111965,
0.582563288526385));
#34752=CARTESIAN_POINT('Ctrl Pts',(-0.117832850528047,-0.0102332806752188,
0.583247418339623));
#34753=CARTESIAN_POINT('Ctrl Pts',(-0.112015701243022,-0.0592509231652696,
0.586564952107665));
#34754=CARTESIAN_POINT('Ctrl Pts',(-0.0437333382095171,-0.131918576929031,
0.592515889830509));
#34755=CARTESIAN_POINT('Ctrl Pts',(0.0865927525795457,-0.108705156320324,
0.600416101694915));
#34756=CARTESIAN_POINT('Ctrl Pts',(0.138357057429181,0.0131316590523252,
0.608316313559322));
#34757=CARTESIAN_POINT('Ctrl Pts',(0.0645961051971127,0.123054699232873,
0.616216525423729));
#34758=CARTESIAN_POINT('Ctrl Pts',(-0.0677700447892944,0.121335637135943,
0.624116737288135));
#34759=CARTESIAN_POINT('Ctrl Pts',(-0.116658230525945,0.0442240676066805,
0.629565658322354));
#34760=CARTESIAN_POINT('Ctrl Pts',(-0.117953914810415,0.00273174284681649,
0.63238117540177));
#34761=CARTESIAN_POINT('Ctrl Pts',(-0.117940203002297,4.7067652063935E-5,
0.632563288526384));
#34762=CARTESIAN_POINT('Ctrl Pts',(-0.11796202899481,1.53301186523688E-5,
0.592436711473616));
#34763=CARTESIAN_POINT('Ctrl Pts',(-0.11789197517919,-0.0379767160352311,
0.5950151495225));
#34764=CARTESIAN_POINT('Ctrl Pts',(-0.077400231210687,-0.114927628746102,
0.600228928637889));
#34765=CARTESIAN_POINT('Ctrl Pts',(0.0534615168199478,-0.12832174587234,
0.608078048819785));
#34766=CARTESIAN_POINT('Ctrl Pts',(0.136703270562712,-0.0252352939724056,
0.615984072019302));
#34767=CARTESIAN_POINT('Ctrl Pts',(0.0957529101571512,0.100776904302778,
0.623890095218819));
#34768=CARTESIAN_POINT('Ctrl Pts',(-0.0321870028708045,0.135235354440354,
0.631796118418337));
#34769=CARTESIAN_POINT('Ctrl Pts',(-0.109365567925802,0.0661098894434327,
0.637978323836602));
#34770=CARTESIAN_POINT('Ctrl Pts',(-0.117746468172191,0.0136055832811398,
0.641525188188362));
#34771=CARTESIAN_POINT('Ctrl Pts',(-0.117656000082187,8.43516556759457E-5,
0.642436711473616));
#34772=CARTESIAN_POINT('Origin',(0.,0.,-0.0924367114736152));
#34773=CARTESIAN_POINT('',(-0.117610072962214,5.33056148506657E-5,0.532563288526385));
#34774=CARTESIAN_POINT('',(-0.117697192808605,-9.79052972080175E-5,0.542436711473616));
#34775=CARTESIAN_POINT('',(-0.117775,-1.30487598617993E-14,-0.0924367114736152));
#34776=CARTESIAN_POINT('Ctrl Pts',(-0.117610072962214,5.330561485066E-5,
0.532563288526385));
#34777=CARTESIAN_POINT('Ctrl Pts',(-0.117515081084069,-0.02296700464597,
0.534113661277477));
#34778=CARTESIAN_POINT('Ctrl Pts',(-0.0998958154709599,-0.0852230040130838,
0.538297437983371));
#34779=CARTESIAN_POINT('Ctrl Pts',(0.000896453507092177,-0.13897594101512,
0.545114618644068));
#34780=CARTESIAN_POINT('Ctrl Pts',(0.116888066275103,-0.0751817515916976,
0.553014830508475));
#34781=CARTESIAN_POINT('Ctrl Pts',(0.126832290918542,0.0568215257651788,
0.560915042372882));
#34782=CARTESIAN_POINT('Ctrl Pts',(0.0217071709283622,0.137273138451102,
0.568815254237287));
#34783=CARTESIAN_POINT('Ctrl Pts',(-0.0923030266130234,0.097000942567024,
0.576031336288457));
#34784=CARTESIAN_POINT('Ctrl Pts',(-0.117490655726745,0.0287559098676526,
0.580614014384821));
#34785=CARTESIAN_POINT('Ctrl Pts',(-0.117743952026517,-0.000104311439111965,
0.582563288526385));
#34786=CARTESIAN_POINT('Ctrl Pts',(-0.117697192808605,-9.79052972080122E-5,
0.542436711473616));
#34787=CARTESIAN_POINT('Ctrl Pts',(-0.11779135888071,-0.011920519912767,
0.543234428723626));
#34788=CARTESIAN_POINT('Ctrl Pts',(-0.110735559311442,-0.0626905594030618,
0.546667487040141));
#34789=CARTESIAN_POINT('Ctrl Pts',(-0.0379577228913647,-0.133730383672961,
0.552735886423163));
#34790=CARTESIAN_POINT('Ctrl Pts',(0.0913424031974019,-0.104791076063462,
0.56064190962268));
#34791=CARTESIAN_POINT('Ctrl Pts',(0.137659831668342,0.0193487722984857,
0.568547932822197));
#34792=CARTESIAN_POINT('Ctrl Pts',(0.0589161298691768,0.125910658348106,
0.576453956021715));
#34793=CARTESIAN_POINT('Ctrl Pts',(-0.0733516660922674,0.11808529682354,
0.584359979221232));
#34794=CARTESIAN_POINT('Ctrl Pts',(-0.117576903938907,0.0405212291720611,
0.589687564371866));
#34795=CARTESIAN_POINT('Ctrl Pts',(-0.117963574998021,0.000853768751192661,
0.592379808455994));
#34796=CARTESIAN_POINT('Ctrl Pts',(-0.11796202899481,1.53301186523688E-5,
0.592436711473616));
#34797=CARTESIAN_POINT('Origin',(0.,0.,-0.0924367114736152));
#34798=CARTESIAN_POINT('',(-0.117931139389423,5.50751932371175E-5,0.482563288526385));
#34799=CARTESIAN_POINT('',(-0.117634119017629,7.2868354416035E-5,0.492436711473616));
#34800=CARTESIAN_POINT('',(-0.117775,-1.30487598617993E-14,-0.0924367114736152));
#34801=CARTESIAN_POINT('Ctrl Pts',(-0.117931139389423,5.50751932371233E-5,
0.482563288526385));
#34802=CARTESIAN_POINT('Ctrl Pts',(-0.117723480179333,-0.0355774509071747,
0.48497990421533));
#34803=CARTESIAN_POINT('Ctrl Pts',(-0.0815990427908323,-0.11040399129502,
0.490029923859077));
#34804=CARTESIAN_POINT('Ctrl Pts',(0.0454314893010671,-0.131343426138561,
0.497713347457628));
#34805=CARTESIAN_POINT('Ctrl Pts',(0.134828208757446,-0.0337115697229769,
0.505613559322033));
#34806=CARTESIAN_POINT('Ctrl Pts',(0.10190123992053,0.0945053073249706,
0.513513771186441));
#34807=CARTESIAN_POINT('Ctrl Pts',(-0.0234762303627364,0.136981686432473,
0.521413983050847));
#34808=CARTESIAN_POINT('Ctrl Pts',(-0.107129919570411,0.0712336270252472,
0.527763822164162));
#34809=CARTESIAN_POINT('Ctrl Pts',(-0.117676430661069,0.0161344153441048,
0.531480257322675));
#34810=CARTESIAN_POINT('Ctrl Pts',(-0.117610072962214,5.330561485066E-5,
0.532563288526385));
#34811=CARTESIAN_POINT('Ctrl Pts',(-0.117634119017629,7.28683544160419E-5,
0.492436711473616));
#34812=CARTESIAN_POINT('Ctrl Pts',(-0.117494141600147,-0.0244488239796579,
0.494089048991258));
#34813=CARTESIAN_POINT('Ctrl Pts',(-0.0980773705094754,-0.0882836093782272,
0.498376727575405));
#34814=CARTESIAN_POINT('Ctrl Pts',(0.00633962999064621,-0.138868330932566,
0.505299747226058));
#34815=CARTESIAN_POINT('Ctrl Pts',(0.119823436886959,-0.0704765792090683,
0.513205770425575));
#34816=CARTESIAN_POINT('Ctrl Pts',(0.124450111907394,0.0619416975118724,
0.521111793625093));
#34817=CARTESIAN_POINT('Ctrl Pts',(0.0160164158031762,0.138087213996209,
0.52901781682461));
#34818=CARTESIAN_POINT('Ctrl Pts',(-0.0945587588515482,0.0937580907599652,
0.536126122774119));
#34819=CARTESIAN_POINT('Ctrl Pts',(-0.117480271566393,0.0271367046984328,
0.54059908765712));
#34820=CARTESIAN_POINT('Ctrl Pts',(-0.117697192808605,-9.79052972080122E-5,
0.542436711473616));
#34821=CARTESIAN_POINT('Origin',(0.,0.,-0.0924367114736152));
#34822=CARTESIAN_POINT('',(-0.117758961667293,-0.000104950384427651,0.432563288526384));
#34823=CARTESIAN_POINT('',(-0.117952286276812,3.39956489144189E-5,0.442436711473616));
#34824=CARTESIAN_POINT('',(-0.117775,-1.30487598617993E-14,-0.0924367114736152));
#34825=CARTESIAN_POINT('Ctrl Pts',(-0.117758961667293,-0.000104950384427652,
0.432563288526384));
#34826=CARTESIAN_POINT('Ctrl Pts',(-0.117844817924839,-0.00971740507401162,
0.43321274319838));
#34827=CARTESIAN_POINT('Ctrl Pts',(-0.11238834839588,-0.0582101957930696,
0.436495601825179));
#34828=CARTESIAN_POINT('Ctrl Pts',(-0.045454021205161,-0.13133563022352,
0.44241186440678));
#34829=CARTESIAN_POINT('Ctrl Pts',(0.085164376794762,-0.109827795821861,
0.450312076271186));
#34830=CARTESIAN_POINT('Ctrl Pts',(0.138516891217783,0.0113219546585138,
0.458212288135593));
#34831=CARTESIAN_POINT('Ctrl Pts',(0.0661991384108791,0.12219979494085,
0.4661125));
#34832=CARTESIAN_POINT('Ctrl Pts',(-0.0661781734963363,0.122211149911198,
0.474012711864406));
#34833=CARTESIAN_POINT('Ctrl Pts',(-0.116387669202521,0.0452586237679377,
0.479496308039868));
#34834=CARTESIAN_POINT('Ctrl Pts',(-0.117949767953432,0.00325157581050499,
0.482346500260528));
#34835=CARTESIAN_POINT('Ctrl Pts',(-0.117931139389423,5.50751932371233E-5,
0.482563288526385));
#34836=CARTESIAN_POINT('Ctrl Pts',(-0.117952286276812,3.39956489144155E-5,
0.442436711473616));
#34837=CARTESIAN_POINT('Ctrl Pts',(-0.117810336120504,-0.0369130001778165,
0.444943669258889));
#34838=CARTESIAN_POINT('Ctrl Pts',(-0.0792807483010678,-0.11295446192069,
0.450085968110668));
#34839=CARTESIAN_POINT('Ctrl Pts',(0.0499845850166584,-0.129715633233345,
0.457863608028953));
#34840=CARTESIAN_POINT('Ctrl Pts',(0.135973695209673,-0.0289094872912353,
0.465769631228471));
#34841=CARTESIAN_POINT('Ctrl Pts',(0.0984334954810092,0.0981603342078928,
0.473675654427988));
#34842=CARTESIAN_POINT('Ctrl Pts',(-0.0285315135918273,0.136053507770195,
0.481581677627505));
#34843=CARTESIAN_POINT('Ctrl Pts',(-0.108458155672614,0.0682577387762276,
0.487835363309382));
#34844=CARTESIAN_POINT('Ctrl Pts',(-0.117717393951882,0.0146612380616908,
0.491453707924752));
#34845=CARTESIAN_POINT('Ctrl Pts',(-0.117634119017629,7.28683544160419E-5,
0.492436711473616));
#34846=CARTESIAN_POINT('Origin',(0.,0.,-0.0924367114736152));
#34847=CARTESIAN_POINT('',(-0.117603494801586,4.59807059966066E-5,0.382563288526384));
#34848=CARTESIAN_POINT('',(-0.117726185906756,-0.000103034036682964,0.392436711473616));
#34849=CARTESIAN_POINT('',(-0.117775,-1.30487598617993E-14,-0.0924367114736152));
#34850=CARTESIAN_POINT('Ctrl Pts',(-0.117603494801586,4.59807059966007E-5,
0.382563288526384));
#34851=CARTESIAN_POINT('Ctrl Pts',(-0.117523654559104,-0.0224626175592834,
0.384078986136234));
#34852=CARTESIAN_POINT('Ctrl Pts',(-0.100492247037195,-0.0841899886309759,
0.388228087700885));
#34853=CARTESIAN_POINT('Ctrl Pts',(-0.000920295459793275,-0.138975785179272,
0.395010593220339));
#34854=CARTESIAN_POINT('Ctrl Pts',(0.115895314901344,-0.0767032710765764,
0.402910805084745));
#34855=CARTESIAN_POINT('Ctrl Pts',(0.127564216682018,0.0551587384938402,
0.410811016949152));
#34856=CARTESIAN_POINT('Ctrl Pts',(0.0234997298595607,0.136977656960748,
0.418711228813559));
#34857=CARTESIAN_POINT('Ctrl Pts',(-0.0915774899741938,0.0980128855194841,
0.42596198600597));
#34858=CARTESIAN_POINT('Ctrl Pts',(-0.117496688612794,0.0292591044291153,
0.430579339243578));
#34859=CARTESIAN_POINT('Ctrl Pts',(-0.117758961667293,-0.000104950384427652,
0.432563288526384));
#34860=CARTESIAN_POINT('Ctrl Pts',(-0.117726185906756,-0.000103034036682944,
0.392436711473616));
#34861=CARTESIAN_POINT('Ctrl Pts',(-0.117818125179144,-0.0108595471866994,
0.393162948460015));
#34862=CARTESIAN_POINT('Ctrl Pts',(-0.111550100869322,-0.0605437012261054,
0.39652452651292));
#34863=CARTESIAN_POINT('Ctrl Pts',(-0.0415471952570256,-0.13265909245389,
0.40252144563233));
#34864=CARTESIAN_POINT('Ctrl Pts',(0.0884857325734624,-0.107214175253801,
0.410427468831849));
#34865=CARTESIAN_POINT('Ctrl Pts',(0.138131189387156,0.0156326185555932,
0.418333492031365));
#34866=CARTESIAN_POINT('Ctrl Pts',(0.062287297122381,0.124277499418049,
0.426239515230884));
#34867=CARTESIAN_POINT('Ctrl Pts',(-0.0701433255283678,0.120018824057881,
0.4341455384304));
#34868=CARTESIAN_POINT('Ctrl Pts',(-0.117063601095489,0.0426502166584235,
0.439544603844645));
#34869=CARTESIAN_POINT('Ctrl Pts',(-0.117959555656036,0.00192608038356173,
0.442308328192384));
#34870=CARTESIAN_POINT('Ctrl Pts',(-0.117952286276812,3.39956489144155E-5,
0.442436711473616));
#34871=CARTESIAN_POINT('Origin',(0.,0.,-0.0924367114736152));
#34872=CARTESIAN_POINT('',(-0.117920926539219,6.26243704048756E-5,0.332563288526384));
#34873=CARTESIAN_POINT('',(-0.117615878293784,5.9477676878486E-5,0.342436711473616));
#34874=CARTESIAN_POINT('',(-0.117775,-1.30487598617993E-14,-0.0924367114736152));
#34875=CARTESIAN_POINT('Ctrl Pts',(-0.117920926539219,6.26243704048737E-5,
0.332563288526384));
#34876=CARTESIAN_POINT('Ctrl Pts',(-0.117693603628949,-0.0350666637837455,
0.334945229074087));
#34877=CARTESIAN_POINT('Ctrl Pts',(-0.0824632530796663,-0.109429893167014,
0.339960573576592));
#34878=CARTESIAN_POINT('Ctrl Pts',(0.0437107063235388,-0.131926077644361,
0.347609322033898));
#34879=CARTESIAN_POINT('Ctrl Pts',(0.134376016486386,-0.0354711432460098,
0.355509533898305));
#34880=CARTESIAN_POINT('Ctrl Pts',(0.103127892463174,0.0931651952503325,
0.363409745762711));
#34881=CARTESIAN_POINT('Ctrl Pts',(-0.0216836207666979,0.137276860396698,
0.371309957627119));
#34882=CARTESIAN_POINT('Ctrl Pts',(-0.106651080731,0.0722748925449633,0.377694471881676));
#34883=CARTESIAN_POINT('Ctrl Pts',(-0.117662370625513,0.0166442803494234,
0.381445582181431));
#34884=CARTESIAN_POINT('Ctrl Pts',(-0.117603494801586,4.59807059966007E-5,
0.382563288526384));
#34885=CARTESIAN_POINT('Ctrl Pts',(-0.117615878293784,5.94776768784704E-5,
0.342436711473616));
#34886=CARTESIAN_POINT('Ctrl Pts',(-0.11750760701874,-0.0234105356203755,
0.344017568727647));
#34887=CARTESIAN_POINT('Ctrl Pts',(-0.0993568477409689,-0.0861600913990265,
0.348233767048184));
#34888=CARTESIAN_POINT('Ctrl Pts',(0.00259563734382704,-0.138988729439456,
0.355085306435226));
#34889=CARTESIAN_POINT('Ctrl Pts',(0.117881001348277,-0.0736795342380946,
0.362991329634744));
#34890=CARTESIAN_POINT('Ctrl Pts',(0.12607389627645,0.0585660048329233,
0.370897352834261));
#34891=CARTESIAN_POINT('Ctrl Pts',(0.0197312453245754,0.137605531147394,
0.378803376033779));
#34892=CARTESIAN_POINT('Ctrl Pts',(-0.0931217327741457,0.0958562111818821,
0.385983162246897));
#34893=CARTESIAN_POINT('Ctrl Pts',(-0.117484499455465,0.0281732773148422,
0.39052760739351));
#34894=CARTESIAN_POINT('Ctrl Pts',(-0.117726185906756,-0.000103034036682944,
0.392436711473616));
#34895=CARTESIAN_POINT('Origin',(0.,0.,-0.0924367114736152));
#34896=CARTESIAN_POINT('',(-0.117774170260593,-0.000104886777209015,0.282563288526384));
#34897=CARTESIAN_POINT('',(-0.11793628481875,5.1384428605368E-5,0.292436711473616));
#34898=CARTESIAN_POINT('',(-0.117775,-1.30487598617993E-14,-0.0924367114736152));
#34899=CARTESIAN_POINT('Ctrl Pts',(-0.117774170260593,-0.00010488677720901,
0.282563288526384));
#34900=CARTESIAN_POINT('Ctrl Pts',(-0.117856360533384,-0.0092011162257308,
0.283178068057138));
#34901=CARTESIAN_POINT('Ctrl Pts',(-0.112752995425492,-0.057169777637724,
0.286426251542693));
#34902=CARTESIAN_POINT('Ctrl Pts',(-0.0471669369944997,-0.130730240818604,
0.292307838983051));
#34903=CARTESIAN_POINT('Ctrl Pts',(0.0837214480778729,-0.110931667893667,
0.300208050847457));
#34904=CARTESIAN_POINT('Ctrl Pts',(0.138653055169421,0.00951031556331505,
0.308108262711865));
#34905=CARTESIAN_POINT('Ctrl Pts',(0.0677908594821406,0.121324009085596,
0.316008474576271));
#34906=CARTESIAN_POINT('Ctrl Pts',(-0.0645749936433688,0.123065779182871,
0.323908686440678));
#34907=CARTESIAN_POINT('Ctrl Pts',(-0.116109941121323,0.0462937466385656,
0.329426957757382));
#34908=CARTESIAN_POINT('Ctrl Pts',(-0.117944925204334,0.00377125198361699,
0.332311825119284));
#34909=CARTESIAN_POINT('Ctrl Pts',(-0.117920926539219,6.26243704048737E-5,
0.332563288526384));
#34910=CARTESIAN_POINT('Ctrl Pts',(-0.11793628481875,5.13844286053676E-5,
0.292436711473616));
#34911=CARTESIAN_POINT('Ctrl Pts',(-0.117738942084994,-0.0358551097426003,
0.294872188995279));
#34912=CARTESIAN_POINT('Ctrl Pts',(-0.0811119992076199,-0.110963296543085,
0.299943007583447));
#34913=CARTESIAN_POINT('Ctrl Pts',(0.046471358419155,-0.131015331511595,
0.307649167238122));
#34914=CARTESIAN_POINT('Ctrl Pts',(0.135145386671506,-0.0325626888604762,
0.315555190437639));
#34915=CARTESIAN_POINT('Ctrl Pts',(0.101042606300054,0.0954724879559945,
0.323461213637157));
#34916=CARTESIAN_POINT('Ctrl Pts',(-0.0248553070174182,0.136772869961425,
0.331367236836674));
#34917=CARTESIAN_POINT('Ctrl Pts',(-0.107513748550757,0.0704052555566997,
0.33769240278216));
#34918=CARTESIAN_POINT('Ctrl Pts',(-0.117688098797311,0.0157147489149463,
0.341382227661141));
#34919=CARTESIAN_POINT('Ctrl Pts',(-0.117615878293784,5.94776768784704E-5,
0.342436711473616));
#34920=CARTESIAN_POINT('Origin',(0.,0.,-0.0924367114736152));
#34921=CARTESIAN_POINT('',(-0.117597921122191,3.83764452643825E-5,0.232563288526384));
#34922=CARTESIAN_POINT('',(-0.117756807889117,-0.000105309437279225,0.242436711473616));
#34923=CARTESIAN_POINT('',(-0.117775,-1.30487598617993E-14,-0.0924367114736152));
#34924=CARTESIAN_POINT('Ctrl Pts',(-0.117597921122191,3.83764452643858E-5,
0.232563288526384));
#34925=CARTESIAN_POINT('Ctrl Pts',(-0.117532990113526,-0.0219578937617309,
0.234044310994991));
#34926=CARTESIAN_POINT('Ctrl Pts',(-0.101078828998682,-0.0831558954107903,
0.238158737418399));
#34927=CARTESIAN_POINT('Ctrl Pts',(-0.00273688716624997,-0.138951881091211,
0.24490656779661));
#34928=CARTESIAN_POINT('Ctrl Pts',(0.114882759277182,-0.0782116834669906,
0.252806779661017));
#34929=CARTESIAN_POINT('Ctrl Pts',(0.128274344207101,0.0534865256689417,
0.260706991525423));
#34930=CARTESIAN_POINT('Ctrl Pts',(0.0252882731449639,0.136658768658679,
0.26860720338983));
#34931=CARTESIAN_POINT('Ctrl Pts',(-0.090841176153826,0.099022467675047,
0.275892635723484));
#34932=CARTESIAN_POINT('Ctrl Pts',(-0.117504299056729,0.0297625209893518,
0.280544664102335));
#34933=CARTESIAN_POINT('Ctrl Pts',(-0.117774170260593,-0.00010488677720901,
0.282563288526384));
#34934=CARTESIAN_POINT('Ctrl Pts',(-0.117756807889117,-0.000105309437279212,
0.242436711473616));
#34935=CARTESIAN_POINT('Ctrl Pts',(-0.117843399042527,-0.00979668321532341,
0.243091468196405));
#34936=CARTESIAN_POINT('Ctrl Pts',(-0.112329964982903,-0.058397845463228,
0.246381565985699));
#34937=CARTESIAN_POINT('Ctrl Pts',(-0.0451064993838265,-0.131491474848312,
0.252307004841499));
#34938=CARTESIAN_POINT('Ctrl Pts',(0.0855648107118161,-0.1095594241143,
0.260213028041017));
#34939=CARTESIAN_POINT('Ctrl Pts',(0.138502247321704,0.0119051136596435,
0.268119051240535));
#34940=CARTESIAN_POINT('Ctrl Pts',(0.0656132363391791,0.122554100141606,
0.276025074440052));
#34941=CARTESIAN_POINT('Ctrl Pts',(-0.066884052510702,0.121865203254083,
0.283931097639569));
#34942=CARTESIAN_POINT('Ctrl Pts',(-0.1165204945288,0.0447817101515102,
0.289401643317424));
#34943=CARTESIAN_POINT('Ctrl Pts',(-0.117952479432728,0.00299799310969985,
0.292236847928773));
#34944=CARTESIAN_POINT('Ctrl Pts',(-0.11793628481875,5.13844286053676E-5,
0.292436711473616));
#34945=CARTESIAN_POINT('Origin',(0.,0.,-0.0924367114736152));
#34946=CARTESIAN_POINT('',(-0.117909687164366,6.9664588846411E-5,0.182563288526384));
#34947=CARTESIAN_POINT('',(-0.117601649275994,4.45452448404882E-5,0.192436711473616));
#34948=CARTESIAN_POINT('',(-0.117775,-1.30487598617993E-14,-0.0924367114736152));
#34949=CARTESIAN_POINT('Ctrl Pts',(-0.117909687164366,6.96645888464118E-5,
0.182563288526384));
#34950=CARTESIAN_POINT('Ctrl Pts',(-0.11766595726848,-0.0345569219122136,
0.184910553932844));
#34951=CARTESIAN_POINT('Ctrl Pts',(-0.0833160382623138,-0.10845204978507,
0.189891223294105));
#34952=CARTESIAN_POINT('Ctrl Pts',(0.0419824540321544,-0.132486185591528,
0.197505296610169));
#34953=CARTESIAN_POINT('Ctrl Pts',(0.133900861976353,-0.0372246554226585,
0.205405508474576));
#34954=CARTESIAN_POINT('Ctrl Pts',(0.10433692245731,0.0918091630494651,
0.213305720338983));
#34955=CARTESIAN_POINT('Ctrl Pts',(-0.0198873058616059,0.137548576426424,
0.221205932203389));
#34956=CARTESIAN_POINT('Ctrl Pts',(-0.10616324692175,0.0733158722115256,
0.22762512159919));
#34957=CARTESIAN_POINT('Ctrl Pts',(-0.117648443848114,0.0171536431540524,
0.231410907040188));
#34958=CARTESIAN_POINT('Ctrl Pts',(-0.117597921122191,3.83764452643858E-5,
0.232563288526384));
#34959=CARTESIAN_POINT('Ctrl Pts',(-0.117601649275994,4.45452448404882E-5,
0.192436711473616));
#34960=CARTESIAN_POINT('Ctrl Pts',(-0.11752478280801,-0.0223710360060294,
0.193946088464036));
#34961=CARTESIAN_POINT('Ctrl Pts',(-0.100593880386987,-0.0840313287987434,
0.198090806520963));
#34962=CARTESIAN_POINT('Ctrl Pts',(-0.00115024004832317,-0.139008205490464,
0.204870865644395));
#34963=CARTESIAN_POINT('Ctrl Pts',(0.115852970087698,-0.0768289890996742,
0.212776888843912));
#34964=CARTESIAN_POINT('Ctrl Pts',(0.127606135899372,0.055147786219953,
0.22068291204343));
#34965=CARTESIAN_POINT('Ctrl Pts',(0.0234317475993789,0.137023930205902,
0.228588935242947));
#34966=CARTESIAN_POINT('Ctrl Pts',(-0.0916394876575414,0.0979452740831826,
0.235840201719676));
#34967=CARTESIAN_POINT('Ctrl Pts',(-0.11749487688974,0.0292102859676066,
0.240456127129899));
#34968=CARTESIAN_POINT('Ctrl Pts',(-0.117756807889117,-0.000105309437279212,
0.242436711473616));
#34969=CARTESIAN_POINT('Origin',(0.,0.,-0.0924367114736152));
#34970=CARTESIAN_POINT('',(-0.117789487689835,-0.000104112672946744,0.132563288526384));
#34971=CARTESIAN_POINT('',(-0.117915129103549,6.69430946510577E-5,0.142436711473616));
#34972=CARTESIAN_POINT('',(-0.117775,-1.30487598617993E-14,-0.0924367114736152));
#34973=CARTESIAN_POINT('Ctrl Pts',(-0.117789487689835,-0.000104112672946739,
0.132563288526384));
#34974=CARTESIAN_POINT('Ctrl Pts',(-0.117867447370286,-0.00868443076951223,
0.133143392915894));
#34975=CARTESIAN_POINT('Ctrl Pts',(-0.113109713752316,-0.056129702894726,
0.136356901260207));
#34976=CARTESIAN_POINT('Ctrl Pts',(-0.0488717923313075,-0.130102508888041,
0.142203813559322));
#34977=CARTESIAN_POINT('Ctrl Pts',(0.0822642127117346,-0.112016585630158,
0.150104025423729));
#34978=CARTESIAN_POINT('Ctrl Pts',(0.138765526166673,0.00769705224861128,
0.158004237288135));
#34979=CARTESIAN_POINT('Ctrl Pts',(0.0693709963376258,0.12042749084372,
0.165904449152542));
#34980=CARTESIAN_POINT('Ctrl Pts',(-0.0629607791409001,0.123899379163224,
0.173804661016949));
#34981=CARTESIAN_POINT('Ctrl Pts',(-0.115824984153554,0.0473294249038356,
0.179357607474896));
#34982=CARTESIAN_POINT('Ctrl Pts',(-0.117939398554652,0.00429074720192216,
0.182277149978042));
#34983=CARTESIAN_POINT('Ctrl Pts',(-0.117909687164366,6.96645888464118E-5,
0.182563288526384));
#34984=CARTESIAN_POINT('Ctrl Pts',(-0.117915129103549,6.69430946510529E-5,
0.142436711473616));
#34985=CARTESIAN_POINT('Ctrl Pts',(-0.117677363460081,-0.0348022339441635,
0.144800708731668));
#34986=CARTESIAN_POINT('Ctrl Pts',(-0.0828943760199795,-0.108955331093341,
0.149800047056226));
#34987=CARTESIAN_POINT('Ctrl Pts',(0.0429243879661372,-0.132219897211806,
0.15743472644729));
#34988=CARTESIAN_POINT('Ctrl Pts',(0.134218946443888,-0.0361922458912883,
0.165340749646808));
#34989=CARTESIAN_POINT('Ctrl Pts',(0.103578348063976,0.0927153171784346,
0.173246772846325));
#34990=CARTESIAN_POINT('Ctrl Pts',(-0.0211610525014389,0.137392918706172,
0.181152796045843));
#34991=CARTESIAN_POINT('Ctrl Pts',(-0.106531690673769,0.0725519877028229,
0.187549442254939));
#34992=CARTESIAN_POINT('Ctrl Pts',(-0.117658990074321,0.0167661061227608,
0.19131074739753));
#34993=CARTESIAN_POINT('Ctrl Pts',(-0.117601649275994,4.45452448404882E-5,
0.192436711473616));
#34994=CARTESIAN_POINT('Origin',(0.,0.,-0.0924367114736152));
#34995=CARTESIAN_POINT('',(-0.117593357284741,3.06645980543279E-5,0.0825632885263843));
#34996=CARTESIAN_POINT('',(-0.117788324723582,-0.000104604007662518,0.0924367114736157));
#34997=CARTESIAN_POINT('',(-0.117775,-1.30487598617993E-14,-0.0924367114736152));
#34998=CARTESIAN_POINT('Ctrl Pts',(-0.117593357284741,3.06645980543228E-5,
0.0825632885263843));
#34999=CARTESIAN_POINT('Ctrl Pts',(-0.11754301899516,-0.021452746571923,
0.0840096358537477));
#35000=CARTESIAN_POINT('Ctrl Pts',(-0.101655671713158,-0.0821210291969121,
0.0880893871359134));
#35001=CARTESIAN_POINT('Ctrl Pts',(-0.0045529857407016,-0.138904079109577,
0.0948025423728811));
#35002=CARTESIAN_POINT('Ctrl Pts',(0.113850559027731,-0.0797068119457511,
0.102702754237288));
#35003=CARTESIAN_POINT('Ctrl Pts',(0.12896255920279,0.0518052156568057,
0.110602966101695));
#35004=CARTESIAN_POINT('Ctrl Pts',(0.0270724914422277,0.136316505597261,
0.118503177966102));
#35005=CARTESIAN_POINT('Ctrl Pts',(-0.0900940209439092,0.100029588267392,
0.125823285440998));
#35006=CARTESIAN_POINT('Ctrl Pts',(-0.117513546702531,0.0302662202125134,
0.130509988961092));
#35007=CARTESIAN_POINT('Ctrl Pts',(-0.117789487689835,-0.000104112672946739,
0.132563288526384));
#35008=CARTESIAN_POINT('Ctrl Pts',(-0.117788324723582,-0.00010460400766255,
0.0924367114736157));
#35009=CARTESIAN_POINT('Ctrl Pts',(-0.117866887107117,-0.00873205619380746,
0.093019987932794));
#35010=CARTESIAN_POINT('Ctrl Pts',(-0.113075788730874,-0.0562533105277103,
0.0962386054584782));
#35011=CARTESIAN_POINT('Ctrl Pts',(-0.0486330432543111,-0.130228357167641,
0.102092564050668));
#35012=CARTESIAN_POINT('Ctrl Pts',(0.0825817545836372,-0.111825131042891,
0.109998587250186));
#35013=CARTESIAN_POINT('Ctrl Pts',(0.138772738128538,0.00816897019039422,
0.117904610449703));
#35014=CARTESIAN_POINT('Ctrl Pts',(0.0688915313895657,0.120741708772585,
0.12581063364922));
#35015=CARTESIAN_POINT('Ctrl Pts',(-0.0635762130827019,0.123623095373164,
0.133716656848738));
#35016=CARTESIAN_POINT('Ctrl Pts',(-0.115947056638979,0.0469156369390546,
0.139258682790203));
#35017=CARTESIAN_POINT('Ctrl Pts',(-0.117942420266852,0.00406928923237253,
0.142165367665162));
#35018=CARTESIAN_POINT('Ctrl Pts',(-0.117915129103549,6.69430946510529E-5,
0.142436711473616));
#35019=CARTESIAN_POINT('Origin',(0.,0.,-0.0924367114736152));
#35020=CARTESIAN_POINT('',(-0.117896184020664,8.43438525025023E-5,0.0325632885263842));
#35021=CARTESIAN_POINT('',(-0.117591431864639,2.92794590778037E-5,0.0424367114736158));
#35022=CARTESIAN_POINT('',(-0.117775,-1.30487598617993E-14,-0.0924367114736152));
#35023=CARTESIAN_POINT('Ctrl Pts',(-0.117896184020664,8.43438525024954E-5,
0.0325632885263842));
#35024=CARTESIAN_POINT('Ctrl Pts',(-0.117638881596538,-0.0340384192378303,
0.0348758787916007));
#35025=CARTESIAN_POINT('Ctrl Pts',(-0.0841595758608773,-0.107483448399194,
0.0398218730116195));
#35026=CARTESIAN_POINT('Ctrl Pts',(0.040248222246223,-0.133016439153077,
0.0474012711864405));
#35027=CARTESIAN_POINT('Ctrl Pts',(0.133402197487182,-0.0389756054074351,
0.0553014830508473));
#35028=CARTESIAN_POINT('Ctrl Pts',(0.105528454455023,0.0904394425945055,
0.0632016949152541));
#35029=CARTESIAN_POINT('Ctrl Pts',(-0.0180877669633101,0.137795734956694,
0.0711019067796609));
#35030=CARTESIAN_POINT('Ctrl Pts',(-0.105666299933038,0.0743567679416689,
0.0775557713167041));
#35031=CARTESIAN_POINT('Ctrl Pts',(-0.117634671289428,0.017662685017247,
0.0813762318989454));
#35032=CARTESIAN_POINT('Ctrl Pts',(-0.117593357284741,3.06645980543228E-5,
0.0825632885263843));
#35033=CARTESIAN_POINT('Ctrl Pts',(-0.117591431864639,2.92794590778002E-5,
0.0424367114736158));
#35034=CARTESIAN_POINT('Ctrl Pts',(-0.11754501123181,-0.0213296840770181,
0.0438746082004259));
#35035=CARTESIAN_POINT('Ctrl Pts',(-0.101789620521557,-0.0818995216066154,
0.0479478459937417));
#35036=CARTESIAN_POINT('Ctrl Pts',(-0.00489492837772915,-0.138925734589418,
0.0546564248535634));
#35037=CARTESIAN_POINT('Ctrl Pts',(0.113740629398734,-0.0799231888543136,
0.062562448053081));
#35038=CARTESIAN_POINT('Ctrl Pts',(0.129045816271948,0.0516898037714297,
0.0704684712525983));
#35039=CARTESIAN_POINT('Ctrl Pts',(0.0271151839788463,0.136342686033388,
0.0783744944521158));
#35040=CARTESIAN_POINT('Ctrl Pts',(-0.0901114389347958,0.100024405106452,
0.0856972411924549));
#35041=CARTESIAN_POINT('Ctrl Pts',(-0.117511929055312,0.0302482226905713,
0.0903846468662882));
#35042=CARTESIAN_POINT('Ctrl Pts',(-0.117788324723582,-0.00010460400766255,
0.0924367114736157));
#35043=CARTESIAN_POINT('Origin',(0.,0.,0.95));
#35044=CARTESIAN_POINT('',(-0.143203996033626,-2.30855198111598E-5,0.907000235762439));
#35045=CARTESIAN_POINT('Ctrl Pts',(-0.0334019664626807,0.112939183906322,
0.932225));
#35046=CARTESIAN_POINT('Ctrl Pts',(-0.0250603177854857,0.115799805022824,
0.931847596094215));
#35047=CARTESIAN_POINT('Ctrl Pts',(-0.0164278988467134,0.117636476238285,
0.931473565046676));
#35048=CARTESIAN_POINT('Ctrl Pts',(-0.00767106646971057,0.118512486061759,
0.931100514589335));
#35049=CARTESIAN_POINT('Ctrl Pts',(-0.00420439075546036,0.118859282922739,
0.930952830483373));
#35050=CARTESIAN_POINT('Ctrl Pts',(-0.000716143526927236,0.119054988716296,
0.930805221836912));
#35051=CARTESIAN_POINT('Ctrl Pts',(0.00277797710115842,0.119101360153194,
0.930657787404542));
#35052=CARTESIAN_POINT('Ctrl Pts',(0.00969984845123832,0.119193222213692,
0.930365719018224));
#35053=CARTESIAN_POINT('Ctrl Pts',(0.0166142532722655,0.118700388967513,
0.930075608100973));
#35054=CARTESIAN_POINT('Ctrl Pts',(0.02344427759502,0.117646722051856,0.929786344238933));
#35055=CARTESIAN_POINT('Ctrl Pts',(0.0272709497102665,0.117056381869396,
0.929624277765593));
#35056=CARTESIAN_POINT('Ctrl Pts',(0.0310712076772195,0.116289673696229,
0.929462477186978));
#35057=CARTESIAN_POINT('Ctrl Pts',(0.0348314922052066,0.115348424870015,
0.929300747212246));
#35058=CARTESIAN_POINT('Ctrl Pts',(0.0378910930422447,0.114582566415658,
0.929169153668624));
#35059=CARTESIAN_POINT('Ctrl Pts',(0.04092399616764,0.113700812218856,0.929037612549819));
#35060=CARTESIAN_POINT('Ctrl Pts',(0.0439095212807944,0.11270886835725,
0.928906608402292));
#35061=CARTESIAN_POINT('Ctrl Pts',(0.0525514734098646,0.10983757066528,
0.928527401553001));
#35062=CARTESIAN_POINT('Ctrl Pts',(0.0608263773706973,0.106040058117234,
0.928151455604188));
#35063=CARTESIAN_POINT('Ctrl Pts',(0.0685605494008651,0.101344813008116,
0.927776330408337));
#35064=CARTESIAN_POINT('Ctrl Pts',(0.072435687838791,0.0989923020054058,
0.927588377249316));
#35065=CARTESIAN_POINT('Ctrl Pts',(0.0761749070710193,0.0964136602636579,
0.92740063013395));
#35066=CARTESIAN_POINT('Ctrl Pts',(0.0797540201577765,0.0936080366646606,
0.927212782134414));
#35067=CARTESIAN_POINT('Ctrl Pts',(0.0820668650566089,0.091795025432075,
0.927091393601291));
#35068=CARTESIAN_POINT('Ctrl Pts',(0.0843049421929101,0.089893314502136,
0.926970374334797));
#35069=CARTESIAN_POINT('Ctrl Pts',(0.0864667806566824,0.087910346105634,
0.926849671848167));
#35070=CARTESIAN_POINT('Ctrl Pts',(0.0931618700565369,0.0817692070177022,
0.9264758631884));
#35071=CARTESIAN_POINT('Ctrl Pts',(0.0991298287989589,0.0748505421836024,
0.926105008552812));
#35072=CARTESIAN_POINT('Ctrl Pts',(0.104322127839002,0.0673319773813505,
0.925734762248716));
#35073=CARTESIAN_POINT('Ctrl Pts',(0.106370940812892,0.0643652505050492,
0.925588667922192));
#35074=CARTESIAN_POINT('Ctrl Pts',(0.108298617033319,0.0613046783141235,
0.925442668312145));
#35075=CARTESIAN_POINT('Ctrl Pts',(0.110100560923862,0.0581597986785966,
0.925296619306966));
#35076=CARTESIAN_POINT('Ctrl Pts',(0.11158855048605,0.0555628542917283,
0.925176016553231));
#35077=CARTESIAN_POINT('Ctrl Pts',(0.112988026000293,0.0529128751968171,
0.925055591079489));
#35078=CARTESIAN_POINT('Ctrl Pts',(0.114293875604956,0.0502227205878152,
0.92493557115538));
#35079=CARTESIAN_POINT('Ctrl Pts',(0.118434599880109,0.0416924974643938,
0.924554999448279));
#35080=CARTESIAN_POINT('Ctrl Pts',(0.121649070098747,0.0327401005258095,
0.924177564198185));
#35081=CARTESIAN_POINT('Ctrl Pts',(0.123868271499824,0.0235442585075687,
0.923800796649243));
#35082=CARTESIAN_POINT('Ctrl Pts',(0.124741985203477,0.0199237970280188,
0.923652460869335));
#35083=CARTESIAN_POINT('Ctrl Pts',(0.125460929083487,0.0162653271532848,
0.923504228586243));
#35084=CARTESIAN_POINT('Ctrl Pts',(0.126018750659753,0.0125790928555092,
0.923355949140843));
#35085=CARTESIAN_POINT('Ctrl Pts',(0.126424880564737,0.00989527772751904,
0.923247992188954));
#35086=CARTESIAN_POINT('Ctrl Pts',(0.126745061646254,0.00719882962072188,
0.923140094926841));
#35087=CARTESIAN_POINT('Ctrl Pts',(0.126976603796028,0.00450277675306522,
0.923032557085152));
#35088=CARTESIAN_POINT('Ctrl Pts',(0.12757677314312,-0.00248553311139155,
0.922753813382129));
#35089=CARTESIAN_POINT('Ctrl Pts',(0.127585234929588,-0.00948784607823892,
0.922476804764986));
#35090=CARTESIAN_POINT('Ctrl Pts',(0.126969800827767,-0.0164342950540157,
0.922200564268829));
#35091=CARTESIAN_POINT('Ctrl Pts',(0.126365890166078,-0.0232506781321251,
0.921929496123068));
#35092=CARTESIAN_POINT('Ctrl Pts',(0.125161228392162,-0.0300136540166471,
0.921659167602865));
#35093=CARTESIAN_POINT('Ctrl Pts',(0.123399407242885,-0.0366692095497128,
0.921388665049245));
#35094=CARTESIAN_POINT('Ctrl Pts',(0.122693706044386,-0.0393351064361743,
0.921280314677605));
#35095=CARTESIAN_POINT('Ctrl Pts',(0.121898903213358,-0.0419812756064514,
0.921172034233936));
#35096=CARTESIAN_POINT('Ctrl Pts',(0.121020997998916,-0.0445959600773696,
0.921064109665588));
#35097=CARTESIAN_POINT('Ctrl Pts',(0.118352374694664,-0.0525439797468811,
0.920736044615448));
#35098=CARTESIAN_POINT('Ctrl Pts',(0.11491247387436,-0.0602240203343106,
0.920410355973602));
#35099=CARTESIAN_POINT('Ctrl Pts',(0.110787244183297,-0.067540847099726,
0.920085467703143));
#35100=CARTESIAN_POINT('Ctrl Pts',(0.108602638591366,-0.0714156327150692,
0.919913416014983));
#35101=CARTESIAN_POINT('Ctrl Pts',(0.106225299026755,-0.0751884756223749,
0.919741588788067));
#35102=CARTESIAN_POINT('Ctrl Pts',(0.103664831029184,-0.0788439383503402,
0.919569751954905));
#35103=CARTESIAN_POINT('Ctrl Pts',(0.101376332819864,-0.0821111222851215,
0.919416167420609));
#35104=CARTESIAN_POINT('Ctrl Pts',(0.0989387376213173,-0.0852871325232165,
0.919262431231772));
#35105=CARTESIAN_POINT('Ctrl Pts',(0.0963759957044455,-0.088340202919688,
0.919109404658397));
#35106=CARTESIAN_POINT('Ctrl Pts',(0.0909694481938422,-0.0947811832006395,
0.918786568623332));
#35107=CARTESIAN_POINT('Ctrl Pts',(0.0849957607581912,-0.100695240401247,
0.918466028662098));
#35108=CARTESIAN_POINT('Ctrl Pts',(0.0785257616471073,-0.105984325129946,
0.918146284163942));
#35109=CARTESIAN_POINT('Ctrl Pts',(0.0742361136603187,-0.109491019840235,
0.917934291655249));
#35110=CARTESIAN_POINT('Ctrl Pts',(0.0697277556719998,-0.112722769515888,
0.917722648813756));
#35111=CARTESIAN_POINT('Ctrl Pts',(0.0650165017469215,-0.115645838880061,
0.917510918298299));
#35112=CARTESIAN_POINT('Ctrl Pts',(0.0626218558869296,-0.117131582604068,
0.917403299475299));
#35113=CARTESIAN_POINT('Ctrl Pts',(0.0601741524651638,-0.118537526250906,
0.917295638036625));
#35114=CARTESIAN_POINT('Ctrl Pts',(0.0576864529767728,-0.119853555264988,
0.917188346403244));
#35115=CARTESIAN_POINT('Ctrl Pts',(0.0492417976832846,-0.12432090006769,
0.916824138079852));
#35116=CARTESIAN_POINT('Ctrl Pts',(0.0403105010214407,-0.127774185485052,
0.916462909477301));
#35117=CARTESIAN_POINT('Ctrl Pts',(0.0310751541446225,-0.130251129571305,
0.916102510949096));
#35118=CARTESIAN_POINT('Ctrl Pts',(0.0264632552530831,-0.131488052865922,
0.91592253702988));
#35119=CARTESIAN_POINT('Ctrl Pts',(0.0217750625284288,-0.132480793424065,
0.915742770110557));
#35120=CARTESIAN_POINT('Ctrl Pts',(0.0170316000051624,-0.133229777506063,
0.915562942492132));
#35121=CARTESIAN_POINT('Ctrl Pts',(0.0138158762359995,-0.133737534424853,
0.91544103240133));
#35122=CARTESIAN_POINT('Ctrl Pts',(0.0105740209053218,-0.134132938348625,
0.915319069467609));
#35123=CARTESIAN_POINT('Ctrl Pts',(0.0073287749381158,-0.134414943979412,
0.91519757274014));
#35124=CARTESIAN_POINT('Ctrl Pts',(-0.00265707911089655,-0.135282695483764,
0.91482371861623));
#35125=CARTESIAN_POINT('Ctrl Pts',(-0.0127097596984602,-0.135087239355917,
0.914452927180717));
#35126=CARTESIAN_POINT('Ctrl Pts',(-0.0226366995613315,-0.13384562451132,
0.914082871556714));
#35127=CARTESIAN_POINT('Ctrl Pts',(-0.0278509024051071,-0.133193456598246,
0.913888496944428));
#35128=CARTESIAN_POINT('Ctrl Pts',(-0.0330306231776361,-0.132251796770583,
0.913694325339435));
#35129=CARTESIAN_POINT('Ctrl Pts',(-0.0381476304341873,-0.131017345860063,
0.913500019539069));
#35130=CARTESIAN_POINT('Ctrl Pts',(-0.0414017963667409,-0.130232295556825,
0.913376450569093));
#35131=CARTESIAN_POINT('Ctrl Pts',(-0.0446227244193663,-0.129330489295675,
0.913253123242388));
#35132=CARTESIAN_POINT('Ctrl Pts',(-0.0477977620148837,-0.128314174106561,
0.913130170982833));
#35133=CARTESIAN_POINT('Ctrl Pts',(-0.0560508514351662,-0.125672397471604,
0.912810572879819));
#35134=CARTESIAN_POINT('Ctrl Pts',(-0.0640066574241223,-0.122256042832264,
0.912493045231938));
#35135=CARTESIAN_POINT('Ctrl Pts',(-0.0715409466919047,-0.118061015146759,
0.912176128537659));
#35136=CARTESIAN_POINT('Ctrl Pts',(-0.0762921378140006,-0.11541559265395,
0.911976277996913));
#35137=CARTESIAN_POINT('Ctrl Pts',(-0.080875618778813,-0.112459902541578,
0.911776670412738));
#35138=CARTESIAN_POINT('Ctrl Pts',(-0.0852772318261866,-0.109220115387155,
0.911576939781678));
#35139=CARTESIAN_POINT('Ctrl Pts',(-0.0875530243079477,-0.107545028738423,
0.911473671851569));
#35140=CARTESIAN_POINT('Ctrl Pts',(-0.0897785308463731,-0.105794887026521,
0.911370439409319));
#35141=CARTESIAN_POINT('Ctrl Pts',(-0.0919449058640415,-0.10397965349885,
0.911267529872683));
#35142=CARTESIAN_POINT('Ctrl Pts',(-0.0992562147283688,-0.0978534136403538,
0.910920220011141));
#35143=CARTESIAN_POINT('Ctrl Pts',(-0.105919754790705,-0.0909713378622389,
0.910575510440108));
#35144=CARTESIAN_POINT('Ctrl Pts',(-0.111868517901189,-0.0834835697610656,
0.910231536759666));
#35145=CARTESIAN_POINT('Ctrl Pts',(-0.115372944257836,-0.0790725129751651,
0.910028901285812));
#35146=CARTESIAN_POINT('Ctrl Pts',(-0.118628912335923,-0.0744505089078481,
0.909826521196012));
#35147=CARTESIAN_POINT('Ctrl Pts',(-0.121618006629831,-0.0696436476859399,
0.90962401532803));
#35148=CARTESIAN_POINT('Ctrl Pts',(-0.123117391998195,-0.0672324365713985,
0.90952243461307));
#35149=CARTESIAN_POINT('Ctrl Pts',(-0.124548834320201,-0.0647754742963825,
0.909420860177745));
#35150=CARTESIAN_POINT('Ctrl Pts',(-0.125905418138961,-0.0622851116177192,
0.9093196043405));
#35151=CARTESIAN_POINT('Ctrl Pts',(-0.130761030150815,-0.0533713719953201,
0.908957179953008));
#35152=CARTESIAN_POINT('Ctrl Pts',(-0.134679363933253,-0.0440025983801541,
0.908597596571227));
#35153=CARTESIAN_POINT('Ctrl Pts',(-0.13756687326497,-0.0343371686472044,
0.908238737834252));
#35154=CARTESIAN_POINT('Ctrl Pts',(-0.139097796244526,-0.0292126731787653,
0.908048475215596));
#35155=CARTESIAN_POINT('Ctrl Pts',(-0.14033830847868,-0.0240043037722782,
0.907858416294146));
#35156=CARTESIAN_POINT('Ctrl Pts',(-0.14126916593033,-0.0187337321988357,
0.90766824565692));
#35157=CARTESIAN_POINT('Ctrl Pts',(-0.141766581419635,-0.0159173354095375,
0.907566625564177));
#35158=CARTESIAN_POINT('Ctrl Pts',(-0.142175147764435,-0.0130838950804596,
0.90746500095103));
#35159=CARTESIAN_POINT('Ctrl Pts',(-0.142491067194012,-0.010247236235083,
0.907363696319434));
#35160=CARTESIAN_POINT('Ctrl Pts',(-0.142699030773042,-0.00837991922086784,
0.907297009462638));
#35161=CARTESIAN_POINT('Ctrl Pts',(-0.142867069971313,-0.00651002641398622,
0.907230418639425));
#35162=CARTESIAN_POINT('Ctrl Pts',(-0.142994592382579,-0.00463854690639179,
0.907163910672075));
#35163=CARTESIAN_POINT('Ctrl Pts',(-0.143099304951117,-0.00310181760319464,
0.907109298937397));
#35164=CARTESIAN_POINT('Ctrl Pts',(-0.143176698406437,-0.00156401794929073,
0.907054743068754));
#35165=CARTESIAN_POINT('Ctrl Pts',(-0.143227225569541,-2.57112916194508E-5,
0.907000235770274));
#35166=CARTESIAN_POINT('',(-0.00156150813732516,0.146115848505824,0.90365));
#35167=CARTESIAN_POINT('Ctrl Pts',(-0.00156268643911937,0.146080787864432,
0.90365));
#35168=CARTESIAN_POINT('Ctrl Pts',(-0.0117053345256504,0.14465327094795,
0.904950888122905));
#35169=CARTESIAN_POINT('Ctrl Pts',(-0.0216455209286645,0.142222180286059,
0.906261527257655));
#35170=CARTESIAN_POINT('Ctrl Pts',(-0.0312038210265984,0.138800205489803,
0.907591018110418));
#35171=CARTESIAN_POINT('Ctrl Pts',(-0.0379790896742497,0.136374586047791,
0.908533409288742));
#35172=CARTESIAN_POINT('Ctrl Pts',(-0.0445622616029078,0.133450051590279,
0.909485272488055));
#35173=CARTESIAN_POINT('Ctrl Pts',(-0.0508780053273359,0.130018961446113,
0.910449848959387));
#35174=CARTESIAN_POINT('Ctrl Pts',(-0.0536010334441123,0.128539649532677,
0.910865725373444));
#35175=CARTESIAN_POINT('Ctrl Pts',(-0.0562660125378511,0.126970478129068,
0.911282720586817));
#35176=CARTESIAN_POINT('Ctrl Pts',(-0.058866712211968,0.125312368815247,
0.911700977969885));
#35177=CARTESIAN_POINT('Ctrl Pts',(-0.0626444387166601,0.12290383100335,
0.912308530628704));
#35178=CARTESIAN_POINT('Ctrl Pts',(-0.0662873724862372,0.120307303169936,
0.912918858991888));
#35179=CARTESIAN_POINT('Ctrl Pts',(-0.069778152687478,0.117522359853825,
0.913532898033536));
#35180=CARTESIAN_POINT('Ctrl Pts',(-0.0759775260377567,0.112576501798998,
0.914623386993416));
#35181=CARTESIAN_POINT('Ctrl Pts',(-0.081698277829649,0.107036582207071,
0.915725579133695));
#35182=CARTESIAN_POINT('Ctrl Pts',(-0.0868900966390514,0.100989570353443,
0.916844711368391));
#35183=CARTESIAN_POINT('Ctrl Pts',(-0.0896166640492451,0.0978138845187795,
0.917432441717011));
#35184=CARTESIAN_POINT('Ctrl Pts',(-0.0921993947360654,0.0944939977198656,
0.918025537507845));
#35185=CARTESIAN_POINT('Ctrl Pts',(-0.0946128443867119,0.0910668838926417,
0.918620601845101));
#35186=CARTESIAN_POINT('Ctrl Pts',(-0.0989927195077328,0.0848474334123951,
0.919700511461385));
#35187=CARTESIAN_POINT('Ctrl Pts',(-0.102828650181205,0.0782631455551165,
0.92078926141647));
#35188=CARTESIAN_POINT('Ctrl Pts',(-0.106079098770626,0.0713949254017264,
0.921892245864136));
#35189=CARTESIAN_POINT('Ctrl Pts',(-0.108178735463834,0.0669583786746003,
0.922604721866953));
#35190=CARTESIAN_POINT('Ctrl Pts',(-0.110033655020259,0.062403198537532,
0.923323137285097));
#35191=CARTESIAN_POINT('Ctrl Pts',(-0.111627678155428,0.0577512547785083,
0.92404894598959));
#35192=CARTESIAN_POINT('Ctrl Pts',(-0.112967174079103,0.0538421147134128,
0.924658860475512));
#35193=CARTESIAN_POINT('Ctrl Pts',(-0.114123078730198,0.049859612891567,
0.925274762706783));
#35194=CARTESIAN_POINT('Ctrl Pts',(-0.11507803961208,0.0458466780964684,
0.925893033154576));
#35195=CARTESIAN_POINT('Ctrl Pts',(-0.117097308962912,0.0373613082845972,
0.92720036897266));
#35196=CARTESIAN_POINT('Ctrl Pts',(-0.118230954345967,0.0287177049851521,
0.928521669794669));
#35197=CARTESIAN_POINT('Ctrl Pts',(-0.118391771793402,0.020045083810393,
0.929866742826164));
#35198=CARTESIAN_POINT('Ctrl Pts',(-0.11848473133085,0.0150319284238029,
0.930644254028062));
#35199=CARTESIAN_POINT('Ctrl Pts',(-0.118251755364909,0.0100092161799773,
0.931429708350036));
#35200=CARTESIAN_POINT('Ctrl Pts',(-0.11766859746431,0.00500517689817996,
0.932225));
#35201=CARTESIAN_POINT('',(-0.115101970897782,0.0902398078595341,0.90365));
#35202=CARTESIAN_POINT('Origin',(0.,0.,0.90365));
#35203=CARTESIAN_POINT('Ctrl Pts',(-0.143227225569541,-2.57112916194508E-5,
0.907000235770274));
#35204=CARTESIAN_POINT('Ctrl Pts',(-0.143488833522934,0.00793898000868948,
0.90671802038504));
#35205=CARTESIAN_POINT('Ctrl Pts',(-0.143031870701996,0.0159171358242676,
0.906437106818573));
#35206=CARTESIAN_POINT('Ctrl Pts',(-0.141906651187533,0.0238323323994448,
0.906156482679268));
#35207=CARTESIAN_POINT('Ctrl Pts',(-0.141282697379586,0.0282214466835871,
0.906000871709079));
#35208=CARTESIAN_POINT('Ctrl Pts',(-0.140452894046849,0.0325912439394045,
0.905845349734719));
#35209=CARTESIAN_POINT('Ctrl Pts',(-0.139423292881505,0.0369284672537908,
0.905689744135006));
#35210=CARTESIAN_POINT('Ctrl Pts',(-0.13875911501036,0.0397263348598034,
0.905589365658919));
#35211=CARTESIAN_POINT('Ctrl Pts',(-0.138011948498085,0.0425090563696419,
0.905489007617642));
#35212=CARTESIAN_POINT('Ctrl Pts',(-0.13718658538945,0.0452640319758816,
0.905388954073411));
#35213=CARTESIAN_POINT('Ctrl Pts',(-0.134156179660795,0.0553792088866476,
0.905021597172627));
#35214=CARTESIAN_POINT('Ctrl Pts',(-0.130067939373984,0.0651554859252432,
0.904657113682601));
#35215=CARTESIAN_POINT('Ctrl Pts',(-0.125020727014944,0.07442120635967,
0.904293300817012));
#35216=CARTESIAN_POINT('Ctrl Pts',(-0.122044721725445,0.0798845851641063,
0.904078784578074));
#35217=CARTESIAN_POINT('Ctrl Pts',(-0.118734281499311,0.0851703778496932,
0.903864501493536));
#35218=CARTESIAN_POINT('Ctrl Pts',(-0.115101970897782,0.0902398078595341,
0.90365));
#35219=CARTESIAN_POINT('',(-0.05,-6.12323399573676E-18,1.));
#35220=CARTESIAN_POINT('',(-0.1,-1.22464679914735E-17,0.95));
#35221=CARTESIAN_POINT('Origin',(0.,0.,1.));
#35222=CARTESIAN_POINT('Ctrl Pts',(0.0850780204044548,-0.119080027477571,
-0.0164977839420937));
#35223=CARTESIAN_POINT('Ctrl Pts',(0.124484376148786,-0.090925728145445,
-0.0138643799872915));
#35224=CARTESIAN_POINT('Ctrl Pts',(0.17250686669983,0.00706609547096537,
-0.00859757207768696));
#35225=CARTESIAN_POINT('Ctrl Pts',(0.0881701387729916,0.148625694711589,
-0.000697360213280174));
#35226=CARTESIAN_POINT('Ctrl Pts',(-0.0762274913006873,0.154908116339636,
0.00720285165112661));
#35227=CARTESIAN_POINT('Ctrl Pts',(-0.171431501518862,0.0208683089584473,
0.0151030635155334));
#35228=CARTESIAN_POINT('Ctrl Pts',(-0.111122107950137,-0.132218525770778,
0.0230032753799401));
#35229=CARTESIAN_POINT('Ctrl Pts',(0.050013392704176,-0.165289372702636,
0.030903487244347));
#35230=CARTESIAN_POINT('Ctrl Pts',(0.165768725130536,-0.0484320089270095,
0.0388036991087536));
#35231=CARTESIAN_POINT('Ctrl Pts',(0.131132152914396,0.112382189969905,
0.0467039109731606));
#35232=CARTESIAN_POINT('Ctrl Pts',(-0.0224762869461261,0.171228238683186,
0.0546041228375672));
#35233=CARTESIAN_POINT('Ctrl Pts',(-0.155692220471689,0.0747310615070771,
0.062504334701974));
#35234=CARTESIAN_POINT('Ctrl Pts',(-0.147655869299913,-0.0895687367181161,
0.0704045465663809));
#35235=CARTESIAN_POINT('Ctrl Pts',(-0.00565764774487061,-0.172605493336333,
0.0783047584307876));
#35236=CARTESIAN_POINT('Ctrl Pts',(0.141473396847448,-0.0990455693335685,
0.0862049702951944));
#35237=CARTESIAN_POINT('Ctrl Pts',(0.160251925615185,0.0643743860018943,
0.0941051821596012));
#35238=CARTESIAN_POINT('Ctrl Pts',(0.0336409180434769,0.169390113302136,
0.102005394024008));
#35239=CARTESIAN_POINT('Ctrl Pts',(-0.123490994764231,0.120725758497873,
0.109905605888415));
#35240=CARTESIAN_POINT('Ctrl Pts',(-0.168584982150601,-0.0374678050106281,
0.117805817752822));
#35241=CARTESIAN_POINT('Ctrl Pts',(-0.0607292448116094,-0.16166845405022,
0.125706029617228));
#35242=CARTESIAN_POINT('Ctrl Pts',(0.102223455999678,-0.139194458136055,
0.133606241481635));
#35243=CARTESIAN_POINT('Ctrl Pts',(0.172433324173149,0.00956453913465353,
0.141506453346042));
#35244=CARTESIAN_POINT('Ctrl Pts',(0.086202040450112,0.149646047845283,
0.149406665210448));
#35245=CARTESIAN_POINT('Ctrl Pts',(-0.0782365529804317,0.153960298370095,
0.157306877074856));
#35246=CARTESIAN_POINT('Ctrl Pts',(-0.171694572067167,0.0185931582621336,
0.165207088939262));
#35247=CARTESIAN_POINT('Ctrl Pts',(-0.109381677027807,-0.133642733856025,
0.173107300803669));
#35248=CARTESIAN_POINT('Ctrl Pts',(0.052168390130379,-0.164630467088263,
0.181007512668076));
#35249=CARTESIAN_POINT('Ctrl Pts',(0.166388377416592,-0.04625623707159,
0.188907724532483));
#35250=CARTESIAN_POINT('Ctrl Pts',(0.129651527078137,0.114084236996722,
0.19680793639689));
#35251=CARTESIAN_POINT('Ctrl Pts',(-0.0247124365344563,0.170921113648968,
0.204708148261296));
#35252=CARTESIAN_POINT('Ctrl Pts',(-0.156655896226217,0.072688800963294,
0.212608360125703));
#35253=CARTESIAN_POINT('Ctrl Pts',(-0.146472369316595,-0.0914908554698463,
0.22050857199011));
#35254=CARTESIAN_POINT('Ctrl Pts',(-0.00340092071136592,-0.172664893209074,
0.228408783854516));
#35255=CARTESIAN_POINT('Ctrl Pts',(0.142756033285632,-0.0971876873308804,
0.236308995718923));
#35256=CARTESIAN_POINT('Ctrl Pts',(0.159396733387471,0.0664636215805494,
0.24420920758333));
#35257=CARTESIAN_POINT('Ctrl Pts',(0.0314238061962717,0.169815417475675,
0.252109419447737));
#35258=CARTESIAN_POINT('Ctrl Pts',(-0.12505855466298,0.119101173436036,
0.260009631312144));
#35259=CARTESIAN_POINT('Ctrl Pts',(-0.168080803576887,-0.0396683132637571,
0.26790984317655));
#35260=CARTESIAN_POINT('Ctrl Pts',(-0.0586107512557457,-0.162448488590979,
0.275810055040957));
#35261=CARTESIAN_POINT('Ctrl Pts',(0.104034251124571,-0.137846313701876,
0.283710266905363));
#35262=CARTESIAN_POINT('Ctrl Pts',(0.172293565052386,0.0118177430073507,
0.291610478769771));
#35263=CARTESIAN_POINT('Ctrl Pts',(0.084238525028331,0.150760082612412,
0.299510690634177));
#35264=CARTESIAN_POINT('Ctrl Pts',(-0.0802424140921812,0.15292444732255,
0.307410902498584));
#35265=CARTESIAN_POINT('Ctrl Pts',(-0.171922949352315,0.0163472044781485,
0.315311114362991));
#35266=CARTESIAN_POINT('Ctrl Pts',(-0.107625373942229,-0.135061136127476,
0.323211326227398));
#35267=CARTESIAN_POINT('Ctrl Pts',(0.0543159572952621,-0.163934463708362,
0.331111538091804));
#35268=CARTESIAN_POINT('Ctrl Pts',(0.166978815646636,-0.0440772813759624,
0.339011749956212));
#35269=CARTESIAN_POINT('Ctrl Pts',(0.128149157817753,0.11576927467532,0.346911961820618));
#35270=CARTESIAN_POINT('Ctrl Pts',(-0.0269445799125943,0.17058347288522,
0.354812173685025));
#35271=CARTESIAN_POINT('Ctrl Pts',(-0.157592688461949,0.070634808356674,
0.362712385549432));
#35272=CARTESIAN_POINT('Ctrl Pts',(-0.145263900126163,-0.0933977030145032,
0.370612597413839));
#35273=CARTESIAN_POINT('Ctrl Pts',(-0.00114358090037083,-0.172694596994154,
0.378512809278245));
#35274=CARTESIAN_POINT('Ctrl Pts',(0.144014258847901,-0.0953132984254496,
0.386413021142653));
#35275=CARTESIAN_POINT('Ctrl Pts',(0.15851431213257,0.0685415527792242,
0.394313233007058));
#35276=CARTESIAN_POINT('Ctrl Pts',(0.0292013200165327,0.170211675620508,
0.402213444871466));
#35277=CARTESIAN_POINT('Ctrl Pts',(-0.126604742061452,0.117456250986493,
0.410113656735872));
#35278=CARTESIAN_POINT('Ctrl Pts',(-0.167547904549645,-0.0418620507055259,
0.418013868600279));
#35279=CARTESIAN_POINT('Ctrl Pts',(-0.0564822415909637,-0.163200759781041,
0.425914080464686));
#35280=CARTESIAN_POINT('Ctrl Pts',(0.105827268468801,-0.136474616162425,
0.433814292329093));
#35281=CARTESIAN_POINT('Ctrl Pts',(0.172124364506242,0.0140689285864832,
0.441714504193499));
#35282=CARTESIAN_POINT('Ctrl Pts',(0.0822606147860967,0.15184835482567,
0.449614716057907));
#35283=CARTESIAN_POINT('Ctrl Pts',(-0.0822345632875265,0.151862464780335,
0.457514927922313));
#35284=CARTESIAN_POINT('Ctrl Pts',(-0.172121948383532,0.0140984571108209,
0.465415139786721));
#35285=CARTESIAN_POINT('Ctrl Pts',(-0.105850679763545,-0.13645645899643,
0.473315351651126));
#35286=CARTESIAN_POINT('Ctrl Pts',(0.0564542429141223,-0.163210447169421,
0.481215563515534));
#35287=CARTESIAN_POINT('Ctrl Pts',(0.167540720455548,-0.0418907937079863,
0.48911577537994));
#35288=CARTESIAN_POINT('Ctrl Pts',(0.126624890361875,0.117434529628606,
0.497015987244348));
#35289=CARTESIAN_POINT('Ctrl Pts',(-0.0291721189860838,0.170216682737359,
0.504916199108753));
#35290=CARTESIAN_POINT('Ctrl Pts',(-0.158502551179345,0.068568745634494,
0.512816410973161));
#35291=CARTESIAN_POINT('Ctrl Pts',(-0.14403060816614,-0.0952885907102249,
0.520716622837567));
#35292=CARTESIAN_POINT('Ctrl Pts',(0.00111395432615138,-0.172694790639464,
0.528616834701974));
#35293=CARTESIAN_POINT('Ctrl Pts',(0.145247875180311,-0.0934226223344961,
0.536517046566381));
#35294=CARTESIAN_POINT('Ctrl Pts',(0.157604803871184,0.0706077715621608,
0.544417258430788));
#35295=CARTESIAN_POINT('Ctrl Pts',(0.0269738439003715,0.170578847907609,
0.552317470295194));
#35296=CARTESIAN_POINT('Ctrl Pts',(-0.128129295177092,0.11579125755285,
0.560217682159602));
#35297=CARTESIAN_POINT('Ctrl Pts',(-0.166986374851081,-0.0440486347386962,
0.568117894024008));
#35298=CARTESIAN_POINT('Ctrl Pts',(-0.0543440802119571,-0.163925143142123,
0.576018105888415));
#35299=CARTESIAN_POINT('Ctrl Pts',(0.107602201995467,-0.135079597771001,
0.583918317752822));
#35300=CARTESIAN_POINT('Ctrl Pts',(0.171925751260969,0.0163177100599224,
0.591818529617229));
#35301=CARTESIAN_POINT('Ctrl Pts',(0.0802686478080903,0.152910679114674,
0.599718741481635));
#35302=CARTESIAN_POINT('Ctrl Pts',(-0.0842126601987931,0.150774531902743,
0.607618953346042));
#35303=CARTESIAN_POINT('Ctrl Pts',(-0.172291535128485,0.0118473005919646,
0.615519165210449));
#35304=CARTESIAN_POINT('Ctrl Pts',(-0.104057897766774,-0.137828464116146,
0.623419377074855));
#35305=CARTESIAN_POINT('Ctrl Pts',(0.0585828816032124,-0.162458541146064,
0.631319588939263));
#35306=CARTESIAN_POINT('Ctrl Pts',(0.168073995820709,-0.0396971477198862,
0.639219800803669));
#35307=CARTESIAN_POINT('Ctrl Pts',(0.12507898518031,0.119079717309719,0.647120012668075));
#35308=CARTESIAN_POINT('Ctrl Pts',(-0.0313946731132146,0.169820805875821,
0.655020224532484));
#35309=CARTESIAN_POINT('Ctrl Pts',(-0.159385328899637,0.0664909658504678,
0.662920436396888));
#35310=CARTESIAN_POINT('Ctrl Pts',(-0.142772704183121,-0.0971631954436711,
0.670820648261297));
#35311=CARTESIAN_POINT('Ctrl Pts',(0.00337129920097031,-0.172665474109675,
0.678720860125702));
#35312=CARTESIAN_POINT('Ctrl Pts',(0.146456671479165,-0.0915159821406338,
0.68662107199011));
#35313=CARTESIAN_POINT('Ctrl Pts',(0.156668364025577,0.0726619248576747,
0.694521283854517));
#35314=CARTESIAN_POINT('Ctrl Pts',(0.0247417584705585,0.17091687158558,
0.702421495718924));
#35315=CARTESIAN_POINT('Ctrl Pts',(-0.129631953475511,0.114106477666574,
0.71032170758333));
#35316=CARTESIAN_POINT('Ctrl Pts',(-0.166396310469803,-0.0462276917499887,
0.718221919447737));
#35317=CARTESIAN_POINT('Ctrl Pts',(-0.0521966324240299,-0.164621514831807,
0.726122131312144));
#35318=CARTESIAN_POINT('Ctrl Pts',(0.109358748279947,-0.133661497021884,
0.73402234317655));
#35319=CARTESIAN_POINT('Ctrl Pts',(0.171697759489448,0.0185637033690059,
0.741922555040957));
#35320=CARTESIAN_POINT('Ctrl Pts',(0.0782629640387094,0.153946873541983,
0.749822766905365));
#35321=CARTESIAN_POINT('Ctrl Pts',(-0.0861763659646394,0.149660835369141,
0.75772297876977));
#35322=CARTESIAN_POINT('Ctrl Pts',(-0.17243168220941,0.00959411813254083,
0.765623190634177));
#35323=CARTESIAN_POINT('Ctrl Pts',(-0.102247331262163,-0.139176914249964,
0.773523402498585));
#35324=CARTESIAN_POINT('Ctrl Pts',(0.0607015038436091,-0.161678879418918,
0.78142361436299));
#35325=CARTESIAN_POINT('Ctrl Pts',(0.168578561585846,-0.0374967082074332,
0.7893238262274));
#35326=CARTESIAN_POINT('Ctrl Pts',(0.123511685603348,0.120704537490262,
0.797224038091803));
#35327=CARTESIAN_POINT('Ctrl Pts',(-0.0336118229326868,0.169395946219611,
0.805124249956213));
#35328=CARTESIAN_POINT('Ctrl Pts',(-0.16024094592625,0.0644017551688373,
0.813024461820617));
#35329=CARTESIAN_POINT('Ctrl Pts',(-0.141490260395339,-0.0990210660472952,
0.820924673685026));
#35330=CARTESIAN_POINT('Ctrl Pts',(0.0056277969043301,-0.172606900899112,
0.828824885549431));
#35331=CARTESIAN_POINT('Ctrl Pts',(0.147640956035951,-0.0895932317207615,
0.836725097413839));
#35332=CARTESIAN_POINT('Ctrl Pts',(0.15570417479137,0.0747027653435218,
0.844625309278246));
#35333=CARTESIAN_POINT('Ctrl Pts',(0.022507302267937,0.171227391193745,
0.852525521142652));
#35334=CARTESIAN_POINT('Ctrl Pts',(-0.131115987327984,0.112398966130108,
0.860425733007058));
#35335=CARTESIAN_POINT('Ctrl Pts',(-0.16577111303378,-0.0483927087664539,
0.868325944871467));
#35336=CARTESIAN_POINT('Ctrl Pts',(-0.050052991301314,-0.165301420121155,
0.876226156735872));
#35337=CARTESIAN_POINT('Ctrl Pts',(0.111120800514148,-0.132198387754511,
0.884126368600279));
#35338=CARTESIAN_POINT('Ctrl Pts',(0.171394279774569,0.0207642914265632,
0.892026580464686));
#35339=CARTESIAN_POINT('Ctrl Pts',(0.0763332480962674,0.155038078338273,
0.899926792329093));
#35340=CARTESIAN_POINT('Ctrl Pts',(-0.0883093241020301,0.148357716484315,
0.9078270041935));
#35341=CARTESIAN_POINT('Ctrl Pts',(-0.14415958729081,0.0546064221138428,
0.913093812103104));
#35342=CARTESIAN_POINT('Ctrl Pts',(-0.146217781693074,0.00621955117001918,
0.915727216057906));
#35343=CARTESIAN_POINT('Ctrl Pts',(0.0795408277542851,-0.111329858282328,
-0.0109985226280626));
#35344=CARTESIAN_POINT('Ctrl Pts',(0.116382471927282,-0.0850079450187934,
-0.00836511867326029));
#35345=CARTESIAN_POINT('Ctrl Pts',(0.161279480944341,0.00660620780878029,
-0.00309831076365578));
#35346=CARTESIAN_POINT('Ctrl Pts',(0.0824316996078882,0.138952584071836,
0.00480190110075102));
#35347=CARTESIAN_POINT('Ctrl Pts',(-0.0712663238620885,0.144826122433691,
0.0127021129651578));
#35348=CARTESIAN_POINT('Ctrl Pts',(-0.160274104511912,0.0195101221266785,
0.0206023248295645));
#35349=CARTESIAN_POINT('Ctrl Pts',(-0.103889869629501,-0.123613254448834,
0.0285025366939713));
#35350=CARTESIAN_POINT('Ctrl Pts',(0.0467583358848584,-0.154531728186116,
0.0364027485583782));
#35351=CARTESIAN_POINT('Ctrl Pts',(0.154979882582751,-0.0452798744204848,
0.0443029604227849));
#35352=CARTESIAN_POINT('Ctrl Pts',(0.122597586761272,0.105067940844772,
0.0522031722871918));
#35353=CARTESIAN_POINT('Ctrl Pts',(-0.0210134469518542,0.160084070774355,
0.0601033841515984));
#35354=CARTESIAN_POINT('Ctrl Pts',(-0.145559194164939,0.0698672872613988,
0.0680035960160053));
#35355=CARTESIAN_POINT('Ctrl Pts',(-0.138045878489652,-0.0837392716191075,
0.0759038078804119));
#35356=CARTESIAN_POINT('Ctrl Pts',(-0.00528942707681416,-0.16137168859408,
0.083804019744819));
#35357=CARTESIAN_POINT('Ctrl Pts',(0.132265784240875,-0.0925993168709629,
0.0917042316092254));
#35358=CARTESIAN_POINT('Ctrl Pts',(0.149822136811053,0.0601846625535317,
0.0996044434736326));
#35359=CARTESIAN_POINT('Ctrl Pts',(0.0314514425097271,0.15836557740051,
0.107504655338039));
#35360=CARTESIAN_POINT('Ctrl Pts',(-0.115453743482173,0.112868479032945,
0.115404867202446));
#35361=CARTESIAN_POINT('Ctrl Pts',(-0.157612847166081,-0.0350292615003714,
0.123305079066853));
#35362=CARTESIAN_POINT('Ctrl Pts',(-0.0567767606515088,-0.151146472329493,
0.13120529093126));
#35363=CARTESIAN_POINT('Ctrl Pts',(0.0955703749036966,-0.130135167300756,
0.139105502795666));
#35364=CARTESIAN_POINT('Ctrl Pts',(0.161210724837657,0.00894204350597287,
0.147005714660073));
#35365=CARTESIAN_POINT('Ctrl Pts',(0.0805916924126166,0.139906528844762,
0.15490592652448));
#35366=CARTESIAN_POINT('Ctrl Pts',(-0.0731446283672545,0.143939991967805,
0.162806138388887));
#35367=CARTESIAN_POINT('Ctrl Pts',(-0.160520053454664,0.0173830466635891,
0.170706350253294));
#35368=CARTESIAN_POINT('Ctrl Pts',(-0.102262712397196,-0.124944769797408,
0.1786065621177));
#35369=CARTESIAN_POINT('Ctrl Pts',(0.0487730780976374,-0.153915706589351,
0.186506773982107));
#35370=CARTESIAN_POINT('Ctrl Pts',(0.155559205603179,-0.0432457098552795,
0.194406985846514));
#35371=CARTESIAN_POINT('Ctrl Pts',(0.121213325537862,0.106659212347636,
0.202307197710921));
#35372=CARTESIAN_POINT('Ctrl Pts',(-0.0231040596435062,0.159796934574786,
0.210207409575327));
#35373=CARTESIAN_POINT('Ctrl Pts',(-0.146460150332438,0.0679579445972159,
0.218107621439734));
#35374=CARTESIAN_POINT('Ctrl Pts',(-0.136939405068282,-0.0855362917640029,
0.226007833304141));
#35375=CARTESIAN_POINT('Ctrl Pts',(-0.00317957619632727,-0.16142722250312,
0.233908045168548));
#35376=CARTESIAN_POINT('Ctrl Pts',(0.133464941949482,-0.0908623527095838,
0.241808257032955));
#35377=CARTESIAN_POINT('Ctrl Pts',(0.149022603660681,0.0621379229433468,
0.249708468897361));
#35378=CARTESIAN_POINT('Ctrl Pts',(0.0293786285125025,0.158763201203343,
0.257608680761768));
#35379=CARTESIAN_POINT('Ctrl Pts',(-0.11691928077733,0.111349627983502,
0.265508892626175));
#35380=CARTESIAN_POINT('Ctrl Pts',(-0.157141482401145,-0.0370865525269131,
0.273409104490581));
#35381=CARTESIAN_POINT('Ctrl Pts',(-0.0547961465019971,-0.15187573933352,
0.281309316354988));
#35382=CARTESIAN_POINT('Ctrl Pts',(0.0972633167756718,-0.12887476509914,
0.289209528219395));
#35383=CARTESIAN_POINT('Ctrl Pts',(0.161080061758064,0.0110486005260055,
0.297109740083802));
#35384=CARTESIAN_POINT('Ctrl Pts',(0.0787559698462676,0.140948058103473,
0.305009951948209));
#35385=CARTESIAN_POINT('Ctrl Pts',(-0.0750199406092437,0.142971557942657,
0.312910163812615));
#35386=CARTESIAN_POINT('Ctrl Pts',(-0.160733567100311,0.0152832678696448,
0.320810375677022));
#35387=CARTESIAN_POINT('Ctrl Pts',(-0.100620716020809,-0.12627085719605,
0.328710587541429));
#35388=CARTESIAN_POINT('Ctrl Pts',(0.050780873638021,-0.153265001687028,
0.336610799405836));
#35389=CARTESIAN_POINT('Ctrl Pts',(0.156111215926553,-0.0412085686659782,
0.344511011270243));
#35390=CARTESIAN_POINT('Ctrl Pts',(0.119808736032893,0.108234581533658,
0.35241122313465));
#35391=CARTESIAN_POINT('Ctrl Pts',(-0.0251909268639622,0.15948126872238,
0.360311434999056));
#35392=CARTESIAN_POINT('Ctrl Pts',(-0.147335972660104,0.066037633436295,
0.368211646863463));
#35393=CARTESIAN_POINT('Ctrl Pts',(-0.135809587528269,-0.0873190346085379,
0.37611185872787));
#35394=CARTESIAN_POINT('Ctrl Pts',(-0.00106915242017828,-0.16145499305586,
0.384012070592276));
#35395=CARTESIAN_POINT('Ctrl Pts',(0.134641277532382,-0.0891099559758252,
0.391912282456683));
#35396=CARTESIAN_POINT('Ctrl Pts',(0.148197613649053,0.0640806146840961,
0.39981249432109));
#35397=CARTESIAN_POINT('Ctrl Pts',(0.0273007899642087,0.159133669400588,
0.407712706185496));
#35398=CARTESIAN_POINT('Ctrl Pts',(-0.118364836573682,0.109811763178865,
0.415612918049904));
#35399=CARTESIAN_POINT('Ctrl Pts',(-0.156643266416161,-0.0391375134115731,
0.42351312991431));
#35400=CARTESIAN_POINT('Ctrl Pts',(-0.0528061681290295,-0.152579049928534,
0.431413341778717));
#35401=CARTESIAN_POINT('Ctrl Pts',(0.0989396379107883,-0.12759234271557,
0.439313553643124));
#35402=CARTESIAN_POINT('Ctrl Pts',(0.160921873410089,0.0131532706104934,
0.447213765507531));
#35403=CARTESIAN_POINT('Ctrl Pts',(0.0769067893276909,0.14196550153073,
0.455113977371937));
#35404=CARTESIAN_POINT('Ctrl Pts',(-0.0768824333571298,0.14197869315729,
0.463014189236344));
#35405=CARTESIAN_POINT('Ctrl Pts',(-0.160919614537593,0.0131808773091078,
0.470914401100751));
#35406=CARTESIAN_POINT('Ctrl Pts',(-0.098961525511766,-0.127575367285184,
0.478814612965158));
#35407=CARTESIAN_POINT('Ctrl Pts',(0.0527799917097706,-0.152588106825801,
0.486714824829564));
#35408=CARTESIAN_POINT('Ctrl Pts',(0.156636549889514,-0.0391643857129832,
0.494615036693972));
#35409=CARTESIAN_POINT('Ctrl Pts',(0.118383673548094,0.109791455527395,
0.502515248558378));
#35410=CARTESIAN_POINT('Ctrl Pts',(-0.027273489444968,0.15913835063573,
0.510415460422786));
#35411=CARTESIAN_POINT('Ctrl Pts',(-0.14818661814222,0.0641060377276359,
0.518315672287191));
#35412=CARTESIAN_POINT('Ctrl Pts',(-0.13465656277644,-0.0890868563302129,
0.526215884151598));
#35413=CARTESIAN_POINT('Ctrl Pts',(0.00104145405313166,-0.161455174098016,
0.534116096016006));
#35414=CARTESIAN_POINT('Ctrl Pts',(0.135794605545242,-0.0873423320868967,
0.542016307880412));
#35415=CARTESIAN_POINT('Ctrl Pts',(0.147347299553637,0.0660123562965002,
0.549916519744819));
#35416=CARTESIAN_POINT('Ctrl Pts',(0.025218286243035,0.15947694475544,0.557816731609225));
#35417=CARTESIAN_POINT('Ctrl Pts',(-0.119790166126449,0.108255133684104,
0.565716943473633));
#35418=CARTESIAN_POINT('Ctrl Pts',(-0.156118283149977,-0.0411817864579589,
0.573617155338038));
#35419=CARTESIAN_POINT('Ctrl Pts',(-0.0508071662111437,-0.153256287737759,
0.581517367202447));
#35420=CARTESIAN_POINT('Ctrl Pts',(0.10059905219016,-0.126288117287442,
0.589417579066852));
#35421=CARTESIAN_POINT('Ctrl Pts',(0.160736186650373,0.0152556930573902,
0.597317790931261));
#35422=CARTESIAN_POINT('Ctrl Pts',(0.0750444669377644,0.14295868582074,
0.605218002795666));
#35423=CARTESIAN_POINT('Ctrl Pts',(-0.0787317883956269,0.140961566980476,
0.613118214660074));
#35424=CARTESIAN_POINT('Ctrl Pts',(-0.161078163949129,0.0110762343935455,
0.62101842652448));
#35425=CARTESIAN_POINT('Ctrl Pts',(-0.097285424406824,-0.128858077230555,
0.628918638388887));
#35426=CARTESIAN_POINT('Ctrl Pts',(0.0547700907096662,-0.151885137631092,
0.636818850253293));
#35427=CARTESIAN_POINT('Ctrl Pts',(0.157135117718952,-0.037113510329848,
0.644719062117701));
#35428=CARTESIAN_POINT('Ctrl Pts',(0.116938381600928,0.111329568301349,
0.652619273982107));
#35429=CARTESIAN_POINT('Ctrl Pts',(-0.0293513915183856,0.158768238906452,
0.660519485846514));
#35430=CARTESIAN_POINT('Ctrl Pts',(-0.149011941419152,0.0621634875469089,
0.668419697710921));
#35431=CARTESIAN_POINT('Ctrl Pts',(-0.133480527843221,-0.0908394548451002,
0.676319909575327));
#35432=CARTESIAN_POINT('Ctrl Pts',(0.00315188256353199,-0.161427765596558,
0.684220121439734));
#35433=CARTESIAN_POINT('Ctrl Pts',(0.136924728904249,-0.0855597830979986,
0.692120333304141));
#35434=CARTESIAN_POINT('Ctrl Pts',(0.14647180668124,0.0679328176880866,
0.700020545168548));
#35435=CARTESIAN_POINT('Ctrl Pts',(0.0231314731994126,0.159792968600594,
0.707920757032954));
#35436=CARTESIAN_POINT('Ctrl Pts',(-0.121195025857785,0.106680005512326,
0.715820968897362));
#35437=CARTESIAN_POINT('Ctrl Pts',(-0.155566622343907,-0.0432190223689262,
0.723721180761768));
#35438=CARTESIAN_POINT('Ctrl Pts',(-0.0487994822782217,-0.1539073369789,
0.731621392626175));
#35439=CARTESIAN_POINT('Ctrl Pts',(0.102241275937164,-0.124962311786944,
0.739521604490582));
#35440=CARTESIAN_POINT('Ctrl Pts',(0.160523033427699,0.0173555088039932,
0.747421816354988));
#35441=CARTESIAN_POINT('Ctrl Pts',(0.0731693204960455,0.143927440877225,
0.755322028219396));
#35442=CARTESIAN_POINT('Ctrl Pts',(-0.0805676889177445,0.139920353941802,
0.763222240083802));
#35443=CARTESIAN_POINT('Ctrl Pts',(-0.161209189739,0.00896969739313117,
0.771122451948209));
#35444=CARTESIAN_POINT('Ctrl Pts',(-0.0955926962756769,-0.130118765235746,
0.779022663812615));
#35445=CARTESIAN_POINT('Ctrl Pts',(0.0567508251684453,-0.151156219176586,
0.786922875677023));
#35446=CARTESIAN_POINT('Ctrl Pts',(0.157606844475459,-0.0350562835700847,
0.794823087541428));
#35447=CARTESIAN_POINT('Ctrl Pts',(0.115473087684851,0.112848639167101,
0.802723299405837));
#35448=CARTESIAN_POINT('Ctrl Pts',(-0.0314242410165019,0.158371030690115,
0.810623511270242));
#35449=CARTESIAN_POINT('Ctrl Pts',(-0.149811871720937,0.0602102504337274,
0.81852372313465));
#35450=CARTESIAN_POINT('Ctrl Pts',(-0.132281550246616,-0.0925764083493082,
0.826423934999057));
#35451=CARTESIAN_POINT('Ctrl Pts',(0.00526151903952945,-0.161373004547461,
0.834324146863462));
#35452=CARTESIAN_POINT('Ctrl Pts',(0.138031935836139,-0.0837621723962628,
0.842224358727871));
#35453=CARTESIAN_POINT('Ctrl Pts',(0.145570370453223,0.0698408327169628,
0.850124570592276));
#35454=CARTESIAN_POINT('Ctrl Pts',(0.0210424436816558,0.160083278442666,
0.858024782456684));
#35455=CARTESIAN_POINT('Ctrl Pts',(-0.122582473291093,0.105083625150338,
0.86592499432109));
#35456=CARTESIAN_POINT('Ctrl Pts',(-0.154982115072408,-0.0452431320599261,
0.873825206185497));
#35457=CARTESIAN_POINT('Ctrl Pts',(-0.0467953572586411,-0.154542991514022,
0.881725418049904));
#35458=CARTESIAN_POINT('Ctrl Pts',(0.103888647286289,-0.123594427089244,
0.88962562991431));
#35459=CARTESIAN_POINT('Ctrl Pts',(0.160239305296586,0.0194128744409952,
0.897525841778718));
#35460=CARTESIAN_POINT('Ctrl Pts',(0.0713651976137454,0.14494762602415,
0.905426053643123));
#35461=CARTESIAN_POINT('Ctrl Pts',(-0.0825618262402486,0.138702046860037,
0.913326265507531));
#35462=CARTESIAN_POINT('Ctrl Pts',(-0.134777147462009,0.0510524339304846,
0.918593073417135));
#35463=CARTESIAN_POINT('Ctrl Pts',(-0.136701386950153,0.00581475974607277,
0.921226477371938));
#35464=CARTESIAN_POINT('Ctrl Pts',(0.0740036351041154,-0.103579689087084,
-0.00549926131403137));
#35465=CARTESIAN_POINT('Ctrl Pts',(0.108280567705778,-0.0790901618921417,
-0.00286585735922911));
#35466=CARTESIAN_POINT('Ctrl Pts',(0.150052095188851,0.00614632014659505,
0.00240095055037541));
#35467=CARTESIAN_POINT('Ctrl Pts',(0.0766932604427849,0.129279473432083,
0.0103011624147822));
#35468=CARTESIAN_POINT('Ctrl Pts',(-0.0663051564234898,0.134744128527746,
0.018201374279189));
#35469=CARTESIAN_POINT('Ctrl Pts',(-0.149116707504962,0.0181519352949098,
0.0261015861435957));
#35470=CARTESIAN_POINT('Ctrl Pts',(-0.0966576313088641,-0.115007983126889,
0.0340017980080025));
#35471=CARTESIAN_POINT('Ctrl Pts',(0.0435032790655407,-0.143774083669597,
0.0419020098724094));
#35472=CARTESIAN_POINT('Ctrl Pts',(0.144191040034967,-0.04212773991396,
0.0498022217368161));
#35473=CARTESIAN_POINT('Ctrl Pts',(0.114063020608148,0.0977536917196387,
0.0577024336012229));
#35474=CARTESIAN_POINT('Ctrl Pts',(-0.0195506069575822,0.148939902865525,
0.0656026454656297));
#35475=CARTESIAN_POINT('Ctrl Pts',(-0.13542616785819,0.0650035130157202,
0.0735028573300364));
#35476=CARTESIAN_POINT('Ctrl Pts',(-0.12843588767939,-0.0779098065200985,
0.0814030691944432));
#35477=CARTESIAN_POINT('Ctrl Pts',(-0.00492120640875794,-0.150137883851829,
0.0893032810588501));
#35478=CARTESIAN_POINT('Ctrl Pts',(0.123058171634303,-0.0861530644083569,
0.0972034929232567));
#35479=CARTESIAN_POINT('Ctrl Pts',(0.139392348006922,0.0559949391051687,
0.105103704787664));
#35480=CARTESIAN_POINT('Ctrl Pts',(0.0292619669759775,0.147341041498886,
0.11300391665207));
#35481=CARTESIAN_POINT('Ctrl Pts',(-0.107416492200115,0.105011199568016,
0.120904128516477));
#35482=CARTESIAN_POINT('Ctrl Pts',(-0.146640712181561,-0.0325907179901145,
0.128804340380884));
#35483=CARTESIAN_POINT('Ctrl Pts',(-0.0528242764914083,-0.140624490608767,
0.136704552245291));
#35484=CARTESIAN_POINT('Ctrl Pts',(0.0889172938077157,-0.121075876465457,
0.144604764109697));
#35485=CARTESIAN_POINT('Ctrl Pts',(0.149988125502165,0.00831954787729212,
0.152504975974104));
#35486=CARTESIAN_POINT('Ctrl Pts',(0.0749813443751213,0.130167009844241,
0.160405187838511));
#35487=CARTESIAN_POINT('Ctrl Pts',(-0.0680527037540773,0.133919685565514,
0.168305399702918));
#35488=CARTESIAN_POINT('Ctrl Pts',(-0.149345534842162,0.0161729350650448,
0.176205611567325));
#35489=CARTESIAN_POINT('Ctrl Pts',(-0.0951437477665844,-0.116246805738792,
0.184105823431731));
#35490=CARTESIAN_POINT('Ctrl Pts',(0.0453777660648959,-0.143200946090439,
0.192006035296138));
#35491=CARTESIAN_POINT('Ctrl Pts',(0.144730033789766,-0.040235182638969,
0.199906247160545));
#35492=CARTESIAN_POINT('Ctrl Pts',(0.112775123997586,0.0992341876985505,
0.207806459024951));
#35493=CARTESIAN_POINT('Ctrl Pts',(-0.021495682752556,0.148672755500605,
0.215706670889359));
#35494=CARTESIAN_POINT('Ctrl Pts',(-0.136264404438658,0.063227088231138,
0.223606882753765));
#35495=CARTESIAN_POINT('Ctrl Pts',(-0.127406440819969,-0.0795817280581598,
0.231507094618172));
#35496=CARTESIAN_POINT('Ctrl Pts',(-0.00295823168128856,-0.150189551797165,
0.239407306482579));
#35497=CARTESIAN_POINT('Ctrl Pts',(0.124173850613332,-0.0845370180882872,
0.247307518346986));
#35498=CARTESIAN_POINT('Ctrl Pts',(0.138648473933891,0.0578122243061442,
0.255207730211393));
#35499=CARTESIAN_POINT('Ctrl Pts',(0.0273334508287331,0.147710984931011,
0.263107942075799));
#35500=CARTESIAN_POINT('Ctrl Pts',(-0.108780006891681,0.103598082530968,
0.271008153940206));
#35501=CARTESIAN_POINT('Ctrl Pts',(-0.146202161225402,-0.0345047917900689,
0.278908365804612));
#35502=CARTESIAN_POINT('Ctrl Pts',(-0.0509815417482485,-0.141302990076062,
0.28680857766902));
#35503=CARTESIAN_POINT('Ctrl Pts',(0.0904923824267724,-0.119903216496403,
0.294708789533426));
#35504=CARTESIAN_POINT('Ctrl Pts',(0.149866558463742,0.0102794580446603,
0.302609001397833));
#35505=CARTESIAN_POINT('Ctrl Pts',(0.0732734146642041,0.131136033594535,
0.31050921326224));
#35506=CARTESIAN_POINT('Ctrl Pts',(-0.0697974671263062,0.133018668562764,
0.318409425126647));
#35507=CARTESIAN_POINT('Ctrl Pts',(-0.149544184848307,0.0142193312611412,
0.326309636991054));
#35508=CARTESIAN_POINT('Ctrl Pts',(-0.0936160580993886,-0.117480578264625,
0.33420984885546));
#35509=CARTESIAN_POINT('Ctrl Pts',(0.0472457899807798,-0.142595539665694,
0.342110060719868));
#35510=CARTESIAN_POINT('Ctrl Pts',(0.14524361620647,-0.0383398559559941,
0.350010272584273));
#35511=CARTESIAN_POINT('Ctrl Pts',(0.111468314248034,0.100699888391995,
0.357910484448681));
#35512=CARTESIAN_POINT('Ctrl Pts',(-0.02343727381533,0.148379064559539,
0.365810696313087));
#35513=CARTESIAN_POINT('Ctrl Pts',(-0.137079256858259,0.0614404585159162,
0.373710908177495));
#35514=CARTESIAN_POINT('Ctrl Pts',(-0.126355274930375,-0.0812403662025727,
0.381611120041901));
#35515=CARTESIAN_POINT('Ctrl Pts',(-0.000994723939985704,-0.150215389117566,
0.389511331906308));
#35516=CARTESIAN_POINT('Ctrl Pts',(0.125268296216863,-0.0829066135262008,
0.397411543770714));
#35517=CARTESIAN_POINT('Ctrl Pts',(0.137880915165535,0.0596196765889682,
0.405311755635121));
#35518=CARTESIAN_POINT('Ctrl Pts',(0.0254002599118846,0.148055663180668,
0.413211967499528));
#35519=CARTESIAN_POINT('Ctrl Pts',(-0.110124931085911,0.102167275371236,
0.421112179363935));
#35520=CARTESIAN_POINT('Ctrl Pts',(-0.145738628282677,-0.0364129761176204,
0.429012391228342));
#35521=CARTESIAN_POINT('Ctrl Pts',(-0.0491300946670952,-0.141957340076027,
0.436912603092748));
#35522=CARTESIAN_POINT('Ctrl Pts',(0.0920520073527751,-0.118710069268716,
0.444812814957155));
#35523=CARTESIAN_POINT('Ctrl Pts',(0.149719382313936,0.0122376126345037,
0.452713026821562));
#35524=CARTESIAN_POINT('Ctrl Pts',(0.0715529638692849,0.13208264823579,
0.460613238685969));
#35525=CARTESIAN_POINT('Ctrl Pts',(-0.071530303426733,0.132094921534244,
0.468513450550375));
#35526=CARTESIAN_POINT('Ctrl Pts',(-0.149717280691655,0.0122632975073946,
0.476413662414783));
#35527=CARTESIAN_POINT('Ctrl Pts',(-0.0920723712599867,-0.118694275573937,
0.484313874279189));
#35528=CARTESIAN_POINT('Ctrl Pts',(0.0491057405054188,-0.141965766482181,
0.492214086143596));
#35529=CARTESIAN_POINT('Ctrl Pts',(0.14573237932348,-0.03643797771798,0.500114298008002));
#35530=CARTESIAN_POINT('Ctrl Pts',(0.110142456734312,0.102148381426183,
0.50801450987241));
#35531=CARTESIAN_POINT('Ctrl Pts',(-0.0253748599038521,0.148060018534101,
0.515914721736816));
#35532=CARTESIAN_POINT('Ctrl Pts',(-0.137870685105096,0.0596433298207777,
0.523814933601224));
#35533=CARTESIAN_POINT('Ctrl Pts',(-0.125282517386741,-0.0828851219502007,
0.531715145465628));
#35534=CARTESIAN_POINT('Ctrl Pts',(0.00096895378011186,-0.150215557556568,
0.539615357330038));
#35535=CARTESIAN_POINT('Ctrl Pts',(0.126341335910172,-0.0812620418392971,
0.547515569194442));
#35536=CARTESIAN_POINT('Ctrl Pts',(0.137089795236089,0.0614169410308395,
0.55541578105885));
#35537=CARTESIAN_POINT('Ctrl Pts',(0.0234627285856986,0.148375041603271,
0.563315992923257));
#35538=CARTESIAN_POINT('Ctrl Pts',(-0.111451037075805,0.100719009815358,
0.571216204787664));
#35539=CARTESIAN_POINT('Ctrl Pts',(-0.145250191448873,-0.0383149381772212,
0.57911641665207));
#35540=CARTESIAN_POINT('Ctrl Pts',(-0.0472702522103304,-0.142587432333395,
0.587016628516477));
#35541=CARTESIAN_POINT('Ctrl Pts',(0.0935959023848529,-0.117496636803883,
0.594916840380884));
#35542=CARTESIAN_POINT('Ctrl Pts',(0.149546622039777,0.0141936760548576,
0.60281705224529));
#35543=CARTESIAN_POINT('Ctrl Pts',(0.0698202860674386,0.133006692526806,
0.610717264109698));
#35544=CARTESIAN_POINT('Ctrl Pts',(-0.0732509165924606,0.13114860205821,
0.618617475974104));
#35545=CARTESIAN_POINT('Ctrl Pts',(-0.149864792769772,0.0103051681951267,
0.626517687838512));
#35546=CARTESIAN_POINT('Ctrl Pts',(-0.0905129510468744,-0.119887690344964,
0.634417899702917));
#35547=CARTESIAN_POINT('Ctrl Pts',(0.0509572998161204,-0.141311734116118,
0.642318111567325));
#35548=CARTESIAN_POINT('Ctrl Pts',(0.146196239617194,-0.0345298729398102,
0.650218323431731));
#35549=CARTESIAN_POINT('Ctrl Pts',(0.108797778021546,0.103579419292979,
0.658118535296138));
#35550=CARTESIAN_POINT('Ctrl Pts',(-0.0273081099235566,0.147715671937082,
0.666018747160545));
#35551=CARTESIAN_POINT('Ctrl Pts',(-0.138638553938667,0.0578360092433499,
0.673918959024952));
#35552=CARTESIAN_POINT('Ctrl Pts',(-0.124188351503322,-0.0845157142465292,
0.681819170889359));
#35553=CARTESIAN_POINT('Ctrl Pts',(0.00293246592609361,-0.150190057083441,
0.689719382753765));
#35554=CARTESIAN_POINT('Ctrl Pts',(0.127392786329333,-0.0796035840553634,
0.697619594618173));
#35555=CARTESIAN_POINT('Ctrl Pts',(0.136275249336903,0.0632037105184985,
0.705519806482578));
#35556=CARTESIAN_POINT('Ctrl Pts',(0.0215211879282666,0.148669065615609,
0.713420018346986));
#35557=CARTESIAN_POINT('Ctrl Pts',(-0.11275809824006,0.0992535333580773,
0.721320230211393));
#35558=CARTESIAN_POINT('Ctrl Pts',(-0.144736934218011,-0.0402103529878636,
0.729220442075799));
#35559=CARTESIAN_POINT('Ctrl Pts',(-0.0454023321324136,-0.143193159125993,
0.737120653940206));
#35560=CARTESIAN_POINT('Ctrl Pts',(0.0951238035943801,-0.116263126552003,
0.745020865804613));
#35561=CARTESIAN_POINT('Ctrl Pts',(0.149348307365949,0.0161473142389802,
0.75292107766902));
#35562=CARTESIAN_POINT('Ctrl Pts',(0.0680756769533821,0.133908008212467,
0.760821289533426));
#35563=CARTESIAN_POINT('Ctrl Pts',(-0.0749590118708499,0.130179872514462,
0.768721501397833));
#35564=CARTESIAN_POINT('Ctrl Pts',(-0.149986697268588,0.00834527665372157,
0.77662171326224));
#35565=CARTESIAN_POINT('Ctrl Pts',(-0.0889380612891912,-0.121060616221528,
0.784521925126647));
#35566=CARTESIAN_POINT('Ctrl Pts',(0.0528001464932815,-0.140633558934255,
0.792422136991054));
#35567=CARTESIAN_POINT('Ctrl Pts',(0.146635127365071,-0.0326158589327362,
0.80032234885546));
#35568=CARTESIAN_POINT('Ctrl Pts',(0.107434489766355,0.104992740843939,
0.808222560719866));
#35569=CARTESIAN_POINT('Ctrl Pts',(-0.0292366591003167,0.147346115160618,
0.816122772584275));
#35570=CARTESIAN_POINT('Ctrl Pts',(-0.139382797515625,0.0560187456986177,
0.82402298444868));
#35571=CARTESIAN_POINT('Ctrl Pts',(-0.123072840097892,-0.0861317506513214,
0.831923196313088));
#35572=CARTESIAN_POINT('Ctrl Pts',(0.00489524117472862,-0.150139108195811,
0.839823408177494));
#35573=CARTESIAN_POINT('Ctrl Pts',(0.128422915636328,-0.0779311130717641,
0.847723620041902));
#35574=CARTESIAN_POINT('Ctrl Pts',(0.135436566115076,0.0649789000904037,
0.855623831906308));
#35575=CARTESIAN_POINT('Ctrl Pts',(0.0195775850953746,0.148939165691587,
0.863524043770715));
#35576=CARTESIAN_POINT('Ctrl Pts',(-0.114048959254202,0.0977682841705676,
0.871424255635121));
#35577=CARTESIAN_POINT('Ctrl Pts',(-0.144193117111036,-0.0420935553533985,
0.879324467499528));
#35578=CARTESIAN_POINT('Ctrl Pts',(-0.0435377232159684,-0.143784562906888,
0.887224679363934));
#35579=CARTESIAN_POINT('Ctrl Pts',(0.09665649405843,-0.114990466423977,
0.895124891228342));
#35580=CARTESIAN_POINT('Ctrl Pts',(0.149084330818603,0.0180614574554272,
0.903025103092748));
#35581=CARTESIAN_POINT('Ctrl Pts',(0.0663971471312236,0.134857173710026,
0.910925314957155));
#35582=CARTESIAN_POINT('Ctrl Pts',(-0.0768143283784672,0.129046377235758,
0.918825526821562));
#35583=CARTESIAN_POINT('Ctrl Pts',(-0.125394707633209,0.0474984457471263,
0.924092334731166));
#35584=CARTESIAN_POINT('Ctrl Pts',(-0.127184992207232,0.00540996832212636,
0.926725738685969));
#35585=CARTESIAN_POINT('Ctrl Pts',(0.0684664424539458,-0.0958295198918399,
-1.80411241501588E-16));
#35586=CARTESIAN_POINT('Ctrl Pts',(0.100178663484274,-0.0731723787654901,
0.00263340395480208));
#35587=CARTESIAN_POINT('Ctrl Pts',(0.138824709433362,0.00568643248440989,
0.00790021186440659));
#35588=CARTESIAN_POINT('Ctrl Pts',(0.0709548212776815,0.119606362792331,
0.0158004237288134));
#35589=CARTESIAN_POINT('Ctrl Pts',(-0.0613439889848912,0.1246621346218,
0.0237006355932201));
#35590=CARTESIAN_POINT('Ctrl Pts',(-0.137959310498012,0.016793748463141,
0.0316008474576269));
#35591=CARTESIAN_POINT('Ctrl Pts',(-0.0894253929882274,-0.106402711804945,
0.0395010593220337));
#35592=CARTESIAN_POINT('Ctrl Pts',(0.040248222246223,-0.133016439153077,
0.0474012711864405));
#35593=CARTESIAN_POINT('Ctrl Pts',(0.133402197487182,-0.0389756054074351,
0.0553014830508473));
#35594=CARTESIAN_POINT('Ctrl Pts',(0.105528454455023,0.0904394425945055,
0.0632016949152541));
#35595=CARTESIAN_POINT('Ctrl Pts',(-0.0180877669633101,0.137795734956694,
0.0711019067796609));
#35596=CARTESIAN_POINT('Ctrl Pts',(-0.125293141551441,0.0601397387700418,
0.0790021186440675));
#35597=CARTESIAN_POINT('Ctrl Pts',(-0.118825896869129,-0.0720803414210898,
0.0869023305084746));
#35598=CARTESIAN_POINT('Ctrl Pts',(-0.0045529857407016,-0.138904079109577,
0.0948025423728811));
#35599=CARTESIAN_POINT('Ctrl Pts',(0.113850559027731,-0.0797068119457511,
0.102702754237288));
#35600=CARTESIAN_POINT('Ctrl Pts',(0.12896255920279,0.0518052156568057,
0.110602966101695));
#35601=CARTESIAN_POINT('Ctrl Pts',(0.0270724914422277,0.136316505597261,
0.118503177966102));
#35602=CARTESIAN_POINT('Ctrl Pts',(-0.0993792409180562,0.0971539201030866,
0.126403389830508));
#35603=CARTESIAN_POINT('Ctrl Pts',(-0.135668577197041,-0.0301521744798576,
0.134303601694915));
#35604=CARTESIAN_POINT('Ctrl Pts',(-0.0488717923313075,-0.130102508888041,
0.142203813559322));
#35605=CARTESIAN_POINT('Ctrl Pts',(0.0822642127117346,-0.112016585630158,
0.150104025423729));
#35606=CARTESIAN_POINT('Ctrl Pts',(0.138765526166673,0.00769705224861128,
0.158004237288135));
#35607=CARTESIAN_POINT('Ctrl Pts',(0.0693709963376258,0.12042749084372,
0.165904449152542));
#35608=CARTESIAN_POINT('Ctrl Pts',(-0.0629607791409001,0.123899379163224,
0.173804661016949));
#35609=CARTESIAN_POINT('Ctrl Pts',(-0.138171016229659,0.0149628234665004,
0.181704872881356));
#35610=CARTESIAN_POINT('Ctrl Pts',(-0.088024783135973,-0.107548841680175,
0.189605084745762));
#35611=CARTESIAN_POINT('Ctrl Pts',(0.0419824540321544,-0.132486185591528,
0.197505296610169));
#35612=CARTESIAN_POINT('Ctrl Pts',(0.133900861976353,-0.0372246554226585,
0.205405508474576));
#35613=CARTESIAN_POINT('Ctrl Pts',(0.10433692245731,0.0918091630494651,
0.213305720338983));
#35614=CARTESIAN_POINT('Ctrl Pts',(-0.0198873058616059,0.137548576426424,
0.221205932203389));
#35615=CARTESIAN_POINT('Ctrl Pts',(-0.126068658544878,0.0584962318650602,
0.229106144067797));
#35616=CARTESIAN_POINT('Ctrl Pts',(-0.117873476571655,-0.0736271643523165,
0.237006355932203));
#35617=CARTESIAN_POINT('Ctrl Pts',(-0.00273688716624997,-0.138951881091211,
0.24490656779661));
#35618=CARTESIAN_POINT('Ctrl Pts',(0.114882759277182,-0.0782116834669906,
0.252806779661017));
#35619=CARTESIAN_POINT('Ctrl Pts',(0.128274344207101,0.0534865256689417,
0.260706991525423));
#35620=CARTESIAN_POINT('Ctrl Pts',(0.0252882731449639,0.136658768658679,
0.26860720338983));
#35621=CARTESIAN_POINT('Ctrl Pts',(-0.100640733006032,0.0958465370784341,
0.276507415254237));
#35622=CARTESIAN_POINT('Ctrl Pts',(-0.13526284004966,-0.0319230310532247,
0.284407627118644));
#35623=CARTESIAN_POINT('Ctrl Pts',(-0.0471669369944997,-0.130730240818604,
0.292307838983051));
#35624=CARTESIAN_POINT('Ctrl Pts',(0.0837214480778729,-0.110931667893667,
0.300208050847457));
#35625=CARTESIAN_POINT('Ctrl Pts',(0.138653055169421,0.00951031556331505,
0.308108262711865));
#35626=CARTESIAN_POINT('Ctrl Pts',(0.0677908594821406,0.121324009085596,
0.316008474576271));
#35627=CARTESIAN_POINT('Ctrl Pts',(-0.0645749936433688,0.123065779182871,
0.323908686440678));
#35628=CARTESIAN_POINT('Ctrl Pts',(-0.138354802596303,0.0131553946526375,
0.331808898305084));
#35629=CARTESIAN_POINT('Ctrl Pts',(-0.0866114001779684,-0.108690299333199,
0.339709110169492));
#35630=CARTESIAN_POINT('Ctrl Pts',(0.0437107063235388,-0.131926077644361,
0.347609322033898));
#35631=CARTESIAN_POINT('Ctrl Pts',(0.134376016486386,-0.0354711432460098,
0.355509533898305));
#35632=CARTESIAN_POINT('Ctrl Pts',(0.103127892463174,0.0931651952503325,
0.363409745762711));
#35633=CARTESIAN_POINT('Ctrl Pts',(-0.0216836207666979,0.137276860396698,
0.371309957627119));
#35634=CARTESIAN_POINT('Ctrl Pts',(-0.126822541056414,0.0568432835955372,
0.379210169491525));
#35635=CARTESIAN_POINT('Ctrl Pts',(-0.116900962332481,-0.0751616977966073,
0.387110381355933));
#35636=CARTESIAN_POINT('Ctrl Pts',(-0.000920295459793275,-0.138975785179272,
0.395010593220339));
#35637=CARTESIAN_POINT('Ctrl Pts',(0.115895314901344,-0.0767032710765764,
0.402910805084745));
#35638=CARTESIAN_POINT('Ctrl Pts',(0.127564216682018,0.0551587384938402,
0.410811016949152));
#35639=CARTESIAN_POINT('Ctrl Pts',(0.0234997298595607,0.136977656960748,
0.418711228813559));
#35640=CARTESIAN_POINT('Ctrl Pts',(-0.10188502559814,0.0945227875636074,
0.426611440677966));
#35641=CARTESIAN_POINT('Ctrl Pts',(-0.134833990149192,-0.0336884388236675,
0.434511652542373));
#35642=CARTESIAN_POINT('Ctrl Pts',(-0.045454021205161,-0.13133563022352,
0.44241186440678));
#35643=CARTESIAN_POINT('Ctrl Pts',(0.085164376794762,-0.109827795821861,
0.450312076271186));
#35644=CARTESIAN_POINT('Ctrl Pts',(0.138516891217783,0.0113219546585138,
0.458212288135593));
#35645=CARTESIAN_POINT('Ctrl Pts',(0.0661991384108791,0.12219979494085,
0.4661125));
#35646=CARTESIAN_POINT('Ctrl Pts',(-0.0661781734963363,0.122211149911198,
0.474012711864406));
#35647=CARTESIAN_POINT('Ctrl Pts',(-0.138514946845716,0.0113457177056816,
0.481912923728814));
#35648=CARTESIAN_POINT('Ctrl Pts',(-0.0851832170082076,-0.109813183862691,
0.48981313559322));
#35649=CARTESIAN_POINT('Ctrl Pts',(0.0454314893010671,-0.131343426138561,
0.497713347457628));
#35650=CARTESIAN_POINT('Ctrl Pts',(0.134828208757446,-0.0337115697229769,
0.505613559322033));
#35651=CARTESIAN_POINT('Ctrl Pts',(0.10190123992053,0.0945053073249706,
0.513513771186441));
#35652=CARTESIAN_POINT('Ctrl Pts',(-0.0234762303627364,0.136981686432473,
0.521413983050847));
#35653=CARTESIAN_POINT('Ctrl Pts',(-0.127554752067971,0.0551806219139196,
0.529314194915254));
#35654=CARTESIAN_POINT('Ctrl Pts',(-0.115908471997041,-0.0766833875701887,
0.537214406779661));
#35655=CARTESIAN_POINT('Ctrl Pts',(0.000896453507092177,-0.13897594101512,
0.545114618644068));
#35656=CARTESIAN_POINT('Ctrl Pts',(0.116888066275103,-0.0751817515916976,
0.553014830508475));
#35657=CARTESIAN_POINT('Ctrl Pts',(0.126832290918542,0.0568215257651788,
0.560915042372882));
#35658=CARTESIAN_POINT('Ctrl Pts',(0.0217071709283622,0.137273138451102,
0.568815254237287));
#35659=CARTESIAN_POINT('Ctrl Pts',(-0.103111908025161,0.0931828859466119,
0.576715466101696));
#35660=CARTESIAN_POINT('Ctrl Pts',(-0.134382099747769,-0.0354480898964837,
0.584615677966101));
#35661=CARTESIAN_POINT('Ctrl Pts',(-0.0437333382095171,-0.131918576929031,
0.592515889830509));
#35662=CARTESIAN_POINT('Ctrl Pts',(0.0865927525795457,-0.108705156320324,
0.600416101694915));
#35663=CARTESIAN_POINT('Ctrl Pts',(0.138357057429181,0.0131316590523252,
0.608316313559322));
#35664=CARTESIAN_POINT('Ctrl Pts',(0.0645961051971127,0.123054699232873,
0.616216525423729));
#35665=CARTESIAN_POINT('Ctrl Pts',(-0.0677700447892944,0.121335637135943,
0.624116737288135));
#35666=CARTESIAN_POINT('Ctrl Pts',(-0.138651421590416,0.00953410199670787,
0.632016949152542));
#35667=CARTESIAN_POINT('Ctrl Pts',(-0.0837404776869246,-0.110917303459374,
0.639917161016949));
#35668=CARTESIAN_POINT('Ctrl Pts',(0.0471445089225743,-0.130738330601145,
0.647817372881356));
#35669=CARTESIAN_POINT('Ctrl Pts',(0.135257361515437,-0.0319462355497722,
0.655717584745763));
#35670=CARTESIAN_POINT('Ctrl Pts',(0.100657174442164,0.0958292702846084,
0.66361779661017));
#35671=CARTESIAN_POINT('Ctrl Pts',(-0.0252648283287276,0.136663104967713,
0.671518008474576));
#35672=CARTESIAN_POINT('Ctrl Pts',(-0.128265166458182,0.0535085309397911,
0.679418220338983));
#35673=CARTESIAN_POINT('Ctrl Pts',(-0.114896175163422,-0.0781919736479584,
0.68731843220339));
#35674=CARTESIAN_POINT('Ctrl Pts',(0.00271304928865532,-0.138952348570324,
0.695218644067796));
#35675=CARTESIAN_POINT('Ctrl Pts',(0.117860843754417,-0.0736473850127282,
0.703118855932203));
#35676=CARTESIAN_POINT('Ctrl Pts',(0.126078691992566,0.0584746033489104,
0.711019067796611));
#35677=CARTESIAN_POINT('Ctrl Pts',(0.0199109026571207,0.137545162630623,
0.718919279661016));
#35678=CARTESIAN_POINT('Ctrl Pts',(-0.104321170622334,0.0918270612038291,
0.726819491525424));
#35679=CARTESIAN_POINT('Ctrl Pts',(-0.133907246092115,-0.0372016836068011,
0.73471970338983));
#35680=CARTESIAN_POINT('Ctrl Pts',(-0.0420051819866054,-0.132478981273086,
0.742619915254238));
#35681=CARTESIAN_POINT('Ctrl Pts',(0.0880063312515965,-0.107563941317063,
0.750520127118644));
#35682=CARTESIAN_POINT('Ctrl Pts',(0.1381735813042,0.0149391196739674,0.758420338983051));
#35683=CARTESIAN_POINT('Ctrl Pts',(0.0629820334107182,0.123888575547709,
0.766320550847457));
#35684=CARTESIAN_POINT('Ctrl Pts',(-0.069350334823955,0.120439391087123,
0.774220762711865));
#35685=CARTESIAN_POINT('Ctrl Pts',(-0.138764204798178,0.00772085591431189,
0.78212097457627));
#35686=CARTESIAN_POINT('Ctrl Pts',(-0.0822834263027052,-0.112002467207309,
0.790021186440679));
#35687=CARTESIAN_POINT('Ctrl Pts',(0.0488494678181175,-0.130110898691923,
0.797921398305084));
#35688=CARTESIAN_POINT('Ctrl Pts',(0.135663410254684,-0.0301754342953877,
0.805821610169492));
#35689=CARTESIAN_POINT('Ctrl Pts',(0.0993958918478579,0.0971368425207782,
0.813721822033898));
#35690=CARTESIAN_POINT('Ctrl Pts',(-0.0270490771841315,0.136321199631122,
0.821622033898304));
#35691=CARTESIAN_POINT('Ctrl Pts',(-0.128953723310312,0.0518272409635079,
0.829522245762713));
#35692=CARTESIAN_POINT('Ctrl Pts',(-0.113864129949169,-0.0796870929533346,
0.837422457627119));
#35693=CARTESIAN_POINT('Ctrl Pts',(0.00452896330992775,-0.13890521184416,
0.845322669491525));
#35694=CARTESIAN_POINT('Ctrl Pts',(0.118813895436517,-0.0721000537472655,
0.853222881355933));
#35695=CARTESIAN_POINT('Ctrl Pts',(0.125302761776928,0.0601169674638447,
0.861123093220339));
#35696=CARTESIAN_POINT('Ctrl Pts',(0.0181127265090936,0.137795052940508,
0.869023305084746));
#35697=CARTESIAN_POINT('Ctrl Pts',(-0.105515445217312,0.0904529431907972,
0.876923516949153));
#35698=CARTESIAN_POINT('Ctrl Pts',(-0.133404119149664,-0.0389439786468707,
0.88482372881356));
#35699=CARTESIAN_POINT('Ctrl Pts',(-0.0402800891732956,-0.133026134299755,
0.892723940677965));
#35700=CARTESIAN_POINT('Ctrl Pts',(0.0894243408305711,-0.10638650575871,
0.900624152542373));
#35701=CARTESIAN_POINT('Ctrl Pts',(0.137929356340621,0.0167100404698593,
0.908524364406779));
#35702=CARTESIAN_POINT('Ctrl Pts',(0.0614290966487016,0.124766721395902,
0.916424576271187));
#35703=CARTESIAN_POINT('Ctrl Pts',(-0.0710668305166857,0.11939070761148,
0.924324788135593));
#35704=CARTESIAN_POINT('Ctrl Pts',(-0.116012267804409,0.0439444575637681,
0.929591596045198));
#35705=CARTESIAN_POINT('Ctrl Pts',(-0.11766859746431,0.00500517689817995,
0.932225));
#35706=CARTESIAN_POINT('',(0.0684664424539459,-0.0958295198918398,0.));
#35707=CARTESIAN_POINT('Ctrl Pts',(0.0684664424539458,-0.0958295198918399,
-1.80411241501588E-16));
#35708=CARTESIAN_POINT('Ctrl Pts',(0.100178663484274,-0.0731723787654901,
0.00263340395480208));
#35709=CARTESIAN_POINT('Ctrl Pts',(0.138824709433362,0.00568643248440989,
0.00790021186440659));
#35710=CARTESIAN_POINT('Ctrl Pts',(0.0709548212776815,0.119606362792331,
0.0158004237288134));
#35711=CARTESIAN_POINT('Ctrl Pts',(-0.0613439889848912,0.1246621346218,
0.0237006355932201));
#35712=CARTESIAN_POINT('Ctrl Pts',(-0.115532083261749,0.0483695320037083,
0.0292882571924104));
#35713=CARTESIAN_POINT('Ctrl Pts',(-0.117931878255507,0.00481801833454289,
0.0322424748367984));
#35714=CARTESIAN_POINT('Ctrl Pts',(-0.117896184020664,8.43438525024954E-5,
0.0325632885263842));
#35715=CARTESIAN_POINT('Ctrl Pts',(0.0635538308725813,0.132076982143461,
2.60208521396521E-18));
#35716=CARTESIAN_POINT('Ctrl Pts',(0.0672186180130936,0.129896798349724,
2.66126088244575E-18));
#35717=CARTESIAN_POINT('Ctrl Pts',(0.0707747244255609,0.12755097155874,
-6.59520968701772E-18));
#35718=CARTESIAN_POINT('Ctrl Pts',(0.0742090918971922,0.125038932664582,
-4.55364912443912E-18));
#35719=CARTESIAN_POINT('Ctrl Pts',(0.080224006754745,0.120639374320277,
-2.50552574932592E-18));
#35720=CARTESIAN_POINT('Ctrl Pts',(0.0858662145577153,0.115730301363634,
1.59702880631994E-17));
#35721=CARTESIAN_POINT('Ctrl Pts',(0.0911015321007297,0.110378142457541,
2.25514051876985E-17));
#35722=CARTESIAN_POINT('Ctrl Pts',(0.0937720491785869,0.107648025011046,
2.59084099019214E-17));
#35723=CARTESIAN_POINT('Ctrl Pts',(0.0963357255281008,0.104802798728268,
-1.64960383635052E-18));
#35724=CARTESIAN_POINT('Ctrl Pts',(0.0987794574485338,0.101861414187154,
-4.33680868994202E-19));
#35725=CARTESIAN_POINT('Ctrl Pts',(0.10293496714428,0.0968596577026072,
1.63396805676607E-18));
#35726=CARTESIAN_POINT('Ctrl Pts',(0.106751261320725,0.0915729561578743,
3.03784192455847E-17));
#35727=CARTESIAN_POINT('Ctrl Pts',(0.110204305377691,0.08604549563647,2.73218947466347E-17));
#35728=CARTESIAN_POINT('Ctrl Pts',(0.111935557805272,0.0832741931890737,
2.57894452987073E-17));
#35729=CARTESIAN_POINT('Ctrl Pts',(0.113575375365209,0.0804423219653594,
5.7323915193469E-18));
#35730=CARTESIAN_POINT('Ctrl Pts',(0.115119932079619,0.077555293108205,
9.54097911787244E-18));
#35731=CARTESIAN_POINT('Ctrl Pts',(0.116773389847001,0.0744647103902093,
1.36180963184181E-17));
#35732=CARTESIAN_POINT('Ctrl Pts',(0.118313357645953,0.0713188633723711,
-9.33067413676427E-18));
#35733=CARTESIAN_POINT('Ctrl Pts',(0.119735247150481,0.0681278580844796,
-4.33680868994202E-18));
#35734=CARTESIAN_POINT('Ctrl Pts',(0.123742606948277,0.059134538797346,
9.73757301374157E-18));
#35735=CARTESIAN_POINT('Ctrl Pts',(0.126819919828835,0.0497749725291024,
2.44496492997929E-17));
#35736=CARTESIAN_POINT('Ctrl Pts',(0.128866909768778,0.040203097865136,
1.21430643318376E-17));
#35737=CARTESIAN_POINT('Ctrl Pts',(0.129678753995803,0.0364068548860612,
7.26222453596554E-18));
#35738=CARTESIAN_POINT('Ctrl Pts',(0.130327963181773,0.0325772120613575,
7.16378425601151E-18));
#35739=CARTESIAN_POINT('Ctrl Pts',(0.130805907644987,0.0287241348669356,
3.46944695195361E-18));
#35740=CARTESIAN_POINT('Ctrl Pts',(0.131145551201884,0.0259860074399329,
8.44125478642762E-19));
#35741=CARTESIAN_POINT('Ctrl Pts',(0.131398222957245,0.023238193513084,
1.89851870451249E-17));
#35742=CARTESIAN_POINT('Ctrl Pts',(0.131560851492827,0.0204930145081475,
1.56125112837913E-17));
#35743=CARTESIAN_POINT('Ctrl Pts',(0.131856680066531,0.0154994112226654,
9.47746335708933E-18));
#35744=CARTESIAN_POINT('Ctrl Pts',(0.131855937211452,0.0105061465300757,
1.21882171850414E-17));
#35745=CARTESIAN_POINT('Ctrl Pts',(0.131544012134307,0.00553446959878105,
1.73472347597681E-17));
#35746=CARTESIAN_POINT('Ctrl Pts',(0.131183605376493,-0.00020994178392047,
2.50428281171472E-17));
#35747=CARTESIAN_POINT('Ctrl Pts',(0.130407809774817,-0.00592569963173127,
6.69723701682335E-18));
#35748=CARTESIAN_POINT('Ctrl Pts',(0.129236296320737,-0.0115776207498215,
6.93889390390723E-18));
#35749=CARTESIAN_POINT('Ctrl Pts',(0.128494418700647,-0.0151567804883794,
7.09192657770507E-18));
#35750=CARTESIAN_POINT('Ctrl Pts',(0.127593716302061,-0.0187102876496501,
1.81123981287573E-17));
#35751=CARTESIAN_POINT('Ctrl Pts',(0.126538054496122,-0.0222283432593045,
1.73472347597681E-17));
#35752=CARTESIAN_POINT('Ctrl Pts',(0.125628643409289,-0.0252590096692432,
1.66880766401104E-17));
#35753=CARTESIAN_POINT('Ctrl Pts',(0.124606340862147,-0.0282558643089978,
1.76789329645073E-17));
#35754=CARTESIAN_POINT('Ctrl Pts',(0.123476980164864,-0.0312080791264482,
1.38777878078145E-17));
#35755=CARTESIAN_POINT('Ctrl Pts',(0.120897724271906,-0.0379504046593839,
5.19665867965098E-18));
#35756=CARTESIAN_POINT('Ctrl Pts',(0.117758352703866,-0.0444696874516502,
3.23003755723985E-17));
#35757=CARTESIAN_POINT('Ctrl Pts',(0.114097802370374,-0.050694248232474,
2.94902990916057E-17));
#35758=CARTESIAN_POINT('Ctrl Pts',(0.11100985408088,-0.0559451313142133,
2.71197891759751E-17));
#35759=CARTESIAN_POINT('Ctrl Pts',(0.107550620981395,-0.0609862743257036,
5.91633367061488E-18));
#35760=CARTESIAN_POINT('Ctrl Pts',(0.103737131336817,-0.0657661572550731,
2.08166817117217E-17));
#35761=CARTESIAN_POINT('Ctrl Pts',(0.10192691642303,-0.0680351067400168,
2.78896869532561E-17));
#35762=CARTESIAN_POINT('Ctrl Pts',(0.10004287794431,-0.0702374362624183,
3.79094719020518E-18));
#35763=CARTESIAN_POINT('Ctrl Pts',(0.098088083467589,-0.0723681596371707,
3.46944695195361E-18));
#35764=CARTESIAN_POINT('Ctrl Pts',(0.092197190805992,-0.078789224788366,
2.50058632912494E-18));
#35765=CARTESIAN_POINT('Ctrl Pts',(0.0856641330198359,-0.0845647204793276,
-6.81778632605364E-18));
#35766=CARTESIAN_POINT('Ctrl Pts',(0.0785460746715851,-0.0895442682019542,
-6.93889390390723E-18));
#35767=CARTESIAN_POINT('Ctrl Pts',(0.0753062120776356,-0.0918107641495869,
-6.9940173507989E-18));
#35768=CARTESIAN_POINT('Ctrl Pts',(0.0719448689431282,-0.0939117521002605,
3.85531108019535E-18));
#35769=CARTESIAN_POINT('Ctrl Pts',(0.068466442453948,-0.0958295198918383,
3.46944695195361E-18));
#35770=CARTESIAN_POINT('Ctrl Pts',(-0.00156268643912563,0.146080787864432,
0.903650000000001));
#35771=CARTESIAN_POINT('Ctrl Pts',(0.0213629386064158,0.146372019480346,
0.902408930776365));
#35772=CARTESIAN_POINT('Ctrl Pts',(0.0443374951530579,0.14156774719521,
0.901167861552729));
#35773=CARTESIAN_POINT('Ctrl Pts',(0.0647363246762687,0.131545720210662,
0.899926792329093));
#35774=CARTESIAN_POINT('Ctrl Pts',(0.108020258655701,0.110280149367703,
0.897293388374291));
#35775=CARTESIAN_POINT('Ctrl Pts',(0.139707269215135,0.0655222203971333,
0.894659984419488));
#35776=CARTESIAN_POINT('Ctrl Pts',(0.145505194618115,0.0176494760483365,
0.892026580464686));
#35777=CARTESIAN_POINT('Ctrl Pts',(0.151303120021096,-0.0302232683004618,
0.889393176509884));
#35778=CARTESIAN_POINT('Ctrl Pts',(0.131211960267621,-0.0812108280274876,
0.886759772555081));
#35779=CARTESIAN_POINT('Ctrl Pts',(0.0943040817549728,-0.112221779952107,
0.884126368600279));
#35780=CARTESIAN_POINT('Ctrl Pts',(0.0573962032423251,-0.143232731876727,
0.881492964645477));
#35781=CARTESIAN_POINT('Ctrl Pts',(0.0036716059705044,-0.15426707599894,
0.878859560690674));
#35782=CARTESIAN_POINT('Ctrl Pts',(-0.0424770462874833,-0.140299462834264,
0.876226156735872));
#35783=CARTESIAN_POINT('Ctrl Pts',(-0.0886256985454704,-0.126331849669587,
0.87359275278107));
#35784=CARTESIAN_POINT('Ctrl Pts',(-0.127198405789625,-0.0873622792180203,
0.870959348826268));
#35785=CARTESIAN_POINT('Ctrl Pts',(-0.140708905127403,-0.0410788815094769,
0.868325944871466));
#35786=CARTESIAN_POINT('Ctrl Pts',(-0.144574583355673,-0.027836090226996,
0.867572464775741));
#35787=CARTESIAN_POINT('Ctrl Pts',(-0.146388495105525,-0.0139945382267495,
0.866818984680017));
#35788=CARTESIAN_POINT('Ctrl Pts',(-0.146273246343463,-0.000123611542196964,
0.866065504584292));
#35789=CARTESIAN_POINT('Origin',(0.,0.,-0.0924367114736152));
#35790=CARTESIAN_POINT('',(-0.0684664424539439,-0.0958295198918412,0.));
#35791=CARTESIAN_POINT('Ctrl Pts',(-0.0686121729278148,-0.0959472995825297,
4.17959937493162E-17));
#35792=CARTESIAN_POINT('Ctrl Pts',(-0.0396139635805184,-0.116414379406814,
0.00240676188548629));
#35793=CARTESIAN_POINT('Ctrl Pts',(0.042075530384929,-0.130578648252184,
0.00744886483747836));
#35794=CARTESIAN_POINT('Ctrl Pts',(0.133186295059001,-0.0398205273591854,
0.0151263088559762));
#35795=CARTESIAN_POINT('Ctrl Pts',(0.106043485420733,0.0899039768168324,
0.0230323320554937));
#35796=CARTESIAN_POINT('Ctrl Pts',(-0.0174538572390982,0.137906280269365,
0.0309383552550111));
#35797=CARTESIAN_POINT('Ctrl Pts',(-0.105510720744521,0.0746991700253994,
0.0374064817277185));
#35798=CARTESIAN_POINT('Ctrl Pts',(-0.11763008980369,0.0178164887288322,
0.0412392671339201));
#35799=CARTESIAN_POINT('Ctrl Pts',(-0.117591431864639,2.92794590778002E-5,
0.0424367114736158));
#35800=CARTESIAN_POINT('Origin',(0.,0.,0.));
#35801=CARTESIAN_POINT('Ctrl Pts',(-0.0510216505388444,0.106149619882937,
-0.0164977839420935));
#35802=CARTESIAN_POINT('Ctrl Pts',(-0.0861748725546967,0.0892529469510397,
-0.0138624428755877));
#35803=CARTESIAN_POINT('Ctrl Pts',(-0.137790539141881,0.0181049606281334,
-0.0085917607425761));
#35804=CARTESIAN_POINT('Ctrl Pts',(-0.0902797247787074,-0.10582739645577,
-0.000685737543058663));
#35805=CARTESIAN_POINT('Ctrl Pts',(0.0393629057248093,-0.133280773711466,
0.00722028565645879));
#35806=CARTESIAN_POINT('Ctrl Pts',(0.133186295059001,-0.0398205273591854,
0.0151263088559762));
#35807=CARTESIAN_POINT('Ctrl Pts',(0.106043485420733,0.0899039768168324,
0.0230323320554937));
#35808=CARTESIAN_POINT('Ctrl Pts',(-0.0174538572390982,0.137906280269365,
0.0309383552550111));
#35809=CARTESIAN_POINT('Ctrl Pts',(-0.125086200033906,0.0606479146403327,
0.0388443784545286));
#35810=CARTESIAN_POINT('Ctrl Pts',(-0.119084788854313,-0.0717206569949895,
0.046750401654046));
#35811=CARTESIAN_POINT('Ctrl Pts',(-0.00489492837772915,-0.138925734589418,
0.0546564248535634));
#35812=CARTESIAN_POINT('Ctrl Pts',(0.113740629398734,-0.0799231888543136,
0.062562448053081));
#35813=CARTESIAN_POINT('Ctrl Pts',(0.129045816271948,0.0516898037714297,
0.0704684712525983));
#35814=CARTESIAN_POINT('Ctrl Pts',(0.0271151839788463,0.136342686033388,
0.0783744944521158));
#35815=CARTESIAN_POINT('Ctrl Pts',(-0.0994488545192835,0.097131556418157,
0.0862805176516332));
#35816=CARTESIAN_POINT('Ctrl Pts',(-0.135665746467832,-0.0303218706918135,
0.0941865408511506));
#35817=CARTESIAN_POINT('Ctrl Pts',(-0.0486330432543111,-0.130228357167641,
0.102092564050668));
#35818=CARTESIAN_POINT('Ctrl Pts',(0.0825817545836372,-0.111825131042891,
0.109998587250186));
#35819=CARTESIAN_POINT('Ctrl Pts',(0.138772738128538,0.00816897019039422,
0.117904610449703));
#35820=CARTESIAN_POINT('Ctrl Pts',(0.0688915313895657,0.120741708772585,
0.12581063364922));
#35821=CARTESIAN_POINT('Ctrl Pts',(-0.0635762130827019,0.123623095373164,
0.133716656848738));
#35822=CARTESIAN_POINT('Ctrl Pts',(-0.138286275523292,0.014195432572335,
0.141622680048255));
#35823=CARTESIAN_POINT('Ctrl Pts',(-0.0873660952430369,-0.108128486159945,
0.149528703247773));
#35824=CARTESIAN_POINT('Ctrl Pts',(0.0429243879661372,-0.132219897211806,
0.15743472644729));
#35825=CARTESIAN_POINT('Ctrl Pts',(0.134218946443888,-0.0361922458912883,
0.165340749646808));
#35826=CARTESIAN_POINT('Ctrl Pts',(0.103578348063976,0.0927153171784346,
0.173246772846325));
#35827=CARTESIAN_POINT('Ctrl Pts',(-0.0211610525014389,0.137392918706172,
0.181152796045843));
#35828=CARTESIAN_POINT('Ctrl Pts',(-0.126676071448117,0.0572518747851005,
0.18905881924536));
#35829=CARTESIAN_POINT('Ctrl Pts',(-0.117108480713923,-0.074901321664099,
0.196964842444878));
#35830=CARTESIAN_POINT('Ctrl Pts',(-0.00115024004832317,-0.139008205490464,
0.204870865644395));
#35831=CARTESIAN_POINT('Ctrl Pts',(0.115852970087698,-0.0768289890996742,
0.212776888843912));
#35832=CARTESIAN_POINT('Ctrl Pts',(0.127606135899372,0.055147786219953,
0.22068291204343));
#35833=CARTESIAN_POINT('Ctrl Pts',(0.0234317475993789,0.137023930205902,
0.228588935242947));
#35834=CARTESIAN_POINT('Ctrl Pts',(-0.102029902232137,0.0944166473397004,
0.236494958442465));
#35835=CARTESIAN_POINT('Ctrl Pts',(-0.134799481036655,-0.0339662208175969,
0.244400981641982));
#35836=CARTESIAN_POINT('Ctrl Pts',(-0.0451064993838265,-0.131491474848312,
0.252307004841499));
#35837=CARTESIAN_POINT('Ctrl Pts',(0.0855648107118161,-0.1095594241143,
0.260213028041017));
#35838=CARTESIAN_POINT('Ctrl Pts',(0.138502247321704,0.0119051136596435,
0.268119051240535));
#35839=CARTESIAN_POINT('Ctrl Pts',(0.0656132363391791,0.122554100141606,
0.276025074440052));
#35840=CARTESIAN_POINT('Ctrl Pts',(-0.066884052510702,0.121865203254083,
0.283931097639569));
#35841=CARTESIAN_POINT('Ctrl Pts',(-0.138618553097211,0.010464271673199,
0.291837120839087));
#35842=CARTESIAN_POINT('Ctrl Pts',(-0.0844209446825288,-0.110443235842333,
0.299743144038604));
#35843=CARTESIAN_POINT('Ctrl Pts',(0.046471358419155,-0.131015331511595,
0.307649167238122));
#35844=CARTESIAN_POINT('Ctrl Pts',(0.135145386671506,-0.0325626888604762,
0.315555190437639));
#35845=CARTESIAN_POINT('Ctrl Pts',(0.101042606300054,0.0954724879559945,
0.323461213637157));
#35846=CARTESIAN_POINT('Ctrl Pts',(-0.0248553070174182,0.136772869961425,
0.331367236836674));
#35847=CARTESIAN_POINT('Ctrl Pts',(-0.12817268430534,0.0538179081940093,
0.339273260036191));
#35848=CARTESIAN_POINT('Ctrl Pts',(-0.115047809886908,-0.0780295180341452,
0.347179283235709));
#35849=CARTESIAN_POINT('Ctrl Pts',(0.00259563734382704,-0.138988729439456,
0.355085306435226));
#35850=CARTESIAN_POINT('Ctrl Pts',(0.117881001348277,-0.0736795342380946,
0.362991329634744));
#35851=CARTESIAN_POINT('Ctrl Pts',(0.12607389627645,0.0585660048329233,
0.370897352834261));
#35852=CARTESIAN_POINT('Ctrl Pts',(0.0197312453245754,0.137605531147394,
0.378803376033779));
#35853=CARTESIAN_POINT('Ctrl Pts',(-0.104536836829869,0.0916332580999962,
0.386709399233296));
#35854=CARTESIAN_POINT('Ctrl Pts',(-0.133835349354862,-0.0375859482716227,
0.394615422432814));
#35855=CARTESIAN_POINT('Ctrl Pts',(-0.0415471952570256,-0.13265909245389,
0.40252144563233));
#35856=CARTESIAN_POINT('Ctrl Pts',(0.0884857325734624,-0.107214175253801,
0.410427468831849));
#35857=CARTESIAN_POINT('Ctrl Pts',(0.138131189387156,0.0156326185555932,
0.418333492031365));
#35858=CARTESIAN_POINT('Ctrl Pts',(0.062287297122381,0.124277499418049,
0.426239515230884));
#35859=CARTESIAN_POINT('Ctrl Pts',(-0.0701433255283678,0.120018824057881,
0.4341455384304));
#35860=CARTESIAN_POINT('Ctrl Pts',(-0.138850177307333,0.00672551158926456,
0.442051561629919));
#35861=CARTESIAN_POINT('Ctrl Pts',(-0.0814144942465354,-0.11267779005197,
0.449957584829435));
#35862=CARTESIAN_POINT('Ctrl Pts',(0.0499845850166584,-0.129715633233345,
0.457863608028953));
#35863=CARTESIAN_POINT('Ctrl Pts',(0.135973695209673,-0.0289094872912353,
0.465769631228471));
#35864=CARTESIAN_POINT('Ctrl Pts',(0.0984334954810092,0.0981603342078928,
0.473675654427988));
#35865=CARTESIAN_POINT('Ctrl Pts',(-0.0285315135918273,0.136053507770195,
0.481581677627505));
#35866=CARTESIAN_POINT('Ctrl Pts',(-0.129576228451988,0.0503448633385094,
0.489487700827023));
#35867=CARTESIAN_POINT('Ctrl Pts',(-0.112903600569895,-0.0811010556205559,
0.49739372402654));
#35868=CARTESIAN_POINT('Ctrl Pts',(0.00633962999064621,-0.138868330932566,
0.505299747226058));
#35869=CARTESIAN_POINT('Ctrl Pts',(0.119823436886959,-0.0704765792090683,
0.513205770425575));
#35870=CARTESIAN_POINT('Ctrl Pts',(0.124450111907394,0.0619416975118724,
0.521111793625093));
#35871=CARTESIAN_POINT('Ctrl Pts',(0.0160164158031762,0.138087213996209,
0.52901781682461));
#35872=CARTESIAN_POINT('Ctrl Pts',(-0.106967865166254,0.0887833321417318,
0.536923840024128));
#35873=CARTESIAN_POINT('Ctrl Pts',(-0.132774037183017,-0.0411783838262002,
0.544829863223645));
#35874=CARTESIAN_POINT('Ctrl Pts',(-0.0379577228913647,-0.133730383672961,
0.552735886423163));
#35875=CARTESIAN_POINT('Ctrl Pts',(0.0913424031974019,-0.104791076063462,
0.56064190962268));
#35876=CARTESIAN_POINT('Ctrl Pts',(0.137659831668342,0.0193487722984857,
0.568547932822197));
#35877=CARTESIAN_POINT('Ctrl Pts',(0.0589161298691768,0.125910658348106,
0.576453956021715));
#35878=CARTESIAN_POINT('Ctrl Pts',(-0.0733516660922674,0.11808529682354,
0.584359979221232));
#35879=CARTESIAN_POINT('Ctrl Pts',(-0.138980979661871,0.00298186797856315,
0.59226600242075));
#35880=CARTESIAN_POINT('Ctrl Pts',(-0.0783489271385985,-0.114830526693234,
0.600172025620267));
#35881=CARTESIAN_POINT('Ctrl Pts',(0.0534615168199478,-0.12832174587234,
0.608078048819785));
#35882=CARTESIAN_POINT('Ctrl Pts',(0.136703270562712,-0.0252352939724056,
0.615984072019302));
#35883=CARTESIAN_POINT('Ctrl Pts',(0.0957529101571512,0.100776904302778,
0.623890095218819));
#35884=CARTESIAN_POINT('Ctrl Pts',(-0.0321870028708045,0.135235354440354,
0.631796118418337));
#35885=CARTESIAN_POINT('Ctrl Pts',(-0.130885684740464,0.0468352620836017,
0.639702141617854));
#35886=CARTESIAN_POINT('Ctrl Pts',(-0.110677409719003,-0.0841137041290149,
0.647608164817372));
#35887=CARTESIAN_POINT('Ctrl Pts',(0.0100790193068892,-0.138647097388359,
0.655514188016889));
#35888=CARTESIAN_POINT('Ctrl Pts',(0.121678866262096,-0.0672224497442505,
0.663420211216407));
#35889=CARTESIAN_POINT('Ctrl Pts',(0.122735961854403,0.0652724131012164,
0.671326234415924));
#35890=CARTESIAN_POINT('Ctrl Pts',(0.0122899564463577,0.138468628991968,
0.679232257615441));
#35891=CARTESIAN_POINT('Ctrl Pts',(-0.109321222024174,0.0858689388531973,
0.687138280814959));
#35892=CARTESIAN_POINT('Ctrl Pts',(-0.131616315159593,-0.0447409189438641,
0.695044304014476));
#35893=CARTESIAN_POINT('Ctrl Pts',(-0.0343406886760894,-0.134704570618338,
0.702950327213994));
#35894=CARTESIAN_POINT('Ctrl Pts',(0.0941327483034478,-0.102291886006113,
0.710856350413511));
#35895=CARTESIAN_POINT('Ctrl Pts',(0.137088516418336,0.0230508765206803,
0.718762373613029));
#35896=CARTESIAN_POINT('Ctrl Pts',(0.0555021824679276,0.127452391053421,
0.726668396812546));
#35897=CARTESIAN_POINT('Ctrl Pts',(-0.0765067445957343,0.116066025541209,
0.734574420012063));
#35898=CARTESIAN_POINT('Ctrl Pts',(-0.139010865120405,-0.000763940859230431,
0.742480443211581));
#35899=CARTESIAN_POINT('Ctrl Pts',(-0.0752264694457675,-0.116899882557203,
0.750386466411098));
#35900=CARTESIAN_POINT('Ctrl Pts',(0.0568996293847587,-0.126834681679914,
0.758292489610617));
#35901=CARTESIAN_POINT('Ctrl Pts',(0.137333582544999,-0.0215427765762162,
0.766198512810132));
#35902=CARTESIAN_POINT('Ctrl Pts',(0.0930027975645983,0.103320297856606,
0.774104536009652));
#35903=CARTESIAN_POINT('Ctrl Pts',(-0.035819122070238,0.13431900488649,
0.782010559209168));
#35904=CARTESIAN_POINT('Ctrl Pts',(-0.13210009942588,0.0432916512297215,
0.789916582408685));
#35905=CARTESIAN_POINT('Ctrl Pts',(-0.108370859366875,-0.0870652729953126,
0.797822605608204));
#35906=CARTESIAN_POINT('Ctrl Pts',(0.0138111005924944,-0.138325195186183,
0.80572862880772));
#35907=CARTESIAN_POINT('Ctrl Pts',(0.123445922182148,-0.0639194978340518,
0.813634652007238));
#35908=CARTESIAN_POINT('Ctrl Pts',(0.120932728835538,0.0685557124046954,
0.821540675206756));
#35909=CARTESIAN_POINT('Ctrl Pts',(0.0085545008581314,0.138749538494654,
0.829446698406273));
#35910=CARTESIAN_POINT('Ctrl Pts',(-0.111595061352101,0.0828921197631381,
0.837352721605791));
#35911=CARTESIAN_POINT('Ctrl Pts',(-0.130363284584795,-0.0482708249720888,
0.845258744805308));
#35912=CARTESIAN_POINT('Ctrl Pts',(-0.0306982239304521,-0.135581215292453,
0.853164768004825));
#35913=CARTESIAN_POINT('Ctrl Pts',(0.0968538014257187,-0.0997179081430208,
0.861070791204343));
#35914=CARTESIAN_POINT('Ctrl Pts',(0.136419444538435,0.0267352712365894,
0.86897681440386));
#35915=CARTESIAN_POINT('Ctrl Pts',(0.0520445414416943,0.128903423908239,
0.876882837603378));
#35916=CARTESIAN_POINT('Ctrl Pts',(-0.0795998263876522,0.113958970288921,
0.884788860802895));
#35917=CARTESIAN_POINT('Ctrl Pts',(-0.138952053011478,-0.00450253390371847,
0.892694884002413));
#35918=CARTESIAN_POINT('Ctrl Pts',(-0.0720261204166176,-0.118897020856024,
0.90060090720193));
#35919=CARTESIAN_POINT('Ctrl Pts',(0.0602520802431792,-0.125231345176025,
0.908506930401448));
#35920=CARTESIAN_POINT('Ctrl Pts',(0.137949690524835,-0.017881538827179,
0.916412953600965));
#35921=CARTESIAN_POINT('Ctrl Pts',(0.0900118016872842,0.105886249500893,
0.924318976800482));
#35922=CARTESIAN_POINT('Ctrl Pts',(0.00399973323748277,0.12400080376067,
0.929589658933494));
#35923=CARTESIAN_POINT('Ctrl Pts',(-0.0334019664626807,0.112939183906322,
0.932225));
#35924=CARTESIAN_POINT('Ctrl Pts',(-0.0551480035117367,0.114734422509853,
-0.0109985226280624));
#35925=CARTESIAN_POINT('Ctrl Pts',(-0.0931442265014884,0.0964712387762041,
-0.00836318156155655));
#35926=CARTESIAN_POINT('Ctrl Pts',(-0.148934286841532,0.0195691911522949,
-0.00309249942854491));
#35927=CARTESIAN_POINT('Ctrl Pts',(-0.097581056797534,-0.114386139408358,
0.00481352377097251));
#35928=CARTESIAN_POINT('Ctrl Pts',(0.0425463629697991,-0.144059796166161,
0.01271954697049));
#35929=CARTESIAN_POINT('Ctrl Pts',(0.143957676595294,-0.0430409945474375,
0.0206255701700074));
#35930=CARTESIAN_POINT('Ctrl Pts',(0.114619704470892,0.0971749203887298,
0.0285315933695248));
#35931=CARTESIAN_POINT('Ctrl Pts',(-0.0188654300703636,0.149059388480494,
0.0364376165690423));
#35932=CARTESIAN_POINT('Ctrl Pts',(-0.13520249003877,0.065552787380297,
0.0443436397685597));
#35933=CARTESIAN_POINT('Ctrl Pts',(-0.128715717437097,-0.0775210327782809,
0.0522496629680772));
#35934=CARTESIAN_POINT('Ctrl Pts',(-0.0052908035023142,-0.150161290708834,
0.0601556861675946));
#35935=CARTESIAN_POINT('Ctrl Pts',(0.122939351496148,-0.0863869407017978,
0.0680617093671122));
#35936=CARTESIAN_POINT('Ctrl Pts',(0.139482338453993,0.0558701933356218,
0.0759677325666295));
#35937=CARTESIAN_POINT('Ctrl Pts',(0.0293081122522375,0.147369339265975,
0.0838737557661469));
#35938=CARTESIAN_POINT('Ctrl Pts',(-0.10749173576994,0.104987027230155,
0.0917797789656645));
#35939=CARTESIAN_POINT('Ctrl Pts',(-0.146637652518404,-0.032774138306667,
0.0996858021651818));
#35940=CARTESIAN_POINT('Ctrl Pts',(-0.0525662186905025,-0.140760516811213,
0.107591825364699));
#35941=CARTESIAN_POINT('Ctrl Pts',(0.089260516735274,-0.120868938074804,
0.115497848564217));
#35942=CARTESIAN_POINT('Ctrl Pts',(0.149995920728193,0.0088296319697477,
0.123403871763734));
#35943=CARTESIAN_POINT('Ctrl Pts',(0.0744631029156597,0.130506640006368,
0.131309894963252));
#35944=CARTESIAN_POINT('Ctrl Pts',(-0.0687179106383172,0.133621057448557,
0.139215918162769));
#35945=CARTESIAN_POINT('Ctrl Pts',(-0.149470115679177,0.0153434817784622,
0.147121941362287));
#35946=CARTESIAN_POINT('Ctrl Pts',(-0.0944317887874227,-0.116873328704402,
0.155027964561804));
#35947=CARTESIAN_POINT('Ctrl Pts',(0.0463958784809096,-0.142913121758123,
0.162933987761322));
#35948=CARTESIAN_POINT('Ctrl Pts',(0.145073843195134,-0.0391192774524402,
0.170840010960839));
#35949=CARTESIAN_POINT('Ctrl Pts',(0.111955200242363,0.10021362663396,0.178746034160356));
#35950=CARTESIAN_POINT('Ctrl Pts',(-0.0228724430773341,0.148504509032441,
0.186652057359874));
#35951=CARTESIAN_POINT('Ctrl Pts',(-0.136920941586459,0.0618820943336314,
0.194558080559391));
#35952=CARTESIAN_POINT('Ctrl Pts',(-0.12657957626731,-0.0809589322677961,
0.202464103758909));
#35953=CARTESIAN_POINT('Ctrl Pts',(-0.00124326519339163,-0.150250431406802,
0.210370126958426));
#35954=CARTESIAN_POINT('Ctrl Pts',(0.125222526785514,-0.0830424989377088,
0.218276150157944));
#35955=CARTESIAN_POINT('Ctrl Pts',(0.137926224580685,0.0596078385548706,
0.226182173357461));
#35956=CARTESIAN_POINT('Ctrl Pts',(0.0253267796170755,0.148105678753651,
0.234088196556978));
#35957=CARTESIAN_POINT('Ctrl Pts',(-0.110281524552332,0.102052551104597,
0.241994219756496));
#35958=CARTESIAN_POINT('Ctrl Pts',(-0.145701328261229,-0.036713223605009,
0.249900242956013));
#35959=CARTESIAN_POINT('Ctrl Pts',(-0.0487544671752176,-0.142125788564551,
0.25780626615553));
#35960=CARTESIAN_POINT('Ctrl Pts',(0.0924848261822464,-0.11841999312036,
0.265712289355049));
#35961=CARTESIAN_POINT('Ctrl Pts',(0.149703554099366,0.012867934356803,
0.273618312554565));
#35962=CARTESIAN_POINT('Ctrl Pts',(0.0709196772318203,0.132465607709839,
0.281524335754083));
#35963=CARTESIAN_POINT('Ctrl Pts',(-0.0722932700879834,0.131720996597282,
0.289430358953601));
#35964=CARTESIAN_POINT('Ctrl Pts',(-0.149829266052005,0.0113105649246307,
0.297336382153118));
#35965=CARTESIAN_POINT('Ctrl Pts',(-0.0912484505038084,-0.119375282723234,
0.305242405352635));
#35966=CARTESIAN_POINT('Ctrl Pts',(0.0502297085693762,-0.141611137350254,
0.313148428552153));
#35967=CARTESIAN_POINT('Ctrl Pts',(0.14607520885827,-0.0351961816339526,
0.32105445175167));
#35968=CARTESIAN_POINT('Ctrl Pts',(0.109214381507085,0.103193782354472,
0.328960474951188));
#35969=CARTESIAN_POINT('Ctrl Pts',(-0.0268654687609187,0.147834314125149,
0.336866498150705));
#35970=CARTESIAN_POINT('Ctrl Pts',(-0.13853859233343,0.0581704072434516,
0.344772521350223));
#35971=CARTESIAN_POINT('Ctrl Pts',(-0.124352249616671,-0.0843401201082281,
0.35267854454974));
#35972=CARTESIAN_POINT('Ctrl Pts',(0.00280555834318869,-0.150229380238954,
0.360584567749258));
#35973=CARTESIAN_POINT('Ctrl Pts',(0.127414574159504,-0.0796383333348297,
0.368490590948775));
#35974=CARTESIAN_POINT('Ctrl Pts',(0.136270065769409,0.0633025040563021,
0.376396614148293));
#35975=CARTESIAN_POINT('Ctrl Pts',(0.0213270008899901,0.148734316408943,
0.38430263734781));
#35976=CARTESIAN_POINT('Ctrl Pts',(-0.112991206354848,0.0990440565156409,
0.392208660547328));
#35977=CARTESIAN_POINT('Ctrl Pts',(-0.144659222864564,-0.0406256948841215,
0.400114683746845));
#35978=CARTESIAN_POINT('Ctrl Pts',(-0.0449073059326639,-0.143387836717301,
0.408020706946362));
#35979=CARTESIAN_POINT('Ctrl Pts',(0.0956419762819073,-0.115885073316145,
0.41592673014588));
#35980=CARTESIAN_POINT('Ctrl Pts',(0.149302487021736,0.0168968995298395,
0.423832753345397));
#35981=CARTESIAN_POINT('Ctrl Pts',(0.0673247541811015,0.134328386125389,
0.431738776544915));
#35982=CARTESIAN_POINT('Ctrl Pts',(-0.0758161353407861,0.129725292316436,
0.439644799744432));
#35983=CARTESIAN_POINT('Ctrl Pts',(-0.150079622765641,0.007269434305358,
0.447550822943949));
#35984=CARTESIAN_POINT('Ctrl Pts',(-0.0879988547449296,-0.121790555496631,
0.455456846143467));
#35985=CARTESIAN_POINT('Ctrl Pts',(0.0540270657832349,-0.140206326560007,
0.463362869342984));
#35986=CARTESIAN_POINT('Ctrl Pts',(0.146970506475833,-0.0312475290356562,
0.471268892542502));
#35987=CARTESIAN_POINT('Ctrl Pts',(0.106394260027447,0.106099006959581,
0.479174915742019));
#35988=CARTESIAN_POINT('Ctrl Pts',(-0.0308389868837996,0.147056773841187,
0.487080938941536));
#35989=CARTESIAN_POINT('Ctrl Pts',(-0.140055647479839,0.0544164814518564,
0.494986962141054));
#35990=CARTESIAN_POINT('Ctrl Pts',(-0.122034628338338,-0.0876600669114554,
0.502892985340571));
#35991=CARTESIAN_POINT('Ctrl Pts',(0.00685234470650933,-0.150099244557128,
0.51079900854009));
#35992=CARTESIAN_POINT('Ctrl Pts',(0.129514103296199,-0.076176340762594,
0.518705031739606));
#35993=CARTESIAN_POINT('Ctrl Pts',(0.134514958571949,0.066951204357981,
0.526611054939125));
#35994=CARTESIAN_POINT('Ctrl Pts',(0.0173117362067031,0.149254955140882,
0.534517078138641));
#35995=CARTESIAN_POINT('Ctrl Pts',(-0.11561884301137,0.0959636440810236,
0.542423101338159));
#35996=CARTESIAN_POINT('Ctrl Pts',(-0.143512077549549,-0.0445086670437286,
0.550329124537675));
#35997=CARTESIAN_POINT('Ctrl Pts',(-0.0410275366085405,-0.144545768130486,
0.558235147737195));
#35998=CARTESIAN_POINT('Ctrl Pts',(0.098729678853994,-0.113266007071779,
0.56614117093671));
#35999=CARTESIAN_POINT('Ctrl Pts',(0.14879300846003,0.0209135955304358,
0.57404719413623));
#36000=CARTESIAN_POINT('Ctrl Pts',(0.0636809452969333,0.136093626047241,
0.581953217335745));
#36001=CARTESIAN_POINT('Ctrl Pts',(-0.0792839490005986,0.127635391939178,
0.589859240535265));
#36002=CARTESIAN_POINT('Ctrl Pts',(-0.150221003701602,0.00322302520629366,
0.59776526373478));
#36003=CARTESIAN_POINT('Ctrl Pts',(-0.0846853612799296,-0.124117393742718,
0.605671286934299));
#36004=CARTESIAN_POINT('Ctrl Pts',(0.0577851928777687,-0.138699709187424,
0.613577310133815));
#36005=CARTESIAN_POINT('Ctrl Pts',(0.147759085906459,-0.0272761869894916,
0.621483333333334));
#36006=CARTESIAN_POINT('Ctrl Pts',(0.103496883574659,0.108927190980628,
0.62938935653285));
#36007=CARTESIAN_POINT('Ctrl Pts',(-0.0347901122093251,0.146172452729842,
0.637295379732368));
#36008=CARTESIAN_POINT('Ctrl Pts',(-0.141471005454986,0.0506230427785409,
0.645201402931886));
#36009=CARTESIAN_POINT('Ctrl Pts',(-0.119628395306551,-0.0909163620091147,
0.653107426131403));
#36010=CARTESIAN_POINT('Ctrl Pts',(0.0108941554469695,-0.149860118849825,
0.661013449330921));
#36011=CARTESIAN_POINT('Ctrl Pts',(0.131519589685118,-0.0726590350451557,
0.668919472530437));
#36012=CARTESIAN_POINT('Ctrl Pts',(0.132662177406628,0.0705512900682209,
0.676825495729956));
#36013=CARTESIAN_POINT('Ctrl Pts',(0.0132839011303035,0.149667216902378,
0.684731518929473));
#36014=CARTESIAN_POINT('Ctrl Pts',(-0.118162526543641,0.0928135505498801,
0.69263754212899));
#36015=CARTESIAN_POINT('Ctrl Pts',(-0.142260725279696,-0.0483593205820741,
0.700543565328508));
#36016=CARTESIAN_POINT('Ctrl Pts',(-0.0371179763826477,-0.145598742005641,
0.708449588528025));
#36017=CARTESIAN_POINT('Ctrl Pts',(0.101745691861845,-0.110564696145857,
0.716355611727543));
#36018=CARTESIAN_POINT('Ctrl Pts',(0.148175488346884,0.0249151057616852,
0.72426163492706));
#36019=CARTESIAN_POINT('Ctrl Pts',(0.0599908964395442,0.137760045689666,
0.732167658126578));
#36020=CARTESIAN_POINT('Ctrl Pts',(-0.0826941930548661,0.125452813002725,
0.740073681326094));
#36021=CARTESIAN_POINT('Ctrl Pts',(-0.150253306133115,-0.000825724231627113,
0.747979704525614));
#36022=CARTESIAN_POINT('Ctrl Pts',(-0.081310376229644,-0.126354107828757,
0.755885727725129));
#36023=CARTESIAN_POINT('Ctrl Pts',(0.0615013612454227,-0.137092379349209,
0.763791750924648));
#36024=CARTESIAN_POINT('Ctrl Pts',(0.148440374085997,-0.0232850389144764,
0.771697774124165));
#36025=CARTESIAN_POINT('Ctrl Pts',(0.100524356866682,0.111676280340869,
0.779603797323682));
#36026=CARTESIAN_POINT('Ctrl Pts',(-0.0387159774106656,0.145181993819149,
0.7875098205232));
#36027=CARTESIAN_POINT('Ctrl Pts',(-0.142783635380297,0.0467928439952764,
0.795415843722717));
#36028=CARTESIAN_POINT('Ctrl Pts',(-0.117135303735115,-0.0941066376761042,
0.803321866922235));
#36029=CARTESIAN_POINT('Ctrl Pts',(0.0149280671231108,-0.149512182952249,
0.811227890121752));
#36030=CARTESIAN_POINT('Ctrl Pts',(0.133429555455635,-0.0690889583890887,
0.819133913321269));
#36031=CARTESIAN_POINT('Ctrl Pts',(0.13071310873075,0.0741001247218646,
0.827039936520788));
#36032=CARTESIAN_POINT('Ctrl Pts',(0.00924634225633868,0.149970844834382,
0.834945959720303));
#36033=CARTESIAN_POINT('Ctrl Pts',(-0.120620261601548,0.0895959825586721,
0.842851982919823));
#36034=CARTESIAN_POINT('Ctrl Pts',(-0.140906356422368,-0.0521747061680897,
0.850758006119338));
#36035=CARTESIAN_POINT('Ctrl Pts',(-0.0331809289437206,-0.146546284922345,
0.858664029318857));
#36036=CARTESIAN_POINT('Ctrl Pts',(0.104686808927989,-0.107782548984136,
0.866570052518374));
#36037=CARTESIAN_POINT('Ctrl Pts',(0.147452305580495,0.0288974742383162,
0.874476075717892));
#36038=CARTESIAN_POINT('Ctrl Pts',(0.0562536202549592,0.139328430172098,
0.882382098917409));
#36039=CARTESIAN_POINT('Ctrl Pts',(-0.0860374264415029,0.123175350607342,
0.890288122116927));
#36040=CARTESIAN_POINT('Ctrl Pts',(-0.150189737621406,-0.00486667430221375,
0.898194145316444));
#36041=CARTESIAN_POINT('Ctrl Pts',(-0.0778512004163494,-0.128512763786642,
0.906100168515961));
#36042=CARTESIAN_POINT('Ctrl Pts',(0.0651249400548213,-0.135359373728788,
0.914006191715479));
#36043=CARTESIAN_POINT('Ctrl Pts',(0.149106309520794,-0.0193277002139675,
0.921912214914997));
#36044=CARTESIAN_POINT('Ctrl Pts',(0.0972914655469444,0.114449752166959,
0.929818238114513));
#36045=CARTESIAN_POINT('Ctrl Pts',(0.00432320985889779,0.134029312831529,
0.935088920247525));
#36046=CARTESIAN_POINT('Ctrl Pts',(-0.0361033354336585,0.122073089461047,
0.937724261314031));
#36047=CARTESIAN_POINT('Ctrl Pts',(-0.0592743564846289,0.123319225136769,
-0.00549926131403118));
#36048=CARTESIAN_POINT('Ctrl Pts',(-0.10011358044828,0.103689530601369,
-0.00286392024752536));
#36049=CARTESIAN_POINT('Ctrl Pts',(-0.160078034541183,0.0210334216764563,
0.00240676188548625));
#36050=CARTESIAN_POINT('Ctrl Pts',(-0.104882388816361,-0.122944882360947,
0.0103127850850037));
#36051=CARTESIAN_POINT('Ctrl Pts',(0.0457298202147887,-0.154838818620857,
0.0182188082845211));
#36052=CARTESIAN_POINT('Ctrl Pts',(0.154729058131587,-0.0462614617356896,
0.0261248314840386));
#36053=CARTESIAN_POINT('Ctrl Pts',(0.123195923521052,0.104445863960627,
0.034030854683556));
#36054=CARTESIAN_POINT('Ctrl Pts',(-0.0202770029016287,0.160212496691623,
0.0419368778830735));
#36055=CARTESIAN_POINT('Ctrl Pts',(-0.145318780043635,0.0704576601202616,
0.049842901082591));
#36056=CARTESIAN_POINT('Ctrl Pts',(-0.138346646019881,-0.0833214085615725,
0.0577489242821084));
#36057=CARTESIAN_POINT('Ctrl Pts',(-0.00568667862689953,-0.16139684682825,
0.0656549474816259));
#36058=CARTESIAN_POINT('Ctrl Pts',(0.132138073593561,-0.0928506925492821,
0.0735609706811433));
#36059=CARTESIAN_POINT('Ctrl Pts',(0.149918860636037,0.060050582899814,
0.0814669938806607));
#36060=CARTESIAN_POINT('Ctrl Pts',(0.031501040525629,0.158395992498563,
0.0893730170801781));
#36061=CARTESIAN_POINT('Ctrl Pts',(-0.115534617020597,0.112842498042153,
0.0972790402796957));
#36062=CARTESIAN_POINT('Ctrl Pts',(-0.157609558568976,-0.0352264059215207,
0.105185063479213));
#36063=CARTESIAN_POINT('Ctrl Pts',(-0.0564993941266941,-0.151292676454786,
0.113091086678731));
#36064=CARTESIAN_POINT('Ctrl Pts',(0.0959392788869109,-0.129912745106718,
0.120997109878248));
#36065=CARTESIAN_POINT('Ctrl Pts',(0.161219103327847,0.00949029374910116,
0.128903133077765));
#36066=CARTESIAN_POINT('Ctrl Pts',(0.0800346744417541,0.140271571240151,
0.136809156277283));
#36067=CARTESIAN_POINT('Ctrl Pts',(-0.0738596081939327,0.143619019523951,
0.1447151794768));
#36068=CARTESIAN_POINT('Ctrl Pts',(-0.160653955835061,0.0164915309845896,
0.152621202676318));
#36069=CARTESIAN_POINT('Ctrl Pts',(-0.101497482331809,-0.125618171248858,
0.160527225875835));
#36070=CARTESIAN_POINT('Ctrl Pts',(0.0498673689956821,-0.15360634630444,
0.168433249075353));
#36071=CARTESIAN_POINT('Ctrl Pts',(0.15592873994638,-0.0420463090135921,
0.17633927227487));
#36072=CARTESIAN_POINT('Ctrl Pts',(0.120332052420749,0.107711936089485,
0.184245295474388));
#36073=CARTESIAN_POINT('Ctrl Pts',(-0.0245838336532294,0.15961609935871,
0.192151318673905));
#36074=CARTESIAN_POINT('Ctrl Pts',(-0.147165811724802,0.0665123138821622,
0.200057341873423));
#36075=CARTESIAN_POINT('Ctrl Pts',(-0.136050671820698,-0.0870165428714931,
0.20796336507294));
#36076=CARTESIAN_POINT('Ctrl Pts',(-0.00133629033845999,-0.16149265732314,
0.215869388272457));
#36077=CARTESIAN_POINT('Ctrl Pts',(0.134592083483329,-0.0892560087757434,
0.223775411471975));
#36078=CARTESIAN_POINT('Ctrl Pts',(0.148246313261997,0.0640678908897882,
0.231681434671492));
#36079=CARTESIAN_POINT('Ctrl Pts',(0.0272218116347722,0.159187427301401,
0.23958745787101));
#36080=CARTESIAN_POINT('Ctrl Pts',(-0.118533146872527,0.109688454869495,
0.247493481070527));
#36081=CARTESIAN_POINT('Ctrl Pts',(-0.156603175485803,-0.0394602263924212,
0.255399504270045));
#36082=CARTESIAN_POINT('Ctrl Pts',(-0.0524024349666086,-0.152760102280791,
0.263305527469562));
#36083=CARTESIAN_POINT('Ctrl Pts',(0.0994048416526766,-0.127280562126421,
0.27121155066908));
#36084=CARTESIAN_POINT('Ctrl Pts',(0.160904860877029,0.0138307550539624,
0.279117573868597));
#36085=CARTESIAN_POINT('Ctrl Pts',(0.0762261181244613,0.142377115278073,
0.287023597068114));
#36086=CARTESIAN_POINT('Ctrl Pts',(-0.0777024876652646,0.141576789940481,
0.294929620267632));
#36087=CARTESIAN_POINT('Ctrl Pts',(-0.1610399790068,0.0121568581760624,
0.302835643467149));
#36088=CARTESIAN_POINT('Ctrl Pts',(-0.098075956325088,-0.128307329604135,
0.310741666666667));
#36089=CARTESIAN_POINT('Ctrl Pts',(0.0539880587195976,-0.152206943188912,
0.318647689866184));
#36090=CARTESIAN_POINT('Ctrl Pts',(0.157005031045033,-0.037829674407429,
0.326553713065702));
#36091=CARTESIAN_POINT('Ctrl Pts',(0.117386156714116,0.11091507675295,0.334459736265219));
#36092=CARTESIAN_POINT('Ctrl Pts',(-0.0288756305044191,0.158895758288873,
0.342365759464736));
#36093=CARTESIAN_POINT('Ctrl Pts',(-0.14890450036152,0.0625229062928939,
0.350271782664254));
#36094=CARTESIAN_POINT('Ctrl Pts',(-0.133656689346435,-0.0906507221823109,
0.358177805863771));
#36095=CARTESIAN_POINT('Ctrl Pts',(0.0030154793425501,-0.161470031038451,
0.366083829063289));
#36096=CARTESIAN_POINT('Ctrl Pts',(0.136948146970731,-0.0855971324315648,
0.373989852262806));
#36097=CARTESIAN_POINT('Ctrl Pts',(0.146466235262368,0.0680390032796811,
0.381895875462324));
#36098=CARTESIAN_POINT('Ctrl Pts',(0.0229227564554051,0.159863101670492,
0.389801898661841));
#36099=CARTESIAN_POINT('Ctrl Pts',(-0.121445575879827,0.106454854931286,
0.397707921861359));
#36100=CARTESIAN_POINT('Ctrl Pts',(-0.155483096374265,-0.0436654414966204,
0.405613945060876));
#36101=CARTESIAN_POINT('Ctrl Pts',(-0.0482674166083024,-0.154116580980712,
0.413519968260394));
#36102=CARTESIAN_POINT('Ctrl Pts',(0.102798219990352,-0.124555971378489,
0.421425991459911));
#36103=CARTESIAN_POINT('Ctrl Pts',(0.160473784656316,0.018161180504086,
0.429332014659428));
#36104=CARTESIAN_POINT('Ctrl Pts',(0.072362211239822,0.144379272832728,
0.437238037858946));
#36105=CARTESIAN_POINT('Ctrl Pts',(-0.0814889451532045,0.139431760574992,
0.445144061058463));
#36106=CARTESIAN_POINT('Ctrl Pts',(-0.16130906822395,0.00781335702145124,
0.453050084257981));
#36107=CARTESIAN_POINT('Ctrl Pts',(-0.0945832152433237,-0.130903320941292,
0.460956107457498));
#36108=CARTESIAN_POINT('Ctrl Pts',(0.0580695465498112,-0.150697019886669,
0.468862130657016));
#36109=CARTESIAN_POINT('Ctrl Pts',(0.157967317741994,-0.033585570780077,
0.476768153856533));
#36110=CARTESIAN_POINT('Ctrl Pts',(0.114355024573885,0.114037679711269,
0.48467417705605));
#36111=CARTESIAN_POINT('Ctrl Pts',(-0.0331464601757716,0.15806003991218,
0.492580200255568));
#36112=CARTESIAN_POINT('Ctrl Pts',(-0.15053506650769,0.0584880995652034,
0.500486223455085));
#36113=CARTESIAN_POINT('Ctrl Pts',(-0.131165656106781,-0.0942190782023548,
0.508392246654604));
#36114=CARTESIAN_POINT('Ctrl Pts',(0.00736505942237213,-0.161330158181689,
0.51629826985412));
#36115=CARTESIAN_POINT('Ctrl Pts',(0.139204769705438,-0.0818761023161199,
0.524204293053638));
#36116=CARTESIAN_POINT('Ctrl Pts',(0.144579805236504,0.0719607112040898,
0.532110316253155));
#36117=CARTESIAN_POINT('Ctrl Pts',(0.0186070566102303,0.160422696285555,
0.540016339452673));
#36118=CARTESIAN_POINT('Ctrl Pts',(-0.124269820856485,0.103143956020315,
0.547922362652189));
#36119=CARTESIAN_POINT('Ctrl Pts',(-0.154250117916081,-0.047838950261257,
0.555828385851708));
#36120=CARTESIAN_POINT('Ctrl Pts',(-0.0440973503257164,-0.15536115258801,
0.563734409051225));
#36121=CARTESIAN_POINT('Ctrl Pts',(0.106116954510586,-0.121740938080097,
0.571640432250743));
#36122=CARTESIAN_POINT('Ctrl Pts',(0.159926185251717,0.022478418762386,
0.579546455450259));
#36123=CARTESIAN_POINT('Ctrl Pts',(0.06844576072469,0.146276593746376,0.587452478649778));
#36124=CARTESIAN_POINT('Ctrl Pts',(-0.08521623190893,0.137185487054817,
0.595358501849294));
#36125=CARTESIAN_POINT('Ctrl Pts',(-0.161461027741333,0.00346418243402402,
0.603264525048813));
#36126=CARTESIAN_POINT('Ctrl Pts',(-0.0910217954212606,-0.133404260792202,
0.611170548248329));
#36127=CARTESIAN_POINT('Ctrl Pts',(0.0621088689355897,-0.149077672502509,
0.619076571447848));
#36128=CARTESIAN_POINT('Ctrl Pts',(0.158814901250206,-0.0293170800065776,
0.626982594647363));
#36129=CARTESIAN_POINT('Ctrl Pts',(0.111240856992166,0.117077477658479,
0.634888617846883));
#36130=CARTESIAN_POINT('Ctrl Pts',(-0.0373932215478457,0.15710955101933,
0.642794641046398));
#36131=CARTESIAN_POINT('Ctrl Pts',(-0.152056326169508,0.0544108234734799,
0.650700664245917));
#36132=CARTESIAN_POINT('Ctrl Pts',(-0.1285793808941,-0.0977190198892145,
0.658606687445434));
#36133=CARTESIAN_POINT('Ctrl Pts',(0.0117092915870499,-0.161073140311291,
0.666512710644951));
#36134=CARTESIAN_POINT('Ctrl Pts',(0.14136031310814,-0.0780956203460609,
0.67441873384447));
#36135=CARTESIAN_POINT('Ctrl Pts',(0.142588392958853,0.0758301670352254,
0.682324757043986));
#36136=CARTESIAN_POINT('Ctrl Pts',(0.0142778458142493,0.160865804812787,
0.690230780243504));
#36137=CARTESIAN_POINT('Ctrl Pts',(-0.127003831063107,0.0997581622465629,
0.698136803443022));
#36138=CARTESIAN_POINT('Ctrl Pts',(-0.152905135399799,-0.0519777222202838,
0.706042826642539));
#36139=CARTESIAN_POINT('Ctrl Pts',(-0.0398952640892059,-0.156492913392945,
0.713948849842056));
#36140=CARTESIAN_POINT('Ctrl Pts',(0.109358635420242,-0.118837506285601,
0.721854873041575));
#36141=CARTESIAN_POINT('Ctrl Pts',(0.159262460275431,0.0267793350026898,
0.729760896241091));
#36142=CARTESIAN_POINT('Ctrl Pts',(0.0644796104111608,0.148067700325911,
0.737666919440608));
#36143=CARTESIAN_POINT('Ctrl Pts',(-0.0888816415139979,0.134839600464242,
0.745572942640127));
#36144=CARTESIAN_POINT('Ctrl Pts',(-0.161495747145824,-0.000887507604023794,
0.753478965839642));
#36145=CARTESIAN_POINT('Ctrl Pts',(-0.0873942830135206,-0.135808333100311,
0.761384989039162));
#36146=CARTESIAN_POINT('Ctrl Pts',(0.0661030931060867,-0.147350077018504,
0.769291012238677));
#36147=CARTESIAN_POINT('Ctrl Pts',(0.159547165626996,-0.0250273012527367,
0.777197035438197));
#36148=CARTESIAN_POINT('Ctrl Pts',(0.108045916168766,0.120032262825132,
0.785103058637712));
#36149=CARTESIAN_POINT('Ctrl Pts',(-0.0416128327510934,0.156044982751807,
0.793009081837232));
#36150=CARTESIAN_POINT('Ctrl Pts',(-0.153467171334714,0.0502940367608314,
0.800915105036747));
#36151=CARTESIAN_POINT('Ctrl Pts',(-0.125899748103356,-0.101148002356896,
0.808821128236267));
#36152=CARTESIAN_POINT('Ctrl Pts',(0.0160450336537275,-0.160699170718315,
0.816727151435783));
#36153=CARTESIAN_POINT('Ctrl Pts',(0.143413188729122,-0.0742584189441255,
0.824633174635301));
#36154=CARTESIAN_POINT('Ctrl Pts',(0.140493488625962,0.0796445370390336,
0.832539197834818));
#36155=CARTESIAN_POINT('Ctrl Pts',(0.00993818365454583,0.161192151174111,
0.840445221034335));
#36156=CARTESIAN_POINT('Ctrl Pts',(-0.129645461850996,0.0962998453542059,
0.848351244233853));
#36157=CARTESIAN_POINT('Ctrl Pts',(-0.151449428259942,-0.0560785873640905,
0.85625726743337));
#36158=CARTESIAN_POINT('Ctrl Pts',(-0.0356636339569891,-0.157511354552237,
0.864163290632887));
#36159=CARTESIAN_POINT('Ctrl Pts',(0.112519816430259,-0.115847189825252,
0.872069313832405));
#36160=CARTESIAN_POINT('Ctrl Pts',(0.158485166622555,0.0310596772400429,
0.879975337031923));
#36161=CARTESIAN_POINT('Ctrl Pts',(0.0604626990682241,0.149753436435956,
0.88788136023144));
#36162=CARTESIAN_POINT('Ctrl Pts',(-0.0924750264953536,0.132391730925763,
0.895787383430957));
#36163=CARTESIAN_POINT('Ctrl Pts',(-0.161427422231335,-0.00523081470070893,
0.903693406630475));
#36164=CARTESIAN_POINT('Ctrl Pts',(-0.083676280416081,-0.13812850671726,
0.911599429829993));
#36165=CARTESIAN_POINT('Ctrl Pts',(0.0699977998664634,-0.145487402281552,
0.91950545302951));
#36166=CARTESIAN_POINT('Ctrl Pts',(0.160262928516753,-0.020773861600756,
0.927411476229027));
#36167=CARTESIAN_POINT('Ctrl Pts',(0.104571129406605,0.123013254833025,
0.935317499428545));
#36168=CARTESIAN_POINT('Ctrl Pts',(0.0046466864803128,0.144057821902388,
0.940588181561556));
#36169=CARTESIAN_POINT('Ctrl Pts',(-0.0388047044046363,0.131206995015772,
0.943223522628062));
#36170=CARTESIAN_POINT('Ctrl Pts',(-0.0634007094575211,0.131904027763685,
0.));
#36171=CARTESIAN_POINT('Ctrl Pts',(-0.107082934395072,0.110907822426533,
0.00263534106650582));
#36172=CARTESIAN_POINT('Ctrl Pts',(-0.171221782240834,0.0224976522006178,
0.00790602319951745));
#36173=CARTESIAN_POINT('Ctrl Pts',(-0.112183720835187,-0.131503625313535,
0.0158120463990349));
#36174=CARTESIAN_POINT('Ctrl Pts',(0.0489132774597784,-0.165617841075552,
0.0237180695985523));
#36175=CARTESIAN_POINT('Ctrl Pts',(0.165500439667881,-0.0494819289239417,
0.0316240927980698));
#36176=CARTESIAN_POINT('Ctrl Pts',(0.131772142571212,0.111716807532525,
0.0395301159975872));
#36177=CARTESIAN_POINT('Ctrl Pts',(-0.0216885757328939,0.171365604902752,
0.0474361391971047));
#36178=CARTESIAN_POINT('Ctrl Pts',(-0.155435070048499,0.0753625328602259,
0.055342162396622));
#36179=CARTESIAN_POINT('Ctrl Pts',(-0.147977574602665,-0.0891217843448639,
0.0632481855961397));
#36180=CARTESIAN_POINT('Ctrl Pts',(-0.00608255375148451,-0.172632402947666,
0.0711542087956569));
#36181=CARTESIAN_POINT('Ctrl Pts',(0.141336795690974,-0.0993144443967663,
0.0790602319951745));
#36182=CARTESIAN_POINT('Ctrl Pts',(0.160355382818083,0.0642309724640062,
0.0869662551946919));
#36183=CARTESIAN_POINT('Ctrl Pts',(0.03369396879902,0.16942264573115,0.0948722783942093));
#36184=CARTESIAN_POINT('Ctrl Pts',(-0.123577498271253,0.120697968854151,
0.102778301593727));
#36185=CARTESIAN_POINT('Ctrl Pts',(-0.168581464619548,-0.0376786735363742,
0.110684324793244));
#36186=CARTESIAN_POINT('Ctrl Pts',(-0.0604325695628853,-0.161824836098358,
0.118590347992762));
#36187=CARTESIAN_POINT('Ctrl Pts',(0.102618041038548,-0.138956552138631,
0.126496371192279));
#36188=CARTESIAN_POINT('Ctrl Pts',(0.172442285927502,0.0101509555284547,
0.134402394391796));
#36189=CARTESIAN_POINT('Ctrl Pts',(0.085606245967848,0.150036502473934,
0.142308417591314));
#36190=CARTESIAN_POINT('Ctrl Pts',(-0.0790013057495479,0.153616981599344,
0.150214440790831));
#36191=CARTESIAN_POINT('Ctrl Pts',(-0.171837795990946,0.0176395801907167,
0.158120463990349));
#36192=CARTESIAN_POINT('Ctrl Pts',(-0.108563175876194,-0.134363013793315,
0.166026487189866));
#36193=CARTESIAN_POINT('Ctrl Pts',(0.0533388595104543,-0.164299570850757,
0.173932510389384));
#36194=CARTESIAN_POINT('Ctrl Pts',(0.166783636697626,-0.0449733405747439,
0.181838533588901));
#36195=CARTESIAN_POINT('Ctrl Pts',(0.128708904599136,0.11521024554501,0.189744556788419));
#36196=CARTESIAN_POINT('Ctrl Pts',(-0.0262952242291247,0.170727689684979,
0.197650579987936));
#36197=CARTESIAN_POINT('Ctrl Pts',(-0.157410681863144,0.071142533430693,
0.205556603187454));
#36198=CARTESIAN_POINT('Ctrl Pts',(-0.145521767374085,-0.0930741534751901,
0.213462626386971));
#36199=CARTESIAN_POINT('Ctrl Pts',(-0.00142931548352814,-0.172734883239477,
0.221368649586489));
#36200=CARTESIAN_POINT('Ctrl Pts',(0.143961640181145,-0.0954695186137778,
0.229274672786006));
#36201=CARTESIAN_POINT('Ctrl Pts',(0.15856640194331,0.0685279432247057,
0.237180695985524));
#36202=CARTESIAN_POINT('Ctrl Pts',(0.0291168436524689,0.17026917584915,
0.24508671918504));
#36203=CARTESIAN_POINT('Ctrl Pts',(-0.126784769192722,0.117324358634392,
0.252992742384559));
#36204=CARTESIAN_POINT('Ctrl Pts',(-0.167505022710376,-0.0422072291798334,
0.260898765584075));
#36205=CARTESIAN_POINT('Ctrl Pts',(-0.0560504027579997,-0.16339441599703,
0.268804788783594));
#36206=CARTESIAN_POINT('Ctrl Pts',(0.106324857123107,-0.136141131132482,
0.27671081198311));
#36207=CARTESIAN_POINT('Ctrl Pts',(0.172106167654692,0.0147935757511219,
0.284616835182629));
#36208=CARTESIAN_POINT('Ctrl Pts',(0.0815325590171024,0.152288622846307,
0.292522858382145));
#36209=CARTESIAN_POINT('Ctrl Pts',(-0.0831117052425459,0.151432583283679,
0.300428881581663));
#36210=CARTESIAN_POINT('Ctrl Pts',(-0.172250691961594,0.0130031514274941,
0.30833490478118));
#36211=CARTESIAN_POINT('Ctrl Pts',(-0.104903462146368,-0.137239376485036,
0.316240927980698));
#36212=CARTESIAN_POINT('Ctrl Pts',(0.0577464088698189,-0.16280274902757,
0.324146951180215));
#36213=CARTESIAN_POINT('Ctrl Pts',(0.167934853231796,-0.0404631671809053,
0.332052974379733));
#36214=CARTESIAN_POINT('Ctrl Pts',(0.125557931921148,0.118636371151428,
0.33995899757925));
#36215=CARTESIAN_POINT('Ctrl Pts',(-0.0308857922479196,0.169957202452597,
0.347865020778768));
#36216=CARTESIAN_POINT('Ctrl Pts',(-0.15927040838961,0.0668754053423362,
0.355771043978284));
#36217=CARTESIAN_POINT('Ctrl Pts',(-0.142961129076198,-0.0969613242563938,
0.363677067177803));
#36218=CARTESIAN_POINT('Ctrl Pts',(0.0032254003419117,-0.172710681837949,
0.371583090377319));
#36219=CARTESIAN_POINT('Ctrl Pts',(0.146481719781958,-0.0915559315282998,
0.379489113576838));
#36220=CARTESIAN_POINT('Ctrl Pts',(0.156662404755327,0.0727755025030601,
0.387395136776354));
#36221=CARTESIAN_POINT('Ctrl Pts',(0.0245185120208197,0.170991886932041,
0.395301159975873));
#36222=CARTESIAN_POINT('Ctrl Pts',(-0.129899945404805,0.113865653346931,
0.403207183175389));
#36223=CARTESIAN_POINT('Ctrl Pts',(-0.166306969883967,-0.0467051881091194,
0.411113206374907));
#36224=CARTESIAN_POINT('Ctrl Pts',(-0.0516275272839405,-0.164845325244123,
0.419019229574424));
#36225=CARTESIAN_POINT('Ctrl Pts',(0.109954463698797,-0.133226869440833,
0.426925252773942));
#36226=CARTESIAN_POINT('Ctrl Pts',(0.171645082290897,0.0194254614783324,
0.434831275973459));
#36227=CARTESIAN_POINT('Ctrl Pts',(0.0773996682985425,0.154430159540067,
0.442737299172977));
#36228=CARTESIAN_POINT('Ctrl Pts',(-0.0871617549656229,0.149138228833548,
0.450643322372495));
#36229=CARTESIAN_POINT('Ctrl Pts',(-0.172538513682259,0.00835727973754467,
0.458549345572012));
#36230=CARTESIAN_POINT('Ctrl Pts',(-0.101167575741718,-0.140016086385953,
0.466455368771529));
#36231=CARTESIAN_POINT('Ctrl Pts',(0.0621120273163875,-0.161187713213332,
0.474361391971047));
#36232=CARTESIAN_POINT('Ctrl Pts',(0.168964129008155,-0.0359236125244978,
0.482267415170563));
#36233=CARTESIAN_POINT('Ctrl Pts',(0.122315789120323,0.121976352462958,
0.490173438370083));
#36234=CARTESIAN_POINT('Ctrl Pts',(-0.0354539334677437,0.169063305983172,
0.498079461569598));
#36235=CARTESIAN_POINT('Ctrl Pts',(-0.161014485535541,0.0625597176785504,
0.505985484769117));
#36236=CARTESIAN_POINT('Ctrl Pts',(-0.140296683875224,-0.100778089493254,
0.513891507968634));
#36237=CARTESIAN_POINT('Ctrl Pts',(0.00787777413823514,-0.17256107180625,
0.521797531168151));
#36238=CARTESIAN_POINT('Ctrl Pts',(0.148895436114678,-0.0875758638696457,
0.529703554367669));
#36239=CARTESIAN_POINT('Ctrl Pts',(0.154644651901059,0.0769702180501986,
0.537609577567186));
#36240=CARTESIAN_POINT('Ctrl Pts',(0.0199023770137573,0.171590437430228,
0.545515600766704));
#36241=CARTESIAN_POINT('Ctrl Pts',(-0.132920798701601,0.110324267959608,
0.553421623966221));
#36242=CARTESIAN_POINT('Ctrl Pts',(-0.164988158282613,-0.0511692334787857,
0.561327647165738));
#36243=CARTESIAN_POINT('Ctrl Pts',(-0.0471671640428923,-0.166176537045534,
0.569233670365257));
#36244=CARTESIAN_POINT('Ctrl Pts',(0.113504230167178,-0.130215869088414,
0.577139693564773));
#36245=CARTESIAN_POINT('Ctrl Pts',(0.171059362043405,0.0240432419943362,
0.585045716764291));
#36246=CARTESIAN_POINT('Ctrl Pts',(0.0732105761524465,0.156459561445511,
0.592951739963808));
#36247=CARTESIAN_POINT('Ctrl Pts',(-0.0911485148172611,0.146735582170455,
0.600857763163326));
#36248=CARTESIAN_POINT('Ctrl Pts',(-0.172701051781065,0.00370533966175465,
0.608763786362843));
#36249=CARTESIAN_POINT('Ctrl Pts',(-0.0973582295625918,-0.142691127841686,
0.616669809562361));
#36250=CARTESIAN_POINT('Ctrl Pts',(0.0664325449934107,-0.159455635817593,
0.624575832761878));
#36251=CARTESIAN_POINT('Ctrl Pts',(0.169870716593952,-0.0313579730236637,
0.632481855961396));
#36252=CARTESIAN_POINT('Ctrl Pts',(0.118984830409674,0.12522776433633,0.640387879160913));
#36253=CARTESIAN_POINT('Ctrl Pts',(-0.0399963308863663,0.168046649308817,
0.648293902360431));
#36254=CARTESIAN_POINT('Ctrl Pts',(-0.162641646884031,0.0581986041684188,
0.656199925559947));
#36255=CARTESIAN_POINT('Ctrl Pts',(-0.137530366481649,-0.104521677769314,
0.664105948759466));
#36256=CARTESIAN_POINT('Ctrl Pts',(0.0125244277271302,-0.172286161772757,
0.672011971958982));
#36257=CARTESIAN_POINT('Ctrl Pts',(0.151201036531162,-0.0835322056469662,
0.679917995158501));
#36258=CARTESIAN_POINT('Ctrl Pts',(0.152514608511077,0.08110904400223,0.687824018358017));
#36259=CARTESIAN_POINT('Ctrl Pts',(0.015271790498195,0.172064392723197,
0.695730041557536));
#36260=CARTESIAN_POINT('Ctrl Pts',(-0.135845135582574,0.106702773943246,
0.703636064757053));
#36261=CARTESIAN_POINT('Ctrl Pts',(-0.163549545519903,-0.0555961238584937,
0.71154208795657));
#36262=CARTESIAN_POINT('Ctrl Pts',(-0.042672551795764,-0.167387084780248,
0.719448111156087));
#36263=CARTESIAN_POINT('Ctrl Pts',(0.116971578978639,-0.127110316425345,
0.727354134355605));
#36264=CARTESIAN_POINT('Ctrl Pts',(0.170349432203978,0.0286435642436946,
0.735260157555123));
#36265=CARTESIAN_POINT('Ctrl Pts',(0.0689683243827774,0.158375354962157,
0.74316618075464));
#36266=CARTESIAN_POINT('Ctrl Pts',(-0.0950690899731296,0.144226387925758,
0.751072203954158));
#36267=CARTESIAN_POINT('Ctrl Pts',(-0.172738188158534,-0.000949290976420475,
0.758978227153675));
#36268=CARTESIAN_POINT('Ctrl Pts',(-0.0934781897973971,-0.145262558371866,
0.766884250353192));
#36269=CARTESIAN_POINT('Ctrl Pts',(0.0707048249667505,-0.157607774687799,
0.77479027355271));
#36270=CARTESIAN_POINT('Ctrl Pts',(0.170653957167994,-0.026769563590997,
0.782696296752227));
#36271=CARTESIAN_POINT('Ctrl Pts',(0.115567475470849,0.128388245309395,
0.790602319951745));
#36272=CARTESIAN_POINT('Ctrl Pts',(-0.044509688091521,0.166907971684466,
0.798508343151262));
#36273=CARTESIAN_POINT('Ctrl Pts',(-0.164150707289131,0.0537952295263864,
0.806414366350779));
#36274=CARTESIAN_POINT('Ctrl Pts',(-0.134664192471597,-0.108189367037688,
0.814320389550297));
#36275=CARTESIAN_POINT('Ctrl Pts',(0.0171620001843438,-0.171886158484381,
0.822226412749814));
#36276=CARTESIAN_POINT('Ctrl Pts',(0.153396822002609,-0.0794278794991626,
0.830132435949332));
#36277=CARTESIAN_POINT('Ctrl Pts',(0.150273868521174,0.0851889493562029,
0.838038459148849));
#36278=CARTESIAN_POINT('Ctrl Pts',(0.010630025052753,0.17241345751384,0.845944482348367));
#36279=CARTESIAN_POINT('Ctrl Pts',(-0.138670662100443,0.10300370814974,
0.853850505547884));
#36280=CARTESIAN_POINT('Ctrl Pts',(-0.161992500097515,-0.0599824685600915,
0.861756528747401));
#36281=CARTESIAN_POINT('Ctrl Pts',(-0.0381463389702577,-0.16847642418213,
0.869662551946919));
#36282=CARTESIAN_POINT('Ctrl Pts',(0.120352823932529,-0.123911830666367,
0.877568575146436));
#36283=CARTESIAN_POINT('Ctrl Pts',(0.169518027664615,0.0332218802417698,
0.885474598345955));
#36284=CARTESIAN_POINT('Ctrl Pts',(0.064671777881489,0.160178442699814,
0.89338062154547));
#36285=CARTESIAN_POINT('Ctrl Pts',(-0.0989126265492044,0.141608111244184,
0.90128664474499));
#36286=CARTESIAN_POINT('Ctrl Pts',(-0.172665106841263,-0.00559495509920419,
0.909192667944505));
#36287=CARTESIAN_POINT('Ctrl Pts',(-0.0895013604158129,-0.147744249647878,
0.917098691144024));
#36288=CARTESIAN_POINT('Ctrl Pts',(0.0748706596781056,-0.155615430834315,
0.925004714343541));
#36289=CARTESIAN_POINT('Ctrl Pts',(0.171419547512711,-0.0222200229875446,
0.932910737543058));
#36290=CARTESIAN_POINT('Ctrl Pts',(0.111850793266265,0.131576757499091,
0.940816760742576));
#36291=CARTESIAN_POINT('Ctrl Pts',(0.00497016310172783,0.154086330973247,
0.946087442875587));
#36292=CARTESIAN_POINT('Ctrl Pts',(-0.0415060733756141,0.140340900570497,
0.948722783942093));
#36293=CARTESIAN_POINT('Ctrl Pts',(-0.146190615322833,-9.92620605964336E-5,
0.858934495415709));
#36294=CARTESIAN_POINT('Ctrl Pts',(-0.146299982018485,-0.0174419138812775,
0.85987517319294));
#36295=CARTESIAN_POINT('Ctrl Pts',(-0.143444813888727,-0.0347497500736094,
0.860815850970171));
#36296=CARTESIAN_POINT('Ctrl Pts',(-0.13746450024346,-0.0509004317121259,
0.861756528747401));
#36297=CARTESIAN_POINT('Ctrl Pts',(-0.120710446388429,-0.0961471204341042,
0.864391869813907));
#36298=CARTESIAN_POINT('Ctrl Pts',(-0.0794283926793434,-0.132311772308117,
0.867027210880413));
#36299=CARTESIAN_POINT('Ctrl Pts',(-0.032370838674336,-0.142966665992496,
0.869662551946919));
#36300=CARTESIAN_POINT('Ctrl Pts',(0.014686715330672,-0.153621559676876,
0.872297893013425));
#36301=CARTESIAN_POINT('Ctrl Pts',(0.0675197696316001,-0.138766695171622,
0.874933234079931));
#36302=CARTESIAN_POINT('Ctrl Pts',(0.10213049740408,-0.105150311100971,
0.877568575146437));
#36303=CARTESIAN_POINT('Ctrl Pts',(0.136741225176558,-0.0715339270303214,
0.880203916212942));
#36304=CARTESIAN_POINT('Ctrl Pts',(0.153129626420586,-0.019156023394278,
0.882839257279448));
#36305=CARTESIAN_POINT('Ctrl Pts',(0.143849452078747,0.028192355500085,
0.885474598345954));
#36306=CARTESIAN_POINT('Ctrl Pts',(0.134569277736908,0.0755407343944486,
0.88810993941246));
#36307=CARTESIAN_POINT('Ctrl Pts',(0.0996205278091978,0.117859588547133,
0.890745280478965));
#36308=CARTESIAN_POINT('Ctrl Pts',(0.0548820854402278,0.135923960380868,
0.893380621545471));
#36309=CARTESIAN_POINT('Ctrl Pts',(0.0101436430712571,0.153988332214605,
0.896015962611977));
#36310=CARTESIAN_POINT('Ctrl Pts',(-0.0443844917389754,0.147798221729394,
0.898651303678484));
#36311=CARTESIAN_POINT('Ctrl Pts',(-0.0839406391927675,0.120169322096223,
0.901286644744989));
#36312=CARTESIAN_POINT('Ctrl Pts',(-0.0957651970765149,0.111910188080244,
0.902074429829993));
#36313=CARTESIAN_POINT('Ctrl Pts',(-0.106251862209464,0.10173528965009,
0.902862214914997));
#36314=CARTESIAN_POINT('Ctrl Pts',(-0.115101970897794,0.0902398078595192,
0.903650000000001));
#36315=CARTESIAN_POINT('Ctrl Pts',(-0.0686121729278153,-0.0959472995825293,
-5.42101086242752E-19));
#36316=CARTESIAN_POINT('Ctrl Pts',(-0.0716149353959019,-0.0943161956304311,
-1.06730581618305E-18));
#36317=CARTESIAN_POINT('Ctrl Pts',(-0.0745354620527207,-0.0925505885939475,
1.1783117230653E-17));
#36318=CARTESIAN_POINT('Ctrl Pts',(-0.0773634912799965,-0.0906526488910235,
6.72205346941013E-18));
#36319=CARTESIAN_POINT('Ctrl Pts',(-0.0815539383946836,-0.0878403667988651,
-2.29049000805066E-18));
#36320=CARTESIAN_POINT('Ctrl Pts',(-0.0855414709026766,-0.0847378275400617,
-2.5182094749946E-17));
#36321=CARTESIAN_POINT('Ctrl Pts',(-0.089317923041959,-0.0813786482814292,
-3.31765864780564E-17));
#36322=CARTESIAN_POINT('Ctrl Pts',(-0.0927862368571965,-0.0782935601084891,
-4.05187703807701E-17));
#36323=CARTESIAN_POINT('Ctrl Pts',(-0.0960787339139733,-0.0749884873641515,
4.97114916498215E-19));
#36324=CARTESIAN_POINT('Ctrl Pts',(-0.0991698906024268,-0.0715076841230725,
-8.67361737988404E-19));
#36325=CARTESIAN_POINT('Ctrl Pts',(-0.103663297594998,-0.0664478740909087,
-2.85080986385392E-18));
#36326=CARTESIAN_POINT('Ctrl Pts',(-0.107740134647113,-0.0610110581939007,
-1.51788304147971E-17));
#36327=CARTESIAN_POINT('Ctrl Pts',(-0.111378619976329,-0.0552695407791115,
-1.51788304147971E-17));
#36328=CARTESIAN_POINT('Ctrl Pts',(-0.113566215904755,-0.0518175218802795,
-1.51788304147971E-17));
#36329=CARTESIAN_POINT('Ctrl Pts',(-0.115595886809481,-0.0482525855570875,
-3.79982201238933E-17));
#36330=CARTESIAN_POINT('Ctrl Pts',(-0.117451481229743,-0.0446106777439056,
-3.20923843055709E-17));
#36331=CARTESIAN_POINT('Ctrl Pts',(-0.121759272594108,-0.0361559319998316,
-1.83818944163349E-17));
#36332=CARTESIAN_POINT('Ctrl Pts',(-0.125146870804877,-0.027267170883122,
-1.0758832179559E-17));
#36333=CARTESIAN_POINT('Ctrl Pts',(-0.127551512867323,-0.0181239349359946,
-1.21430643318376E-17));
#36334=CARTESIAN_POINT('Ctrl Pts',(-0.128525246808636,-0.0144214798745123,
-1.27035942545157E-17));
#36335=CARTESIAN_POINT('Ctrl Pts',(-0.129337364222068,-0.0106768832185224,
-3.87407706984377E-19));
#36336=CARTESIAN_POINT('Ctrl Pts',(-0.129981634111732,-0.00690081199580598,
2.60208521396521E-18));
#36337=CARTESIAN_POINT('Ctrl Pts',(-0.130488787940845,-0.00392837915310221,
4.95534245334234E-18));
#36338=CARTESIAN_POINT('Ctrl Pts',(-0.130891436982594,-0.000937368841373321,
-5.77147351242312E-18));
#36339=CARTESIAN_POINT('Ctrl Pts',(-0.131185766414779,0.00205408358364406,
-5.20417042793042E-18));
#36340=CARTESIAN_POINT('Ctrl Pts',(-0.131681056523625,0.00708802390756766,
-4.24952717536476E-18));
#36341=CARTESIAN_POINT('Ctrl Pts',(-0.131871567589099,0.0121324651245783,
-2.3640808795201E-17));
#36342=CARTESIAN_POINT('Ctrl Pts',(-0.131747571113314,0.0171617682916428,
-1.73472347597681E-17));
#36343=CARTESIAN_POINT('Ctrl Pts',(-0.131588224313727,0.0236248823338087,
-9.16854279395534E-18));
#36344=CARTESIAN_POINT('Ctrl Pts',(-0.130910003388584,0.0300630957896326,
1.9164721863282E-18));
#36345=CARTESIAN_POINT('Ctrl Pts',(-0.129749448943416,0.0364359420359482,
1.73472347597681E-18));
#36346=CARTESIAN_POINT('Ctrl Pts',(-0.129188162258574,0.039518084159911,
1.64682313529719E-18));
#36347=CARTESIAN_POINT('Ctrl Pts',(-0.128513877700937,0.0425849598402651,
-2.5119873647686E-17));
#36348=CARTESIAN_POINT('Ctrl Pts',(-0.127729776371406,0.0456319959092621,
-2.60208521396521E-17));
#36349=CARTESIAN_POINT('Ctrl Pts',(-0.126905460209866,0.0488353077541379,
-2.69680398361349E-17));
#36350=CARTESIAN_POINT('Ctrl Pts',(-0.125961589290349,0.0520090496451376,
-6.80234412585701E-18));
#36351=CARTESIAN_POINT('Ctrl Pts',(-0.124905367512152,0.0551421622546814,
-8.67361737988404E-18));
#36352=CARTESIAN_POINT('Ctrl Pts',(-0.122242239861443,0.0630419035736882,
-1.33917927173935E-17));
#36353=CARTESIAN_POINT('Ctrl Pts',(-0.118863777535182,0.0706951392673794,
8.60987302363936E-19));
#36354=CARTESIAN_POINT('Ctrl Pts',(-0.114842094503769,0.0780194918792452,
1.73472347597681E-18));
#36355=CARTESIAN_POINT('Ctrl Pts',(-0.112169428435535,0.0828869935059547,
2.31537714896978E-18));
#36356=CARTESIAN_POINT('Ctrl Pts',(-0.109212095329563,0.0876093199712314,
1.58690079118504E-17));
#36357=CARTESIAN_POINT('Ctrl Pts',(-0.105985186696901,0.0921609434032714,
1.90819582357449E-17));
#36358=CARTESIAN_POINT('Ctrl Pts',(-0.104153982707569,0.0947438956760198,
2.09052411731938E-17));
#36359=CARTESIAN_POINT('Ctrl Pts',(-0.102235981964729,0.0972711925776025,
1.37027400976072E-17));
#36360=CARTESIAN_POINT('Ctrl Pts',(-0.10024275281245,0.0997277902811201,
1.21430643318376E-17));
#36361=CARTESIAN_POINT('Ctrl Pts',(-0.0937332858648147,0.107750521403832,
7.04949150570437E-18));
#36362=CARTESIAN_POINT('Ctrl Pts',(-0.0864043214638765,0.115051138974542,
-2.08047340785725E-18));
#36363=CARTESIAN_POINT('Ctrl Pts',(-0.0783638198438572,0.121477900017692,
0.));
#36364=CARTESIAN_POINT('Ctrl Pts',(-0.0736196559743728,0.125269903176152,
1.22754863308587E-18));
#36365=CARTESIAN_POINT('Ctrl Pts',(-0.0686268317545984,0.128757413629593,
6.34938948147863E-19));
#36366=CARTESIAN_POINT('Ctrl Pts',(-0.0634007094575211,0.131904027763685,
0.));
#36367=CARTESIAN_POINT('Origin',(0.,0.,0.));
#36368=CARTESIAN_POINT('Origin',(-0.0577350269189626,-0.1,-0.3));
#36369=CARTESIAN_POINT('',(-0.0577350269189626,-0.1,-0.3));
#36370=CARTESIAN_POINT('',(0.0577350269189626,-0.1,-0.3));
#36371=CARTESIAN_POINT('',(-0.0288675134594813,-0.1,-0.3));
#36372=CARTESIAN_POINT('',(-0.0577350269189626,-0.1,-0.1));
#36373=CARTESIAN_POINT('',(-0.0577350269189626,-0.1,-0.3));
#36374=CARTESIAN_POINT('',(0.0577350269189626,-0.1,-0.1));
#36375=CARTESIAN_POINT('',(-0.0577350269189626,-0.1,-0.1));
#36376=CARTESIAN_POINT('',(0.0577350269189626,-0.1,-0.3));
#36377=CARTESIAN_POINT('Origin',(-0.115470053837925,1.41410031829988E-17,
-0.3));
#36378=CARTESIAN_POINT('',(-0.115470053837925,1.41410031829988E-17,-0.3));
#36379=CARTESIAN_POINT('',(-0.101036297108185,-0.025,-0.3));
#36380=CARTESIAN_POINT('',(-0.115470053837925,1.38777878078145E-17,-0.1));
#36381=CARTESIAN_POINT('',(-0.115470053837925,1.41410031829988E-17,-0.3));
#36382=CARTESIAN_POINT('',(-0.115470053837925,1.41410031829988E-17,-0.1));
#36383=CARTESIAN_POINT('Origin',(-0.0577350269189626,0.1,-0.3));
#36384=CARTESIAN_POINT('',(-0.0577350269189626,0.1,-0.3));
#36385=CARTESIAN_POINT('',(-0.0721687836487032,0.075,-0.3));
#36386=CARTESIAN_POINT('',(-0.0577350269189626,0.1,-0.1));
#36387=CARTESIAN_POINT('',(-0.0577350269189626,0.1,-0.3));
#36388=CARTESIAN_POINT('',(-0.0577350269189626,0.1,-0.1));
#36389=CARTESIAN_POINT('Origin',(0.0577350269189626,0.1,-0.3));
#36390=CARTESIAN_POINT('',(0.0577350269189626,0.1,-0.3));
#36391=CARTESIAN_POINT('',(0.0288675134594813,0.1,-0.3));
#36392=CARTESIAN_POINT('',(0.0577350269189626,0.1,-0.1));
#36393=CARTESIAN_POINT('',(0.0577350269189626,0.1,-0.3));
#36394=CARTESIAN_POINT('',(0.0577350269189626,0.1,-0.1));
#36395=CARTESIAN_POINT('Origin',(0.115470053837925,0.,-0.3));
#36396=CARTESIAN_POINT('',(0.115470053837925,0.,-0.3));
#36397=CARTESIAN_POINT('',(0.101036297108185,0.025,-0.3));
#36398=CARTESIAN_POINT('',(0.115470053837925,0.,-0.1));
#36399=CARTESIAN_POINT('',(0.115470053837925,0.,-0.3));
#36400=CARTESIAN_POINT('',(0.115470053837925,0.,-0.1));
#36401=CARTESIAN_POINT('Origin',(0.0577350269189626,-0.1,-0.3));
#36402=CARTESIAN_POINT('',(0.0721687836487032,-0.075,-0.3));
#36403=CARTESIAN_POINT('',(0.0577350269189626,-0.1,-0.1));
#36404=CARTESIAN_POINT('Origin',(0.,0.,-0.1));
#36405=CARTESIAN_POINT('Origin',(0.,0.,0.));
#36406=CARTESIAN_POINT('',(-0.3,-3.67394039744206E-17,0.));
#36407=CARTESIAN_POINT('Origin',(0.,0.,0.));
#36408=CARTESIAN_POINT('Origin',(0.,0.,-0.3));
#36409=CARTESIAN_POINT('',(-0.3,-3.67394039744206E-17,-0.3));
#36410=CARTESIAN_POINT('',(-0.3,-3.67394039744206E-17,-0.3));
#36411=CARTESIAN_POINT('Origin',(0.,0.,-0.3));
#36412=CARTESIAN_POINT('Origin',(0.,0.,-0.3));
#36413=CARTESIAN_POINT('Origin',(0.,0.,1.));
#36462=UNCERTAINTY_MEASURE_WITH_UNIT(LENGTH_MEASURE(0.001),#36483,
'DISTANCE_ACCURACY_VALUE',
'Maximum model space distance between geometric entities at asserted c
onnectivities');
#36463=UNCERTAINTY_MEASURE_WITH_UNIT(LENGTH_MEASURE(0.001),#36483,
'DISTANCE_ACCURACY_VALUE',
'Maximum model space distance between geometric entities at asserted c
onnectivities');
#36481=(
GEOMETRIC_REPRESENTATION_CONTEXT(3)
GLOBAL_UNCERTAINTY_ASSIGNED_CONTEXT((#36462))
GLOBAL_UNIT_ASSIGNED_CONTEXT((#36483,#36485,#36486))
REPRESENTATION_CONTEXT('','3D')
);
#36482=(
GEOMETRIC_REPRESENTATION_CONTEXT(3)
GLOBAL_UNCERTAINTY_ASSIGNED_CONTEXT((#36463))
GLOBAL_UNIT_ASSIGNED_CONTEXT((#36483,#36485,#36486))
REPRESENTATION_CONTEXT('','3D')
);
#36483=(
LENGTH_UNIT()
NAMED_UNIT(*)
SI_UNIT(.CENTI.,.METRE.)
);
#36485=(
NAMED_UNIT(*)
PLANE_ANGLE_UNIT()
SI_UNIT($,.RADIAN.)
);
#36486=(
NAMED_UNIT(*)
SI_UNIT($,.STERADIAN.)
SOLID_ANGLE_UNIT()
);
#36504=SHAPE_DEFINITION_REPRESENTATION(#36522,#36571);
#36522=PRODUCT_DEFINITION_SHAPE('',$,#36590);
#36571=SHAPE_REPRESENTATION('',(#10601),#36481);
#36572=PRODUCT_DEFINITION_CONTEXT('part definition',#36628,'design');
#36590=PRODUCT_DEFINITION('Socket head cap screw M3x10',
'Socket head cap screw M3x10',#36608,#36572);
#36608=PRODUCT_DEFINITION_FORMATION('',$,#36647);
#36628=APPLICATION_CONTEXT(
'Core Data for Automotive Mechanical Design Process');
#36629=PRODUCT_CONTEXT('part definition',#36628,'mechanical');
#36647=PRODUCT('Socket head cap screw M3x10',
'Socket head cap screw M3x10',$,(#36629));
#36659=PRESENTATION_STYLE_ASSIGNMENT((#36673));
#36673=SURFACE_STYLE_USAGE(.BOTH.,#36687);
#36687=SURFACE_SIDE_STYLE('',(#36701));
#36701=SURFACE_STYLE_FILL_AREA(#36715);
#36715=FILL_AREA_STYLE('Dark gray',(#36729));
#36729=FILL_AREA_STYLE_COLOUR('Dark gray',#36743);
#36743=COLOUR_RGB('Dark gray',0.250980392156863,0.282352941176471,0.32156862745098);
ENDSEC;
END-ISO-10303-21;
